ISO-10303-21;
HEADER;
/* Generated by software containing ST-Developer
 * from STEP Tools, Inc. (www.steptools.com) 
 */

FILE_DESCRIPTION(
/* description */ (''),
/* implementation_level */ '2;1');

FILE_NAME(
/* name */ 'Socket head cap screw M3x16.step',
/* time_stamp */ '2026-11-10T05:40:20-08:00',
/* author */ (''),
/* organization */ (''),
/* preprocessor_version */ 'ST-DEVELOPER v20.2',
/* originating_system */ 'Autodesk Translation Framework v15.17.0.0',
/* authorisation */ '');

FILE_SCHEMA (('AUTOMOTIVE_DESIGN { 1 0 10303 214 3 1 1 }'));
ENDSEC;

DATA;
#10=MECHANICAL_DESIGN_GEOMETRIC_PRESENTATION_REPRESENTATION('',(#577),#18580);
#75=CONICAL_SURFACE('',#7011,0.1,0.785398163397448);
#156=B_SPLINE_SURFACE_WITH_KNOTS('',3,3,((#15243,#15244,#15245,#15246,#15247,
#15248,#15249,#15250,#15251,#15252,#15253,#15254,#15255,#15256,#15257,#15258,
#15259,#15260,#15261,#15262,#15263,#15264,#15265,#15266,#15267,#15268,#15269,
#15270,#15271,#15272,#15273,#15274,#15275,#15276,#15277,#15278,#15279,#15280,
#15281,#15282,#15283,#15284,#15285,#15286,#15287,#15288,#15289,#15290,#15291,
#15292,#15293,#15294,#15295,#15296,#15297,#15298,#15299,#15300,#15301,#15302,
#15303,#15304,#15305,#15306,#15307,#15308,#15309,#15310,#15311,#15312,#15313,
#15314,#15315,#15316,#15317,#15318,#15319,#15320,#15321,#15322,#15323,#15324,
#15325,#15326,#15327,#15328,#15329,#15330,#15331,#15332,#15333,#15334,#15335,
#15336,#15337,#15338,#15339,#15340,#15341,#15342,#15343,#15344,#15345,#15346,
#15347,#15348,#15349,#15350,#15351,#15352,#15353,#15354,#15355,#15356,#15357,
#15358,#15359,#15360,#15361,#15362,#15363,#15364,#15365,#15366,#15367,#15368,
#15369,#15370,#15371,#15372,#15373,#15374,#15375,#15376,#15377,#15378,#15379,
#15380,#15381,#15382,#15383,#15384,#15385,#15386,#15387,#15388,#15389,#15390,
#15391,#15392,#15393,#15394,#15395,#15396,#15397,#15398,#15399,#15400,#15401,
#15402,#15403,#15404,#15405,#15406,#15407,#15408,#15409,#15410,#15411,#15412,
#15413,#15414,#15415,#15416,#15417,#15418,#15419,#15420,#15421,#15422,#15423,
#15424,#15425,#15426,#15427,#15428,#15429,#15430,#15431,#15432,#15433,#15434,
#15435,#15436,#15437,#15438),(#15439,#15440,#15441,#15442,#15443,#15444,
#15445,#15446,#15447,#15448,#15449,#15450,#15451,#15452,#15453,#15454,#15455,
#15456,#15457,#15458,#15459,#15460,#15461,#15462,#15463,#15464,#15465,#15466,
#15467,#15468,#15469,#15470,#15471,#15472,#15473,#15474,#15475,#15476,#15477,
#15478,#15479,#15480,#15481,#15482,#15483,#15484,#15485,#15486,#15487,#15488,
#15489,#15490,#15491,#15492,#15493,#15494,#15495,#15496,#15497,#15498,#15499,
#15500,#15501,#15502,#15503,#15504,#15505,#15506,#15507,#15508,#15509,#15510,
#15511,#15512,#15513,#15514,#15515,#15516,#15517,#15518,#15519,#15520,#15521,
#15522,#15523,#15524,#15525,#15526,#15527,#15528,#15529,#15530,#15531,#15532,
#15533,#15534,#15535,#15536,#15537,#15538,#15539,#15540,#15541,#15542,#15543,
#15544,#15545,#15546,#15547,#15548,#15549,#15550,#15551,#15552,#15553,#15554,
#15555,#15556,#15557,#15558,#15559,#15560,#15561,#15562,#15563,#15564,#15565,
#15566,#15567,#15568,#15569,#15570,#15571,#15572,#15573,#15574,#15575,#15576,
#15577,#15578,#15579,#15580,#15581,#15582,#15583,#15584,#15585,#15586,#15587,
#15588,#15589,#15590,#15591,#15592,#15593,#15594,#15595,#15596,#15597,#15598,
#15599,#15600,#15601,#15602,#15603,#15604,#15605,#15606,#15607,#15608,#15609,
#15610,#15611,#15612,#15613,#15614,#15615,#15616,#15617,#15618,#15619,#15620,
#15621,#15622,#15623,#15624,#15625,#15626,#15627,#15628,#15629,#15630,#15631,
#15632,#15633,#15634),(#15635,#15636,#15637,#15638,#15639,#15640,#15641,
#15642,#15643,#15644,#15645,#15646,#15647,#15648,#15649,#15650,#15651,#15652,
#15653,#15654,#15655,#15656,#15657,#15658,#15659,#15660,#15661,#15662,#15663,
#15664,#15665,#15666,#15667,#15668,#15669,#15670,#15671,#15672,#15673,#15674,
#15675,#15676,#15677,#15678,#15679,#15680,#15681,#15682,#15683,#15684,#15685,
#15686,#15687,#15688,#15689,#15690,#15691,#15692,#15693,#15694,#15695,#15696,
#15697,#15698,#15699,#15700,#15701,#15702,#15703,#15704,#15705,#15706,#15707,
#15708,#15709,#15710,#15711,#15712,#15713,#15714,#15715,#15716,#15717,#15718,
#15719,#15720,#15721,#15722,#15723,#15724,#15725,#15726,#15727,#15728,#15729,
#15730,#15731,#15732,#15733,#15734,#15735,#15736,#15737,#15738,#15739,#15740,
#15741,#15742,#15743,#15744,#15745,#15746,#15747,#15748,#15749,#15750,#15751,
#15752,#15753,#15754,#15755,#15756,#15757,#15758,#15759,#15760,#15761,#15762,
#15763,#15764,#15765,#15766,#15767,#15768,#15769,#15770,#15771,#15772,#15773,
#15774,#15775,#15776,#15777,#15778,#15779,#15780,#15781,#15782,#15783,#15784,
#15785,#15786,#15787,#15788,#15789,#15790,#15791,#15792,#15793,#15794,#15795,
#15796,#15797,#15798,#15799,#15800,#15801,#15802,#15803,#15804,#15805,#15806,
#15807,#15808,#15809,#15810,#15811,#15812,#15813,#15814,#15815,#15816,#15817,
#15818,#15819,#15820,#15821,#15822,#15823,#15824,#15825,#15826,#15827,#15828,
#15829,#15830),(#15831,#15832,#15833,#15834,#15835,#15836,#15837,#15838,
#15839,#15840,#15841,#15842,#15843,#15844,#15845,#15846,#15847,#15848,#15849,
#15850,#15851,#15852,#15853,#15854,#15855,#15856,#15857,#15858,#15859,#15860,
#15861,#15862,#15863,#15864,#15865,#15866,#15867,#15868,#15869,#15870,#15871,
#15872,#15873,#15874,#15875,#15876,#15877,#15878,#15879,#15880,#15881,#15882,
#15883,#15884,#15885,#15886,#15887,#15888,#15889,#15890,#15891,#15892,#15893,
#15894,#15895,#15896,#15897,#15898,#15899,#15900,#15901,#15902,#15903,#15904,
#15905,#15906,#15907,#15908,#15909,#15910,#15911,#15912,#15913,#15914,#15915,
#15916,#15917,#15918,#15919,#15920,#15921,#15922,#15923,#15924,#15925,#15926,
#15927,#15928,#15929,#15930,#15931,#15932,#15933,#15934,#15935,#15936,#15937,
#15938,#15939,#15940,#15941,#15942,#15943,#15944,#15945,#15946,#15947,#15948,
#15949,#15950,#15951,#15952,#15953,#15954,#15955,#15956,#15957,#15958,#15959,
#15960,#15961,#15962,#15963,#15964,#15965,#15966,#15967,#15968,#15969,#15970,
#15971,#15972,#15973,#15974,#15975,#15976,#15977,#15978,#15979,#15980,#15981,
#15982,#15983,#15984,#15985,#15986,#15987,#15988,#15989,#15990,#15991,#15992,
#15993,#15994,#15995,#15996,#15997,#15998,#15999,#16000,#16001,#16002,#16003,
#16004,#16005,#16006,#16007,#16008,#16009,#16010,#16011,#16012,#16013,#16014,
#16015,#16016,#16017,#16018,#16019,#16020,#16021,#16022,#16023,#16024,#16025,
#16026)),.UNSPECIFIED.,.F.,.F.,.F.,(4,4),(4,1,1,1,1,1,1,1,1,1,1,1,1,1,1,
1,1,1,1,1,1,1,1,1,1,1,1,1,1,1,1,1,1,1,1,1,1,1,1,1,1,1,1,1,1,1,1,1,1,1,1,
1,1,1,1,1,1,1,1,1,1,1,1,1,1,1,1,1,1,1,1,1,1,1,1,1,1,1,1,1,1,1,1,1,1,1,1,
1,1,1,1,1,1,1,1,1,1,1,1,1,1,1,1,1,1,1,1,1,1,1,1,1,1,1,1,1,1,1,1,1,1,1,1,
1,1,1,1,1,1,1,1,1,1,1,1,1,1,1,1,1,1,1,1,1,1,1,1,1,1,1,1,1,1,1,1,1,1,1,1,
1,1,1,1,1,1,1,1,1,1,1,1,1,1,1,1,1,1,1,1,1,1,1,1,1,1,1,1,1,1,1,1,1,1,4),
(0.,0.0329955678841871),(11.6159397475006,12.61358260836,13.6112254692194,
14.6088683300789,15.6065111909383,16.6041540517977,17.6017969126571,18.5994397735165,
19.5970826343759,20.5947254952353,21.5923683560947,22.5900112169541,23.5876540778135,
24.5852969386729,25.5829397995323,26.5805826603917,27.5782255212511,28.5758683821105,
29.5735112429699,30.5711541038294,31.5687969646888,32.5664398255482,33.5640826864076,
34.561725547267,35.5593684081264,36.5570112689858,37.5546541298452,38.5522969907046,
39.549939851564,40.5475827124234,41.5452255732828,42.5428684341422,43.5405112950016,
44.538154155861,45.5357970167204,46.5334398775799,47.5310827384393,48.5287255992987,
49.5263684601581,50.5240113210175,51.5216541818769,52.5192970427363,53.5169399035957,
54.5145827644551,55.5122256253145,56.5098684861739,57.5075113470333,58.5051542078927,
59.5027970687521,60.5004399296115,61.4980827904709,62.4957256513303,63.4933685121897,
64.4910113730492,65.4886542339086,66.486297094768,67.4839399556274,68.4815828164868,
69.4792256773462,70.4768685382056,71.474511399065,72.4721542599244,73.4697971207838,
74.4674399816432,75.4650828425026,76.462725703362,77.4603685642214,78.4580114250808,
79.4556542859402,80.4532971467996,81.4509400076591,82.4485828685185,83.4462257293779,
84.4438685902373,85.4415114510967,86.4391543119561,87.4367971728155,88.4344400336749,
89.4320828945343,90.4297257553937,91.4273686162531,92.4250114771125,93.4226543379719,
94.4202971988313,95.4179400596907,96.4155829205502,97.4132257814096,98.410868642269,
99.4085115031284,100.406154363988,101.403797224847,102.401440085707,103.399082946566,
104.396725807425,105.394368668285,106.392011529144,107.389654390004,108.387297250863,
109.384940111722,110.382582972582,111.380225833441,112.377868694301,113.37551155516,
114.373154416019,115.370797276879,116.368440137738,117.366082998598,118.363725859457,
119.361368720316,120.359011581176,121.356654442035,122.354297302895,123.351940163754,
124.349583024614,125.347225885473,126.344868746332,127.342511607192,128.340154468051,
129.337797328911,130.33544018977,131.333083050629,132.330725911489,133.328368772348,
134.326011633208,135.323654494067,136.321297354926,137.318940215786,138.316583076645,
139.314225937505,140.311868798364,141.309511659223,142.307154520083,143.304797380942,
144.302440241802,145.300083102661,146.29772596352,147.29536882438,148.293011685239,
149.290654546099,150.288297406958,151.285940267817,152.283583128677,153.281225989536,
154.278868850396,155.276511711255,156.274154572115,157.271797432974,158.269440293833,
159.267083154693,160.264726015552,161.262368876412,162.260011737271,163.25765459813,
164.25529745899,165.252940319849,166.250583180709,167.248226041568,168.245868902427,
169.243511763287,170.241154624146,171.238797485006,172.236440345865,173.234083206724,
174.231726067584,175.229368928443,176.227011789303,177.224654650162,178.222297511021,
179.219940371881,180.21758323274,181.2152260936,182.212868954459,183.210511815318,
184.208154676178,185.205797537037,186.203440397897,187.201083258756,188.198726119616,
189.196368980475,190.194011841334,191.191654702194,192.189297563053,193.186940423913,
194.184583284772,195.182226145631,196.179869006491,197.17751186735,198.17515472821,
199.172797589069,200.170440449928,201.168083310788,202.165726171647,203.163369032507,
204.161011893366),.UNSPECIFIED.);
#157=B_SPLINE_SURFACE_WITH_KNOTS('',3,3,((#16116,#16117,#16118,#16119,#16120,
#16121,#16122,#16123,#16124,#16125,#16126,#16127,#16128,#16129,#16130,#16131,
#16132,#16133,#16134,#16135,#16136,#16137,#16138,#16139,#16140,#16141,#16142,
#16143,#16144,#16145,#16146,#16147,#16148,#16149,#16150,#16151,#16152,#16153,
#16154,#16155,#16156,#16157,#16158,#16159,#16160,#16161,#16162,#16163,#16164,
#16165,#16166,#16167,#16168,#16169,#16170,#16171,#16172,#16173,#16174,#16175,
#16176,#16177,#16178,#16179,#16180,#16181,#16182,#16183,#16184,#16185,#16186,
#16187,#16188,#16189,#16190,#16191,#16192,#16193,#16194,#16195,#16196,#16197,
#16198,#16199,#16200,#16201,#16202,#16203,#16204,#16205,#16206,#16207,#16208,
#16209,#16210,#16211,#16212,#16213,#16214,#16215,#16216,#16217,#16218,#16219,
#16220,#16221,#16222,#16223,#16224,#16225,#16226,#16227,#16228,#16229,#16230,
#16231,#16232,#16233,#16234,#16235,#16236,#16237,#16238,#16239,#16240,#16241,
#16242,#16243,#16244,#16245,#16246,#16247,#16248,#16249,#16250,#16251,#16252,
#16253,#16254,#16255,#16256,#16257,#16258,#16259,#16260,#16261,#16262,#16263,
#16264,#16265,#16266,#16267,#16268,#16269,#16270,#16271,#16272,#16273,#16274,
#16275,#16276,#16277,#16278,#16279,#16280,#16281,#16282,#16283,#16284,#16285,
#16286,#16287,#16288,#16289,#16290,#16291,#16292,#16293,#16294,#16295,#16296,
#16297,#16298,#16299,#16300,#16301,#16302,#16303,#16304,#16305,#16306,#16307,
#16308,#16309,#16310,#16311,#16312,#16313),(#16314,#16315,#16316,#16317,
#16318,#16319,#16320,#16321,#16322,#16323,#16324,#16325,#16326,#16327,#16328,
#16329,#16330,#16331,#16332,#16333,#16334,#16335,#16336,#16337,#16338,#16339,
#16340,#16341,#16342,#16343,#16344,#16345,#16346,#16347,#16348,#16349,#16350,
#16351,#16352,#16353,#16354,#16355,#16356,#16357,#16358,#16359,#16360,#16361,
#16362,#16363,#16364,#16365,#16366,#16367,#16368,#16369,#16370,#16371,#16372,
#16373,#16374,#16375,#16376,#16377,#16378,#16379,#16380,#16381,#16382,#16383,
#16384,#16385,#16386,#16387,#16388,#16389,#16390,#16391,#16392,#16393,#16394,
#16395,#16396,#16397,#16398,#16399,#16400,#16401,#16402,#16403,#16404,#16405,
#16406,#16407,#16408,#16409,#16410,#16411,#16412,#16413,#16414,#16415,#16416,
#16417,#16418,#16419,#16420,#16421,#16422,#16423,#16424,#16425,#16426,#16427,
#16428,#16429,#16430,#16431,#16432,#16433,#16434,#16435,#16436,#16437,#16438,
#16439,#16440,#16441,#16442,#16443,#16444,#16445,#16446,#16447,#16448,#16449,
#16450,#16451,#16452,#16453,#16454,#16455,#16456,#16457,#16458,#16459,#16460,
#16461,#16462,#16463,#16464,#16465,#16466,#16467,#16468,#16469,#16470,#16471,
#16472,#16473,#16474,#16475,#16476,#16477,#16478,#16479,#16480,#16481,#16482,
#16483,#16484,#16485,#16486,#16487,#16488,#16489,#16490,#16491,#16492,#16493,
#16494,#16495,#16496,#16497,#16498,#16499,#16500,#16501,#16502,#16503,#16504,
#16505,#16506,#16507,#16508,#16509,#16510,#16511),(#16512,#16513,#16514,
#16515,#16516,#16517,#16518,#16519,#16520,#16521,#16522,#16523,#16524,#16525,
#16526,#16527,#16528,#16529,#16530,#16531,#16532,#16533,#16534,#16535,#16536,
#16537,#16538,#16539,#16540,#16541,#16542,#16543,#16544,#16545,#16546,#16547,
#16548,#16549,#16550,#16551,#16552,#16553,#16554,#16555,#16556,#16557,#16558,
#16559,#16560,#16561,#16562,#16563,#16564,#16565,#16566,#16567,#16568,#16569,
#16570,#16571,#16572,#16573,#16574,#16575,#16576,#16577,#16578,#16579,#16580,
#16581,#16582,#16583,#16584,#16585,#16586,#16587,#16588,#16589,#16590,#16591,
#16592,#16593,#16594,#16595,#16596,#16597,#16598,#16599,#16600,#16601,#16602,
#16603,#16604,#16605,#16606,#16607,#16608,#16609,#16610,#16611,#16612,#16613,
#16614,#16615,#16616,#16617,#16618,#16619,#16620,#16621,#16622,#16623,#16624,
#16625,#16626,#16627,#16628,#16629,#16630,#16631,#16632,#16633,#16634,#16635,
#16636,#16637,#16638,#16639,#16640,#16641,#16642,#16643,#16644,#16645,#16646,
#16647,#16648,#16649,#16650,#16651,#16652,#16653,#16654,#16655,#16656,#16657,
#16658,#16659,#16660,#16661,#16662,#16663,#16664,#16665,#16666,#16667,#16668,
#16669,#16670,#16671,#16672,#16673,#16674,#16675,#16676,#16677,#16678,#16679,
#16680,#16681,#16682,#16683,#16684,#16685,#16686,#16687,#16688,#16689,#16690,
#16691,#16692,#16693,#16694,#16695,#16696,#16697,#16698,#16699,#16700,#16701,
#16702,#16703,#16704,#16705,#16706,#16707,#16708,#16709),(#16710,#16711,
#16712,#16713,#16714,#16715,#16716,#16717,#16718,#16719,#16720,#16721,#16722,
#16723,#16724,#16725,#16726,#16727,#16728,#16729,#16730,#16731,#16732,#16733,
#16734,#16735,#16736,#16737,#16738,#16739,#16740,#16741,#16742,#16743,#16744,
#16745,#16746,#16747,#16748,#16749,#16750,#16751,#16752,#16753,#16754,#16755,
#16756,#16757,#16758,#16759,#16760,#16761,#16762,#16763,#16764,#16765,#16766,
#16767,#16768,#16769,#16770,#16771,#16772,#16773,#16774,#16775,#16776,#16777,
#16778,#16779,#16780,#16781,#16782,#16783,#16784,#16785,#16786,#16787,#16788,
#16789,#16790,#16791,#16792,#16793,#16794,#16795,#16796,#16797,#16798,#16799,
#16800,#16801,#16802,#16803,#16804,#16805,#16806,#16807,#16808,#16809,#16810,
#16811,#16812,#16813,#16814,#16815,#16816,#16817,#16818,#16819,#16820,#16821,
#16822,#16823,#16824,#16825,#16826,#16827,#16828,#16829,#16830,#16831,#16832,
#16833,#16834,#16835,#16836,#16837,#16838,#16839,#16840,#16841,#16842,#16843,
#16844,#16845,#16846,#16847,#16848,#16849,#16850,#16851,#16852,#16853,#16854,
#16855,#16856,#16857,#16858,#16859,#16860,#16861,#16862,#16863,#16864,#16865,
#16866,#16867,#16868,#16869,#16870,#16871,#16872,#16873,#16874,#16875,#16876,
#16877,#16878,#16879,#16880,#16881,#16882,#16883,#16884,#16885,#16886,#16887,
#16888,#16889,#16890,#16891,#16892,#16893,#16894,#16895,#16896,#16897,#16898,
#16899,#16900,#16901,#16902,#16903,#16904,#16905,#16906,#16907)),
 .UNSPECIFIED.,.F.,.F.,.F.,(4,4),(4,1,1,1,1,1,1,1,1,1,1,1,1,1,1,1,1,1,1,
1,1,1,1,1,1,1,1,1,1,1,1,1,1,1,1,1,1,1,1,1,1,1,1,1,1,1,1,1,1,1,1,1,1,1,1,
1,1,1,1,1,1,1,1,1,1,1,1,1,1,1,1,1,1,1,1,1,1,1,1,1,1,1,1,1,1,1,1,1,1,1,1,
1,1,1,1,1,1,1,1,1,1,1,1,1,1,1,1,1,1,1,1,1,1,1,1,1,1,1,1,1,1,1,1,1,1,1,1,
1,1,1,1,1,1,1,1,1,1,1,1,1,1,1,1,1,1,1,1,1,1,1,1,1,1,1,1,1,1,1,1,1,1,1,1,
1,1,1,1,1,1,1,1,1,1,1,1,1,1,1,1,1,1,1,1,1,1,1,1,1,1,1,1,1,1,1,1,4),(0.,
0.0329955678841871),(8.30203615430855,9.30007843543257,10.2981207165566,
11.2961629976806,12.2942052788047,13.2922475599287,14.2902898410527,15.2883321221767,
16.2863744033008,17.2844166844248,18.2824589655488,19.2805012466728,20.2785435277969,
21.2765858089209,22.2746280900449,23.272670371169,24.270712652293,25.268754933417,
26.266797214541,27.2648394956651,28.2628817767891,29.2609240579131,30.2589663390371,
31.2570086201612,32.2550509012852,33.2530931824092,34.2511354635333,35.2491777446573,
36.2472200257813,37.2452623069053,38.2433045880294,39.2413468691534,40.2393891502774,
41.2374314314014,42.2354737125255,43.2335159936495,44.2315582747735,45.2296005558975,
46.2276428370216,47.2256851181456,48.2237273992696,49.2217696803937,50.2198119615177,
51.2178542426417,52.2158965237657,53.2139388048898,54.2119810860138,55.2100233671378,
56.2080656482619,57.2061079293859,58.2041502105099,59.2021924916339,60.200234772758,
61.198277053882,62.196319335006,63.19436161613,64.1924038972541,65.1904461783781,
66.1884884595021,67.1865307406262,68.1845730217502,69.1826153028742,70.1806575839982,
71.1786998651223,72.1767421462463,73.1747844273703,74.1728267084943,75.1708689896184,
76.1689112707424,77.1669535518664,78.1649958329905,79.1630381141145,80.1610803952385,
81.1591226763625,82.1571649574865,83.1552072386106,84.1532495197346,85.1512918008586,
86.1493340819827,87.1473763631067,88.1454186442307,89.1434609253548,90.1415032064788,
91.1395454876028,92.1375877687268,93.1356300498508,94.1336723309749,95.1317146120989,
96.1297568932229,97.127799174347,98.125841455471,99.123883736595,100.121926017719,
101.119968298843,102.118010579967,103.116052861091,104.114095142215,105.112137423339,
106.110179704463,107.108221985587,108.106264266711,109.104306547835,110.102348828959,
111.100391110083,112.098433391207,113.096475672331,114.094517953455,115.092560234579,
116.090602515703,117.088644796828,118.086687077952,119.084729359076,120.0827716402,
121.080813921324,122.078856202448,123.076898483572,124.074940764696,125.07298304582,
126.071025326944,127.069067608068,128.067109889192,129.065152170316,130.06319445144,
131.061236732564,132.059279013688,133.057321294812,134.055363575936,135.05340585706,
136.051448138184,137.049490419308,138.047532700432,139.045574981556,140.04361726268,
141.041659543804,142.039701824928,143.037744106052,144.035786387176,145.0338286683,
146.031870949424,147.029913230548,148.027955511672,149.025997792796,150.02404007392,
151.022082355044,152.020124636168,153.018166917292,154.016209198417,155.014251479541,
156.012293760665,157.010336041789,158.008378322913,159.006420604037,160.004462885161,
161.002505166285,162.000547447409,162.998589728533,163.996632009657,164.994674290781,
165.992716571905,166.990758853029,167.988801134153,168.986843415277,169.984885696401,
170.982927977525,171.980970258649,172.979012539773,173.977054820897,174.975097102021,
175.973139383145,176.971181664269,177.969223945393,178.967266226517,179.965308507641,
180.963350788765,181.961393069889,182.959435351013,183.957477632137,184.955519913261,
185.953562194385,186.951604475509,187.949646756633,188.947689037757,189.945731318881,
190.943773600006,191.94181588113,192.939858162254,193.937900443378,194.935942724502,
195.933985005626,196.93202728675,197.930069567874,198.928111848998,199.926154130122,
200.924196411246,201.92223869237,202.920280973494),.UNSPECIFIED.);
#372=B_SPLINE_CURVE_WITH_KNOTS('',3,(#12867,#12868,#12869,#12870,#12871,
#12872,#12873,#12874,#12875,#12876),.UNSPECIFIED.,.F.,.F.,(4,3,3,4),(-4.09202352044852,
-3.99057144343763,-2.99292858257822,-2.07317267331971),.UNSPECIFIED.);
#373=B_SPLINE_CURVE_WITH_KNOTS('',3,(#12879,#12880,#12881,#12882,#12883,
#12884,#12885),.UNSPECIFIED.,.F.,.F.,(4,3,4),(0.,0.998042281124014,1.12274180646116),
 .UNSPECIFIED.);
#374=B_SPLINE_CURVE_WITH_KNOTS('',3,(#12890,#12891,#12892,#12893,#12894,
#12895,#12896,#12897,#12898,#12899,#12900,#12901,#12902,#12903,#12904,#12905,
#12906,#12907,#12908,#12909,#12910,#12911),.UNSPECIFIED.,.F.,.F.,(4,3,3,
3,3,3,3,4),(-10.3752088276281,-9.97642860859406,-8.97878574773466,-7.98114288687525,
-6.98350002601584,-5.98585716515644,-4.98821430429703,-4.09202352044852),
 .UNSPECIFIED.);
#375=B_SPLINE_CURVE_WITH_KNOTS('',3,(#12912,#12913,#12914,#12915,#12916,
#12917,#12918,#12919,#12920,#12921,#12922,#12923,#12924,#12925,#12926,#12927,
#12928,#12929,#12930,#12931,#12932,#12933),.UNSPECIFIED.,.F.,.F.,(4,3,3,
3,3,3,3,4),(1.12274180646116,1.99608456224804,2.99412684337208,3.99216912449611,
4.99021140562014,5.98825368674417,6.98629596786821,7.40592711364074),
 .UNSPECIFIED.);
#376=B_SPLINE_CURVE_WITH_KNOTS('',3,(#12938,#12939,#12940,#12941,#12942,
#12943,#12944,#12945,#12946,#12947,#12948,#12949,#12950,#12951,#12952,#12953,
#12954,#12955,#12956,#12957,#12958,#12959),.UNSPECIFIED.,.F.,.F.,(4,3,3,
3,3,3,3,4),(-16.6583941348077,-15.9622857737505,-14.9646429128911,-13.9670000520317,
-12.9693571911723,-11.9717143303129,-10.9740714694535,-10.3752088276281),
 .UNSPECIFIED.);
#377=B_SPLINE_CURVE_WITH_KNOTS('',3,(#12960,#12961,#12962,#12963,#12964,
#12965,#12966,#12967,#12968,#12969,#12970,#12971,#12972,#12973,#12974,#12975,
#12976,#12977,#12978,#12979,#12980,#12981),.UNSPECIFIED.,.F.,.F.,(4,3,3,
3,3,3,3,4),(7.40592711364074,7.98433824899223,8.98238053011626,9.98042281124028,
10.9784650923643,11.9765073734883,12.9745496546124,13.6891124208203),
 .UNSPECIFIED.);
#378=B_SPLINE_CURVE_WITH_KNOTS('',3,(#12986,#12987,#12988,#12989,#12990,
#12991,#12992,#12993,#12994,#12995,#12996,#12997,#12998,#12999,#13000,#13001,
#13002,#13003,#13004,#13005,#13006,#13007),.UNSPECIFIED.,.F.,.F.,(4,3,3,
3,3,3,3,4),(-22.9415794419873,-21.9481429389069,-20.9505000780475,-19.9528572171881,
-18.9552143563287,-17.9575714954693,-16.9599286346099,-16.6583941348077),
 .UNSPECIFIED.);
#379=B_SPLINE_CURVE_WITH_KNOTS('',3,(#13008,#13009,#13010,#13011,#13012,
#13013,#13014,#13015,#13016,#13017,#13018,#13019,#13020,#13021,#13022,#13023,
#13024,#13025,#13026,#13027,#13028,#13029,#13030,#13031,#13032),
 .UNSPECIFIED.,.F.,.F.,(4,3,3,3,3,3,3,3,4),(13.6891124208203,13.9725919357364,
14.9706342168604,15.9686764979844,16.9667187791085,17.9647610602325,18.9628033413565,
19.9608456224805,19.9722977279999),.UNSPECIFIED.);
#380=B_SPLINE_CURVE_WITH_KNOTS('',3,(#13037,#13038,#13039,#13040,#13041,
#13042,#13043,#13044,#13045,#13046,#13047,#13048,#13049,#13050,#13051,#13052,
#13053,#13054,#13055,#13056,#13057,#13058),.UNSPECIFIED.,.F.,.F.,(4,3,3,
3,3,3,3,4),(-29.2247647491669,-28.9316429649228,-27.9340001040634,-26.936357243204,
-25.9387143823446,-24.9410715214852,-23.9434286606257,-22.9415794419873),
 .UNSPECIFIED.);
#381=B_SPLINE_CURVE_WITH_KNOTS('',3,(#13059,#13060,#13061,#13062,#13063,
#13064,#13065,#13066,#13067,#13068,#13069,#13070,#13071,#13072,#13073,#13074,
#13075,#13076,#13077,#13078,#13079,#13080),.UNSPECIFIED.,.F.,.F.,(4,3,3,
3,3,3,3,4),(19.9722977279999,20.9588879036046,21.9569301847286,22.9549724658526,
23.9530147469767,24.9510570281007,25.9490993092247,26.2554830351795),
 .UNSPECIFIED.);
#382=B_SPLINE_CURVE_WITH_KNOTS('',3,(#13085,#13086,#13087,#13088,#13089,
#13090,#13091,#13092,#13093,#13094,#13095,#13096,#13097,#13098,#13099,#13100,
#13101,#13102,#13103,#13104,#13105,#13106),.UNSPECIFIED.,.F.,.F.,(4,3,3,
3,3,3,3,4),(-35.5079500563465,-34.9175001300792,-33.9198572692198,-32.9222144083604,
-31.924571547501,-30.9269286866416,-29.9292858257822,-29.2247647491669),
 .UNSPECIFIED.);
#383=B_SPLINE_CURVE_WITH_KNOTS('',3,(#13107,#13108,#13109,#13110,#13111,
#13112,#13113,#13114,#13115,#13116,#13117,#13118,#13119,#13120,#13121,#13122,
#13123,#13124,#13125,#13126,#13127,#13128),.UNSPECIFIED.,.F.,.F.,(4,3,3,
3,3,3,3,4),(26.2554830351795,26.9471415903487,27.9451838714728,28.9432261525968,
29.9412684337208,30.9393107148448,31.9373529959689,32.5386683423591),
 .UNSPECIFIED.);
#384=B_SPLINE_CURVE_WITH_KNOTS('',3,(#13133,#13134,#13135,#13136,#13137,
#13138,#13139,#13140,#13141,#13142,#13143,#13144,#13145,#13146,#13147,#13148,
#13149,#13150,#13151,#13152,#13153,#13154),.UNSPECIFIED.,.F.,.F.,(4,3,3,
3,3,3,3,4),(-41.791135363526,-40.9033572952357,-39.9057144343762,-38.9080715735168,
-37.9104287126574,-36.912785851798,-35.9151429909386,-35.5079500563465),
 .UNSPECIFIED.);
#385=B_SPLINE_CURVE_WITH_KNOTS('',3,(#13155,#13156,#13157,#13158,#13159,
#13160,#13161,#13162,#13163,#13164,#13165,#13166,#13167,#13168,#13169,#13170,
#13171,#13172,#13173,#13174,#13175,#13176),.UNSPECIFIED.,.F.,.F.,(4,3,3,
3,3,3,3,4),(32.5386683423591,32.9353952770929,33.9334375582169,34.931479839341,
35.929522120465,36.927564401589,37.9256066827131,38.8218536495387),
 .UNSPECIFIED.);
#386=B_SPLINE_CURVE_WITH_KNOTS('',3,(#13181,#13182,#13183,#13184,#13185,
#13186,#13187,#13188,#13189,#13190,#13191,#13192,#13193,#13194,#13195,#13196,
#13197,#13198,#13199,#13200,#13201,#13202,#13203,#13204,#13205),
 .UNSPECIFIED.,.F.,.F.,(4,3,3,3,3,3,3,3,4),(-48.0743206707056,-47.8868573212515,
-46.8892144603921,-45.8915715995327,-44.8939287386733,-43.8962858778139,
-42.8986430169545,-41.9010001560951,-41.791135363526),.UNSPECIFIED.);
#387=B_SPLINE_CURVE_WITH_KNOTS('',3,(#13206,#13207,#13208,#13209,#13210,
#13211,#13212,#13213,#13214,#13215,#13216,#13217,#13218,#13219,#13220,#13221,
#13222,#13223,#13224,#13225,#13226,#13227,#13228,#13229,#13230),
 .UNSPECIFIED.,.F.,.F.,(4,3,3,3,3,3,3,3,4),(38.8218536495387,38.9236489638371,
39.9216912449611,40.9197335260851,41.9177758072091,42.9158180883332,43.9138603694572,
44.9119026505812,45.1050389567183),.UNSPECIFIED.);
#388=B_SPLINE_CURVE_WITH_KNOTS('',3,(#13235,#13236,#13237,#13238,#13239,
#13240,#13241,#13242,#13243,#13244,#13245,#13246,#13247,#13248,#13249,#13250,
#13251,#13252,#13253,#13254,#13255,#13256),.UNSPECIFIED.,.F.,.F.,(4,3,3,
3,3,3,3,4),(-54.3575059778852,-53.8727144864079,-52.8750716255485,-51.8774287646891,
-50.8797859038297,-49.8821430429703,-48.8845001821109,-48.0743206707056),
 .UNSPECIFIED.);
#389=B_SPLINE_CURVE_WITH_KNOTS('',3,(#13257,#13258,#13259,#13260,#13261,
#13262,#13263,#13264,#13265,#13266,#13267,#13268,#13269,#13270,#13271,#13272,
#13273,#13274,#13275,#13276,#13277,#13278),.UNSPECIFIED.,.F.,.F.,(4,3,3,
3,3,3,3,4),(45.1050389567183,45.9099449317052,46.9079872128293,47.9060294939533,
48.9040717750773,49.9021140562014,50.9001563373254,51.3882242638979),
 .UNSPECIFIED.);
#390=B_SPLINE_CURVE_WITH_KNOTS('',3,(#13283,#13284,#13285,#13286,#13287,
#13288,#13289,#13290,#13291,#13292,#13293,#13294,#13295,#13296,#13297,#13298,
#13299,#13300,#13301,#13302,#13303,#13304),.UNSPECIFIED.,.F.,.F.,(4,3,3,
3,3,3,3,4),(-60.6406912850648,-59.8585716515644,-58.860928790705,-57.8632859298455,
-56.8656430689861,-55.8680002081267,-54.8703573472673,-54.3575059778852),
 .UNSPECIFIED.);
#391=B_SPLINE_CURVE_WITH_KNOTS('',3,(#13305,#13306,#13307,#13308,#13309,
#13310,#13311,#13312,#13313,#13314,#13315,#13316,#13317,#13318,#13319,#13320,
#13321,#13322,#13323,#13324,#13325,#13326),.UNSPECIFIED.,.F.,.F.,(4,3,3,
3,3,3,3,4),(51.3882242638979,51.8981986184494,52.8962408995734,53.8942831806975,
54.8923254618215,55.8903677429455,56.8884100240695,57.6714095710775),
 .UNSPECIFIED.);
#392=B_SPLINE_CURVE_WITH_KNOTS('',3,(#13331,#13332,#13333,#13334,#13335,
#13336,#13337,#13338,#13339,#13340,#13341,#13342,#13343,#13344,#13345,#13346,
#13347,#13348,#13349,#13350,#13351,#13352,#13353,#13354,#13355),
 .UNSPECIFIED.,.F.,.F.,(4,3,3,3,3,3,3,3,4),(-66.9238765922444,-66.8420716775802,
-65.8444288167208,-64.8467859558614,-63.849143095002,-62.8515002341426,
-61.8538573732832,-60.8562145124238,-60.6406912850648),.UNSPECIFIED.);
#393=B_SPLINE_CURVE_WITH_KNOTS('',3,(#13356,#13357,#13358,#13359,#13360,
#13361,#13362,#13363,#13364,#13365,#13366,#13367,#13368,#13369,#13370,#13371,
#13372,#13373,#13374,#13375,#13376,#13377,#13378,#13379,#13380),
 .UNSPECIFIED.,.F.,.F.,(4,3,3,3,3,3,3,3,4),(57.6714095710775,57.8864523051936,
58.8844945863176,59.8825368674416,60.8805791485657,61.8786214296897,62.8766637108137,
63.8747059919378,63.9545948782571),.UNSPECIFIED.);
#394=B_SPLINE_CURVE_WITH_KNOTS('',3,(#13385,#13386,#13387,#13388,#13389,
#13390,#13391,#13392,#13393,#13394,#13395,#13396,#13397,#13398,#13399,#13400,
#13401,#13402,#13403,#13404,#13405,#13406),.UNSPECIFIED.,.F.,.F.,(4,3,3,
3,3,3,3,4),(-73.207061899424,-72.8279288427366,-71.8302859818773,-70.8326431210178,
-69.8350002601584,-68.837357399299,-67.8397145384396,-66.9238765922444),
 .UNSPECIFIED.);
#395=B_SPLINE_CURVE_WITH_KNOTS('',3,(#13407,#13408,#13409,#13410,#13411,
#13412,#13413,#13414,#13415,#13416,#13417,#13418,#13419,#13420,#13421,#13422,
#13423,#13424,#13425,#13426,#13427,#13428),.UNSPECIFIED.,.F.,.F.,(4,3,3,
3,3,3,3,4),(63.9545948782571,64.8727482730618,65.8707905541858,66.8688328353098,
67.8668751164338,68.8649173975579,69.8629596786819,70.2377801854366),
 .UNSPECIFIED.);
#396=B_SPLINE_CURVE_WITH_KNOTS('',3,(#13433,#13434,#13435,#13436,#13437,
#13438,#13439,#13440,#13441,#13442,#13443,#13444,#13445,#13446,#13447,#13448,
#13449,#13450,#13451,#13452,#13453,#13454),.UNSPECIFIED.,.F.,.F.,(4,3,3,
3,3,3,3,4),(-79.4902472066036,-78.8137860078931,-77.8161431470337,-76.8185002861743,
-75.8208574253149,-74.8232145644555,-73.825571703596,-73.207061899424),
 .UNSPECIFIED.);
#397=B_SPLINE_CURVE_WITH_KNOTS('',3,(#13455,#13456,#13457,#13458,#13459,
#13460,#13461,#13462,#13463,#13464,#13465,#13466,#13467,#13468,#13469,#13470,
#13471,#13472,#13473,#13474,#13475,#13476),.UNSPECIFIED.,.F.,.F.,(4,3,3,
3,3,3,3,4),(70.2377801854366,70.8610019598059,71.85904424093,72.857086522054,
73.855128803178,74.853171084302,75.8512133654261,76.5209654926162),
 .UNSPECIFIED.);
#398=B_SPLINE_CURVE_WITH_KNOTS('',3,(#13481,#13482,#13483,#13484,#13485,
#13486,#13487,#13488,#13489,#13490,#13491,#13492,#13493,#13494,#13495,#13496,
#13497,#13498,#13499,#13500,#13501,#13502),.UNSPECIFIED.,.F.,.F.,(4,3,3,
3,3,3,3,4),(-85.7734325137832,-84.7996431730495,-83.8020003121901,-82.8043574513307,
-81.8067145904713,-80.8090717296119,-79.8114288687525,-79.4902472066036),
 .UNSPECIFIED.);
#399=B_SPLINE_CURVE_WITH_KNOTS('',3,(#13503,#13504,#13505,#13506,#13507,
#13508,#13509,#13510,#13511,#13512,#13513,#13514,#13515,#13516,#13517,#13518,
#13519,#13520,#13521,#13522,#13523,#13524),.UNSPECIFIED.,.F.,.F.,(4,3,3,
3,3,3,3,4),(76.5209654926162,76.8492556465501,77.8472979276741,78.8453402087982,
79.8433824899222,80.8414247710462,81.8394670521702,82.8041507997958),
 .UNSPECIFIED.);
#400=B_SPLINE_CURVE_WITH_KNOTS('',3,(#13529,#13530,#13531,#13532,#13533,
#13534,#13535,#13536,#13537,#13538,#13539,#13540,#13541,#13542,#13543,#13544,
#13545,#13546,#13547,#13548,#13549,#13550,#13551,#13552,#13553),
 .UNSPECIFIED.,.F.,.F.,(4,3,3,3,3,3,3,3,4),(-92.0566178209628,-91.7831431990654,
-90.7855003382059,-89.7878574773465,-88.7902146164871,-87.7925717556277,
-86.7949288947683,-85.7972860339089,-85.7734325137832),.UNSPECIFIED.);
#401=B_SPLINE_CURVE_WITH_KNOTS('',3,(#13554,#13555,#13556,#13557,#13558,
#13559,#13560,#13561,#13562,#13563,#13564,#13565,#13566,#13567,#13568,#13569,
#13570,#13571,#13572,#13573,#13574,#13575,#13576,#13577,#13578),
 .UNSPECIFIED.,.F.,.F.,(4,3,3,3,3,3,3,3,4),(82.8041507997958,82.8375093332942,
83.8355516144183,84.8335938955423,85.8316361766664,86.8296784577904,87.8277207389144,
88.8257630200384,89.0873361069754),.UNSPECIFIED.);
#402=B_SPLINE_CURVE_WITH_KNOTS('',3,(#13583,#13584,#13585,#13586,#13587,
#13588,#13589,#13590,#13591,#13592,#13593,#13594,#13595,#13596,#13597,#13598,
#13599,#13600,#13601,#13602,#13603,#13604),.UNSPECIFIED.,.F.,.F.,(4,3,3,
3,3,3,3,4),(-98.3398031281424,-97.7690003642218,-96.7713575033624,-95.773714642503,
-94.7760717816436,-93.7784289207842,-92.7807860599248,-92.0566178209628),
 .UNSPECIFIED.);
#403=B_SPLINE_CURVE_WITH_KNOTS('',3,(#13605,#13606,#13607,#13608,#13609,
#13610,#13611,#13612,#13613,#13614,#13615,#13616,#13617,#13618,#13619,#13620,
#13621,#13622,#13623,#13624,#13625,#13626),.UNSPECIFIED.,.F.,.F.,(4,3,3,
3,3,3,3,4),(89.0873361069754,89.8238053011624,90.8218475822865,91.8198898634105,
92.8179321445345,93.8159744256585,94.8140167067826,95.370521414155),
 .UNSPECIFIED.);
#404=B_SPLINE_CURVE_WITH_KNOTS('',3,(#13631,#13632,#13633,#13634,#13635,
#13636,#13637,#13638,#13639,#13640,#13641,#13642,#13643,#13644,#13645,#13646,
#13647,#13648,#13649,#13650,#13651,#13652),.UNSPECIFIED.,.F.,.F.,(4,3,3,
3,3,3,3,4),(-104.622988435322,-103.754857529378,-102.757214668519,-101.759571807659,
-100.7619289468,-99.7642860859406,-98.7666432250812,-98.3398031281424),
 .UNSPECIFIED.);
#405=B_SPLINE_CURVE_WITH_KNOTS('',3,(#13653,#13654,#13655,#13656,#13657,
#13658,#13659,#13660,#13661,#13662,#13663,#13664,#13665,#13666,#13667,#13668,
#13669,#13670,#13671,#13672,#13673,#13674),.UNSPECIFIED.,.F.,.F.,(4,3,3,
3,3,3,3,4),(95.370521414155,95.8120589879066,96.8101012690306,97.8081435501546,
98.8061858312787,99.8042281124027,100.802270393527,101.653706721335),
 .UNSPECIFIED.);
#406=B_SPLINE_CURVE_WITH_KNOTS('',3,(#13679,#13680,#13681,#13682,#13683,
#13684,#13685,#13686,#13687,#13688,#13689,#13690,#13691,#13692,#13693,#13694,
#13695,#13696,#13697,#13698,#13699,#13700,#13701,#13702,#13703),
 .UNSPECIFIED.,.F.,.F.,(4,3,3,3,3,3,3,3,4),(-110.906173742502,-110.738357555394,
-109.740714694535,-108.743071833675,-107.745428972816,-106.747786111956,
-105.750143251097,-104.752500390238,-104.622988435322),.UNSPECIFIED.);
#407=B_SPLINE_CURVE_WITH_KNOTS('',3,(#13704,#13705,#13706,#13707,#13708,
#13709,#13710,#13711,#13712,#13713,#13714,#13715,#13716,#13717,#13718,#13719,
#13720,#13721,#13722,#13723,#13724,#13725,#13726,#13727,#13728),
 .UNSPECIFIED.,.F.,.F.,(4,3,3,3,3,3,3,3,4),(101.653706721335,101.800312674651,
102.798354955775,103.796397236899,104.794439518023,105.792481799147,106.790524080271,
107.788566361395,107.936892028514),.UNSPECIFIED.);
#408=B_SPLINE_CURVE_WITH_KNOTS('',3,(#13733,#13734,#13735,#13736,#13737,
#13738,#13739,#13740,#13741,#13742,#13743,#13744,#13745,#13746,#13747,#13748,
#13749,#13750,#13751,#13752,#13753,#13754),.UNSPECIFIED.,.F.,.F.,(4,3,3,
3,3,3,3,4),(-117.189359049681,-116.724214720551,-115.726571859691,-114.728928998832,
-113.731286137972,-112.733643277113,-111.736000416253,-110.906173742502),
 .UNSPECIFIED.);
#409=B_SPLINE_CURVE_WITH_KNOTS('',3,(#13755,#13756,#13757,#13758,#13759,
#13760,#13761,#13762,#13763,#13764,#13765,#13766,#13767,#13768,#13769,#13770,
#13771,#13772,#13773,#13774,#13775,#13776),.UNSPECIFIED.,.F.,.F.,(4,3,3,
3,3,3,3,4),(107.936892028514,108.786608642519,109.784650923643,110.782693204767,
111.780735485891,112.778777767015,113.776820048139,114.220077335694),
 .UNSPECIFIED.);
#410=B_SPLINE_CURVE_WITH_KNOTS('',3,(#13781,#13782,#13783,#13784,#13785,
#13786,#13787,#13788,#13789,#13790,#13791,#13792,#13793,#13794,#13795,#13796,
#13797,#13798,#13799,#13800,#13801,#13802),.UNSPECIFIED.,.F.,.F.,(4,3,3,
3,3,3,3,4),(-123.472544356861,-122.710071885707,-121.712429024848,-120.714786163988,
-119.717143303129,-118.719500442269,-117.72185758141,-117.189359049681),
 .UNSPECIFIED.);
#411=B_SPLINE_CURVE_WITH_KNOTS('',3,(#13803,#13804,#13805,#13806,#13807,
#13808,#13809,#13810,#13811,#13812,#13813,#13814,#13815,#13816,#13817,#13818,
#13819,#13820,#13821,#13822,#13823,#13824),.UNSPECIFIED.,.F.,.F.,(4,3,3,
3,3,3,3,4),(114.220077335694,114.774862329263,115.772904610387,116.770946891511,
117.768989172635,118.767031453759,119.765073734883,120.503262642873),
 .UNSPECIFIED.);
#412=B_SPLINE_CURVE_WITH_KNOTS('',3,(#13829,#13830,#13831,#13832,#13833,
#13834,#13835,#13836,#13837,#13838,#13839,#13840,#13841,#13842,#13843,#13844,
#13845,#13846,#13847,#13848,#13849,#13850,#13851,#13852,#13853),
 .UNSPECIFIED.,.F.,.F.,(4,3,3,3,3,3,3,3,4),(-129.75572966404,-129.693571911723,
-128.695929050863,-127.698286190004,-126.700643329145,-125.703000468285,
-124.705357607426,-123.707714746566,-123.472544356861),.UNSPECIFIED.);
#413=B_SPLINE_CURVE_WITH_KNOTS('',3,(#13854,#13855,#13856,#13857,#13858,
#13859,#13860,#13861,#13862,#13863,#13864,#13865,#13866,#13867,#13868,#13869,
#13870,#13871,#13872,#13873,#13874,#13875,#13876,#13877,#13878),
 .UNSPECIFIED.,.F.,.F.,(4,3,3,3,3,3,3,3,4),(120.503262642873,120.763116016007,
121.761158297131,122.759200578255,123.757242859379,124.755285140503,125.753327421627,
126.751369702751,126.786447950053),.UNSPECIFIED.);
#414=B_SPLINE_CURVE_WITH_KNOTS('',3,(#13883,#13884,#13885,#13886,#13887,
#13888,#13889,#13890,#13891,#13892,#13893,#13894,#13895,#13896,#13897,#13898,
#13899,#13900,#13901,#13902,#13903,#13904),.UNSPECIFIED.,.F.,.F.,(4,3,3,
3,3,3,3,4),(-136.03891497122,-135.679429076879,-134.68178621602,-133.68414335516,
-132.686500494301,-131.688857633442,-130.691214772582,-129.75572966404),
 .UNSPECIFIED.);
#415=B_SPLINE_CURVE_WITH_KNOTS('',3,(#13905,#13906,#13907,#13908,#13909,
#13910,#13911,#13912,#13913,#13914,#13915,#13916,#13917,#13918,#13919,#13920,
#13921,#13922,#13923,#13924,#13925,#13926),.UNSPECIFIED.,.F.,.F.,(4,3,3,
3,3,3,3,4),(126.786447950053,127.749411983875,128.747454265,129.745496546124,
130.743538827248,131.741581108372,132.739623389496,133.069633257233),
 .UNSPECIFIED.);
#416=B_SPLINE_CURVE_WITH_KNOTS('',3,(#13931,#13932,#13933,#13934,#13935,
#13936,#13937,#13938,#13939,#13940,#13941,#13942,#13943,#13944,#13945,#13946,
#13947,#13948,#13949,#13950,#13951,#13952),.UNSPECIFIED.,.F.,.F.,(4,3,3,
3,3,3,3,4),(-142.322100278399,-141.665286242036,-140.667643381176,-139.670000520317,
-138.672357659457,-137.674714798598,-136.677071937739,-136.03891497122),
 .UNSPECIFIED.);
#417=B_SPLINE_CURVE_WITH_KNOTS('',3,(#13953,#13954,#13955,#13956,#13957,
#13958,#13959,#13960,#13961,#13962,#13963,#13964,#13965,#13966,#13967,#13968,
#13969,#13970,#13971,#13972,#13973,#13974),.UNSPECIFIED.,.F.,.F.,(4,3,3,
3,3,3,3,4),(133.069633257233,133.73766567062,134.735707951744,135.733750232868,
136.731792513992,137.729834795116,138.72787707624,139.352818564412),
 .UNSPECIFIED.);
#418=B_SPLINE_CURVE_WITH_KNOTS('',3,(#13979,#13980,#13981,#13982,#13983,
#13984,#13985,#13986,#13987,#13988,#13989,#13990,#13991,#13992,#13993,#13994,
#13995,#13996,#13997,#13998,#13999,#14000),.UNSPECIFIED.,.F.,.F.,(4,3,3,
3,3,3,3,4),(-148.605285585579,-147.651143407192,-146.653500546333,-145.655857685473,
-144.658214824614,-143.660571963754,-142.662929102895,-142.322100278399),
 .UNSPECIFIED.);
#419=B_SPLINE_CURVE_WITH_KNOTS('',3,(#14001,#14002,#14003,#14004,#14005,
#14006,#14007,#14008,#14009,#14010,#14011,#14012,#14013,#14014,#14015,#14016,
#14017,#14018,#14019,#14020,#14021,#14022),.UNSPECIFIED.,.F.,.F.,(4,3,3,
3,3,3,3,4),(139.352818564412,139.725919357364,140.723961638488,141.722003919612,
142.720046200736,143.71808848186,144.716130762984,145.636003871592),
 .UNSPECIFIED.);
#420=B_SPLINE_CURVE_WITH_KNOTS('',3,(#14027,#14028,#14029,#14030,#14031,
#14032,#14033,#14034,#14035,#14036,#14037,#14038,#14039,#14040,#14041,#14042,
#14043,#14044,#14045,#14046,#14047,#14048,#14049,#14050,#14051),
 .UNSPECIFIED.,.F.,.F.,(4,3,3,3,3,3,3,3,4),(-154.888470892759,-154.634643433208,
-153.637000572349,-152.639357711489,-151.64171485063,-150.64407198977,-149.646429128911,
-148.648786268052,-148.605285585579),.UNSPECIFIED.);
#421=B_SPLINE_CURVE_WITH_KNOTS('',3,(#14052,#14053,#14054,#14055,#14056,
#14057,#14058,#14059,#14060,#14061,#14062,#14063,#14064,#14065,#14066,#14067,
#14068,#14069,#14070,#14071,#14072,#14073,#14074,#14075,#14076),
 .UNSPECIFIED.,.F.,.F.,(4,3,3,3,3,3,3,3,4),(145.636003871592,145.714173044108,
146.712215325232,147.710257606356,148.70829988748,149.706342168604,150.704384449728,
151.702426730852,151.919189178771),.UNSPECIFIED.);
#422=B_SPLINE_CURVE_WITH_KNOTS('',3,(#14081,#14082,#14083,#14084,#14085,
#14086,#14087,#14088,#14089,#14090,#14091,#14092,#14093,#14094,#14095,#14096,
#14097,#14098,#14099,#14100,#14101,#14102),.UNSPECIFIED.,.F.,.F.,(4,3,3,
3,3,3,3,4),(-161.171656199938,-160.620500598364,-159.622857737505,-158.625214876646,
-157.627572015786,-156.629929154927,-155.632286294067,-154.888470892759),
 .UNSPECIFIED.);
#423=B_SPLINE_CURVE_WITH_KNOTS('',3,(#14103,#14104,#14105,#14106,#14107,
#14108,#14109,#14110,#14111,#14112,#14113,#14114,#14115,#14116,#14117,#14118,
#14119,#14120,#14121,#14122,#14123,#14124),.UNSPECIFIED.,.F.,.F.,(4,3,3,
3,3,3,3,4),(151.919189178771,152.700469011976,153.6985112931,154.696553574224,
155.694595855348,156.692638136472,157.690680417596,158.202374485951),
 .UNSPECIFIED.);
#424=B_SPLINE_CURVE_WITH_KNOTS('',3,(#14129,#14130,#14131,#14132,#14133,
#14134,#14135,#14136,#14137,#14138,#14139,#14140,#14141,#14142,#14143,#14144,
#14145,#14146,#14147,#14148,#14149,#14150),.UNSPECIFIED.,.F.,.F.,(4,3,3,
3,3,3,3,4),(-167.454841507118,-166.606357763521,-165.608714902661,-164.611072041802,
-163.613429180943,-162.615786320083,-161.618143459224,-161.171656199938),
 .UNSPECIFIED.);
#425=B_SPLINE_CURVE_WITH_KNOTS('',3,(#14151,#14152,#14153,#14154,#14155,
#14156,#14157,#14158,#14159,#14160,#14161,#14162,#14163,#14164,#14165,#14166,
#14167,#14168,#14169,#14170,#14171,#14172),.UNSPECIFIED.,.F.,.F.,(4,3,3,
3,3,3,3,4),(158.202374485951,158.68872269872,159.686764979844,160.684807260968,
161.682849542092,162.680891823216,163.67893410434,164.48555979313),
 .UNSPECIFIED.);
#426=B_SPLINE_CURVE_WITH_KNOTS('',3,(#14177,#14178,#14179,#14180,#14181,
#14182,#14183,#14184,#14185,#14186,#14187,#14188,#14189,#14190,#14191,#14192,
#14193,#14194,#14195,#14196,#14197,#14198,#14199,#14200,#14201),
 .UNSPECIFIED.,.F.,.F.,(4,3,3,3,3,3,3,3,4),(-173.738026814297,-173.589857789537,
-172.592214928677,-171.594572067818,-170.596929206958,-169.599286346099,
-168.60164348524,-167.60400062438,-167.454841507118),.UNSPECIFIED.);
#427=B_SPLINE_CURVE_WITH_KNOTS('',3,(#14202,#14203,#14204,#14205,#14206,
#14207,#14208,#14209,#14210,#14211,#14212,#14213,#14214,#14215,#14216,#14217,
#14218,#14219,#14220,#14221,#14222,#14223,#14224,#14225,#14226),
 .UNSPECIFIED.,.F.,.F.,(4,3,3,3,3,3,3,3,4),(164.48555979313,164.676976385465,
165.675018666588,166.673060947713,167.671103228837,168.669145509961,169.667187791085,
170.665230072209,170.76874510031),.UNSPECIFIED.);
#428=B_SPLINE_CURVE_WITH_KNOTS('',3,(#14231,#14232,#14233,#14234,#14235,
#14236,#14237,#14238,#14239,#14240,#14241,#14242,#14243,#14244,#14245,#14246,
#14247,#14248,#14249,#14250,#14251,#14252),.UNSPECIFIED.,.F.,.F.,(4,3,3,
3,3,3,3,4),(-180.021212121477,-179.575714954693,-178.578072093834,-177.580429232974,
-176.582786372115,-175.585143511255,-174.587500650396,-173.738026814297),
 .UNSPECIFIED.);
#429=B_SPLINE_CURVE_WITH_KNOTS('',3,(#14253,#14254,#14255,#14256,#14257,
#14258,#14259,#14260,#14261,#14262,#14263,#14264,#14265,#14266,#14267,#14268,
#14269,#14270,#14271,#14272,#14273,#14274),.UNSPECIFIED.,.F.,.F.,(4,3,3,
3,3,3,3,4),(170.76874510031,171.663272353333,172.661314634457,173.659356915581,
174.657399196705,175.655441477829,176.653483758953,177.051930407489),
 .UNSPECIFIED.);
#430=B_SPLINE_CURVE_WITH_KNOTS('',3,(#14279,#14280,#14281,#14282,#14283,
#14284,#14285,#14286,#14287,#14288,#14289,#14290,#14291,#14292,#14293,#14294,
#14295,#14296,#14297,#14298,#14299,#14300),.UNSPECIFIED.,.F.,.F.,(4,3,3,
3,3,3,3,4),(-186.304397428656,-185.56157211985,-184.56392925899,-183.566286398131,
-182.568643537271,-181.571000676412,-180.573357815553,-180.021212121477),
 .UNSPECIFIED.);
#431=B_SPLINE_CURVE_WITH_KNOTS('',3,(#14301,#14302,#14303,#14304,#14305,
#14306,#14307,#14308,#14309,#14310,#14311,#14312,#14313,#14314,#14315,#14316,
#14317,#14318,#14319,#14320,#14321,#14322),.UNSPECIFIED.,.F.,.F.,(4,3,3,
3,3,3,3,4),(177.051930407489,177.651526040077,178.649568321201,179.647610602325,
180.645652883449,181.643695164573,182.641737445697,183.335115714669),
 .UNSPECIFIED.);
#432=B_SPLINE_CURVE_WITH_KNOTS('',3,(#14328,#14329,#14330,#14331,#14332,
#14333,#14334,#14335,#14336,#14337),.UNSPECIFIED.,.F.,.F.,(4,1,1,1,1,1,
1,4),(197.920337176157,198.17515472821,199.172797589069,200.170440449928,
201.168083310788,202.165726171647,203.163369032507,204.161011893366),
 .UNSPECIFIED.);
#433=B_SPLINE_CURVE_WITH_KNOTS('',3,(#14340,#14341,#14342,#14343,#14344,
#14345,#14346,#14347,#14348),.UNSPECIFIED.,.F.,.F.,(4,1,1,1,1,1,4),(197.920337176157,
197.930069567874,198.928111848998,199.926154130122,200.924196411246,201.92223869237,
202.920280973494),.UNSPECIFIED.);
#434=B_SPLINE_CURVE_WITH_KNOTS('',3,(#14353,#14354,#14355,#14356,#14357,
#14358,#14359,#14360,#14361,#14362),.UNSPECIFIED.,.F.,.F.,(4,1,1,1,1,1,
1,4),(191.637151868977,192.189297563053,193.186940423913,194.184583284772,
195.182226145631,196.179869006491,197.17751186735,197.920337176157),
 .UNSPECIFIED.);
#435=B_SPLINE_CURVE_WITH_KNOTS('',3,(#14363,#14364,#14365,#14366,#14367,
#14368,#14369,#14370,#14371,#14372),.UNSPECIFIED.,.F.,.F.,(4,1,1,1,1,1,
1,4),(191.637151868977,191.94181588113,192.939858162254,193.937900443378,
194.935942724502,195.933985005626,196.93202728675,197.920337176157),
 .UNSPECIFIED.);
#436=B_SPLINE_CURVE_WITH_KNOTS('',3,(#14377,#14378,#14379,#14380,#14381,
#14382,#14383,#14384,#14385,#14386),.UNSPECIFIED.,.F.,.F.,(4,1,1,1,1,1,
1,4),(185.353966561798,186.203440397897,187.201083258756,188.198726119616,
189.196368980475,190.194011841334,191.191654702194,191.637151868977),
 .UNSPECIFIED.);
#437=B_SPLINE_CURVE_WITH_KNOTS('',3,(#14387,#14388,#14389,#14390,#14391,
#14392,#14393,#14394,#14395,#14396),.UNSPECIFIED.,.F.,.F.,(4,1,1,1,1,1,
1,4),(185.353966561798,185.953562194385,186.951604475509,187.949646756633,
188.947689037757,189.945731318881,190.943773600006,191.637151868977),
 .UNSPECIFIED.);
#438=B_SPLINE_CURVE_WITH_KNOTS('',3,(#14401,#14402,#14403,#14404,#14405,
#14406,#14407,#14408,#14409,#14410,#14411),.UNSPECIFIED.,.F.,.F.,(4,1,1,
1,1,1,1,1,4),(179.070781254618,179.219940371881,180.21758323274,181.2152260936,
182.212868954459,183.210511815318,184.208154676178,185.205797537037,185.353966561798),
 .UNSPECIFIED.);
#439=B_SPLINE_CURVE_WITH_KNOTS('',3,(#14412,#14413,#14414,#14415,#14416,
#14417,#14418,#14419,#14420,#14421),.UNSPECIFIED.,.F.,.F.,(4,1,1,1,1,1,
1,4),(179.070781254618,179.965308507641,180.963350788765,181.961393069889,
182.959435351013,183.957477632137,184.955519913261,185.353966561798),
 .UNSPECIFIED.);
#440=B_SPLINE_CURVE_WITH_KNOTS('',3,(#14426,#14427,#14428,#14429,#14430,
#14431,#14432,#14433,#14434,#14435),.UNSPECIFIED.,.F.,.F.,(4,1,1,1,1,1,
1,4),(172.787595947439,173.234083206724,174.231726067584,175.229368928443,
176.227011789303,177.224654650162,178.222297511021,179.070781254618),
 .UNSPECIFIED.);
#441=B_SPLINE_CURVE_WITH_KNOTS('',3,(#14436,#14437,#14438,#14439,#14440,
#14441,#14442,#14443,#14444,#14445,#14446),.UNSPECIFIED.,.F.,.F.,(4,1,1,
1,1,1,1,1,4),(172.787595947439,172.979012539773,173.977054820897,174.975097102021,
175.973139383145,176.971181664269,177.969223945393,178.967266226517,179.070781254618),
 .UNSPECIFIED.);
#442=B_SPLINE_CURVE_WITH_KNOTS('',3,(#14451,#14452,#14453,#14454,#14455,
#14456,#14457,#14458,#14459,#14460),.UNSPECIFIED.,.F.,.F.,(4,1,1,1,1,1,
1,4),(166.504410640259,167.248226041568,168.245868902427,169.243511763287,
170.241154624146,171.238797485006,172.236440345865,172.787595947439),
 .UNSPECIFIED.);
#443=B_SPLINE_CURVE_WITH_KNOTS('',3,(#14461,#14462,#14463,#14464,#14465,
#14466,#14467,#14468,#14469,#14470),.UNSPECIFIED.,.F.,.F.,(4,1,1,1,1,1,
1,4),(166.504410640259,166.990758853029,167.988801134153,168.986843415277,
169.984885696401,170.982927977525,171.980970258649,172.787595947439),
 .UNSPECIFIED.);
#444=B_SPLINE_CURVE_WITH_KNOTS('',3,(#14475,#14476,#14477,#14478,#14479,
#14480,#14481,#14482,#14483,#14484,#14485),.UNSPECIFIED.,.F.,.F.,(4,1,1,
1,1,1,1,1,4),(160.22122533308,160.264726015552,161.262368876412,162.260011737271,
163.25765459813,164.25529745899,165.252940319849,166.250583180709,166.504410640259),
 .UNSPECIFIED.);
#445=B_SPLINE_CURVE_WITH_KNOTS('',3,(#14486,#14487,#14488,#14489,#14490,
#14491,#14492,#14493,#14494,#14495),.UNSPECIFIED.,.F.,.F.,(4,1,1,1,1,1,
1,4),(160.22122533308,161.002505166285,162.000547447409,162.998589728533,
163.996632009657,164.994674290781,165.992716571905,166.504410640259),
 .UNSPECIFIED.);
#446=B_SPLINE_CURVE_WITH_KNOTS('',3,(#14500,#14501,#14502,#14503,#14504,
#14505,#14506,#14507,#14508,#14509),.UNSPECIFIED.,.F.,.F.,(4,1,1,1,1,1,
1,4),(153.9380400259,154.278868850396,155.276511711255,156.274154572115,
157.271797432974,158.269440293833,159.267083154693,160.22122533308),
 .UNSPECIFIED.);
#447=B_SPLINE_CURVE_WITH_KNOTS('',3,(#14510,#14511,#14512,#14513,#14514,
#14515,#14516,#14517,#14518,#14519,#14520),.UNSPECIFIED.,.F.,.F.,(4,1,1,
1,1,1,1,1,4),(153.9380400259,154.016209198417,155.014251479541,156.012293760665,
157.010336041789,158.008378322913,159.006420604037,160.004462885161,160.22122533308),
 .UNSPECIFIED.);
#448=B_SPLINE_CURVE_WITH_KNOTS('',3,(#14525,#14526,#14527,#14528,#14529,
#14530,#14531,#14532,#14533,#14534),.UNSPECIFIED.,.F.,.F.,(4,1,1,1,1,1,
1,4),(147.65485471872,148.293011685239,149.290654546099,150.288297406958,
151.285940267817,152.283583128677,153.281225989536,153.9380400259),
 .UNSPECIFIED.);
#449=B_SPLINE_CURVE_WITH_KNOTS('',3,(#14535,#14536,#14537,#14538,#14539,
#14540,#14541,#14542,#14543,#14544),.UNSPECIFIED.,.F.,.F.,(4,1,1,1,1,1,
1,4),(147.65485471872,148.027955511672,149.025997792796,150.02404007392,
151.022082355044,152.020124636168,153.018166917292,153.9380400259),
 .UNSPECIFIED.);
#450=B_SPLINE_CURVE_WITH_KNOTS('',3,(#14549,#14550,#14551,#14552,#14553,
#14554,#14555,#14556,#14557,#14558),.UNSPECIFIED.,.F.,.F.,(4,1,1,1,1,1,
1,4),(141.371669411541,142.307154520083,143.304797380942,144.302440241802,
145.300083102661,146.29772596352,147.29536882438,147.65485471872),
 .UNSPECIFIED.);
#451=B_SPLINE_CURVE_WITH_KNOTS('',3,(#14559,#14560,#14561,#14562,#14563,
#14564,#14565,#14566,#14567,#14568),.UNSPECIFIED.,.F.,.F.,(4,1,1,1,1,1,
1,4),(141.371669411541,142.039701824928,143.037744106052,144.035786387176,
145.0338286683,146.031870949424,147.029913230548,147.65485471872),
 .UNSPECIFIED.);
#452=B_SPLINE_CURVE_WITH_KNOTS('',3,(#14573,#14574,#14575,#14576,#14577,
#14578,#14579,#14580,#14581,#14582,#14583),.UNSPECIFIED.,.F.,.F.,(4,1,1,
1,1,1,1,1,4),(135.088484104361,135.323654494067,136.321297354926,137.318940215786,
138.316583076645,139.314225937505,140.311868798364,141.309511659223,141.371669411541),
 .UNSPECIFIED.);
#453=B_SPLINE_CURVE_WITH_KNOTS('',3,(#14584,#14585,#14586,#14587,#14588,
#14589,#14590,#14591,#14592,#14593),.UNSPECIFIED.,.F.,.F.,(4,1,1,1,1,1,
1,4),(135.088484104361,136.051448138184,137.049490419308,138.047532700432,
139.045574981556,140.04361726268,141.041659543804,141.371669411541),
 .UNSPECIFIED.);
#454=B_SPLINE_CURVE_WITH_KNOTS('',3,(#14598,#14599,#14600,#14601,#14602,
#14603,#14604,#14605,#14606,#14607),.UNSPECIFIED.,.F.,.F.,(4,1,1,1,1,1,
1,4),(128.805298797182,129.337797328911,130.33544018977,131.333083050629,
132.330725911489,133.328368772348,134.326011633208,135.088484104361),
 .UNSPECIFIED.);
#455=B_SPLINE_CURVE_WITH_KNOTS('',3,(#14608,#14609,#14610,#14611,#14612,
#14613,#14614,#14615,#14616,#14617,#14618),.UNSPECIFIED.,.F.,.F.,(4,1,1,
1,1,1,1,1,4),(128.805298797182,129.065152170316,130.06319445144,131.061236732564,
132.059279013688,133.057321294812,134.055363575936,135.05340585706,135.088484104361),
 .UNSPECIFIED.);
#456=B_SPLINE_CURVE_WITH_KNOTS('',3,(#14623,#14624,#14625,#14626,#14627,
#14628,#14629,#14630,#14631,#14632),.UNSPECIFIED.,.F.,.F.,(4,1,1,1,1,1,
1,4),(122.522113490002,123.351940163754,124.349583024614,125.347225885473,
126.344868746332,127.342511607192,128.340154468051,128.805298797182),
 .UNSPECIFIED.);
#457=B_SPLINE_CURVE_WITH_KNOTS('',3,(#14633,#14634,#14635,#14636,#14637,
#14638,#14639,#14640,#14641,#14642),.UNSPECIFIED.,.F.,.F.,(4,1,1,1,1,1,
1,4),(122.522113490002,123.076898483572,124.074940764696,125.07298304582,
126.071025326944,127.069067608068,128.067109889192,128.805298797182),
 .UNSPECIFIED.);
#458=B_SPLINE_CURVE_WITH_KNOTS('',3,(#14647,#14648,#14649,#14650,#14651,
#14652,#14653,#14654,#14655,#14656,#14657),.UNSPECIFIED.,.F.,.F.,(4,1,1,
1,1,1,1,1,4),(116.238928182823,116.368440137738,117.366082998598,118.363725859457,
119.361368720316,120.359011581176,121.356654442035,122.354297302895,122.522113490002),
 .UNSPECIFIED.);
#459=B_SPLINE_CURVE_WITH_KNOTS('',3,(#14658,#14659,#14660,#14661,#14662,
#14663,#14664,#14665,#14666,#14667),.UNSPECIFIED.,.F.,.F.,(4,1,1,1,1,1,
1,4),(116.238928182823,117.088644796828,118.086687077952,119.084729359076,
120.0827716402,121.080813921324,122.078856202448,122.522113490002),
 .UNSPECIFIED.);
#460=B_SPLINE_CURVE_WITH_KNOTS('',3,(#14672,#14673,#14674,#14675,#14676,
#14677,#14678,#14679,#14680,#14681),.UNSPECIFIED.,.F.,.F.,(4,1,1,1,1,1,
1,4),(109.955742875643,110.382582972582,111.380225833441,112.377868694301,
113.37551155516,114.373154416019,115.370797276879,116.238928182823),
 .UNSPECIFIED.);
#461=B_SPLINE_CURVE_WITH_KNOTS('',3,(#14682,#14683,#14684,#14685,#14686,
#14687,#14688,#14689,#14690,#14691,#14692),.UNSPECIFIED.,.F.,.F.,(4,1,1,
1,1,1,1,1,4),(109.955742875643,110.102348828959,111.100391110083,112.098433391207,
113.096475672331,114.094517953455,115.092560234579,116.090602515703,116.238928182823),
 .UNSPECIFIED.);
#462=B_SPLINE_CURVE_WITH_KNOTS('',3,(#14697,#14698,#14699,#14700,#14701,
#14702,#14703,#14704,#14705,#14706),.UNSPECIFIED.,.F.,.F.,(4,1,1,1,1,1,
1,4),(103.672557568463,104.396725807425,105.394368668285,106.392011529144,
107.389654390004,108.387297250863,109.384940111722,109.955742875643),
 .UNSPECIFIED.);
#463=B_SPLINE_CURVE_WITH_KNOTS('',3,(#14707,#14708,#14709,#14710,#14711,
#14712,#14713,#14714,#14715,#14716),.UNSPECIFIED.,.F.,.F.,(4,1,1,1,1,1,
1,4),(103.672557568463,104.114095142215,105.112137423339,106.110179704463,
107.108221985587,108.106264266711,109.104306547835,109.955742875643),
 .UNSPECIFIED.);
#464=B_SPLINE_CURVE_WITH_KNOTS('',3,(#14721,#14722,#14723,#14724,#14725,
#14726,#14727,#14728,#14729,#14730,#14731),.UNSPECIFIED.,.F.,.F.,(4,1,1,
1,1,1,1,1,4),(97.3893722612837,97.4132257814096,98.410868642269,99.4085115031284,
100.406154363988,101.403797224847,102.401440085707,103.399082946566,103.672557568463),
 .UNSPECIFIED.);
#465=B_SPLINE_CURVE_WITH_KNOTS('',3,(#14732,#14733,#14734,#14735,#14736,
#14737,#14738,#14739,#14740,#14741),.UNSPECIFIED.,.F.,.F.,(4,1,1,1,1,1,
1,4),(97.3893722612838,98.125841455471,99.123883736595,100.121926017719,
101.119968298843,102.118010579967,103.116052861091,103.672557568463),
 .UNSPECIFIED.);
#466=B_SPLINE_CURVE_WITH_KNOTS('',3,(#14746,#14747,#14748,#14749,#14750,
#14751,#14752,#14753,#14754,#14755),.UNSPECIFIED.,.F.,.F.,(4,1,1,1,1,1,
1,4),(91.1061869541041,91.4273686162531,92.4250114771125,93.4226543379719,
94.4202971988313,95.4179400596907,96.4155829205502,97.3893722612837),
 .UNSPECIFIED.);
#467=B_SPLINE_CURVE_WITH_KNOTS('',3,(#14756,#14757,#14758,#14759,#14760,
#14761,#14762,#14763,#14764,#14765,#14766),.UNSPECIFIED.,.F.,.F.,(4,1,1,
1,1,1,1,1,4),(91.1061869541042,91.1395454876028,92.1375877687268,93.1356300498508,
94.1336723309749,95.1317146120989,96.1297568932229,97.127799174347,97.3893722612838),
 .UNSPECIFIED.);
#468=B_SPLINE_CURVE_WITH_KNOTS('',3,(#14771,#14772,#14773,#14774,#14775,
#14776,#14777,#14778,#14779,#14780),.UNSPECIFIED.,.F.,.F.,(4,1,1,1,1,1,
1,4),(84.8230016469245,85.4415114510967,86.4391543119561,87.4367971728155,
88.4344400336749,89.4320828945343,90.4297257553937,91.1061869541041),
 .UNSPECIFIED.);
#469=B_SPLINE_CURVE_WITH_KNOTS('',3,(#14781,#14782,#14783,#14784,#14785,
#14786,#14787,#14788,#14789,#14790),.UNSPECIFIED.,.F.,.F.,(4,1,1,1,1,1,
1,4),(84.8230016469246,85.1512918008586,86.1493340819827,87.1473763631067,
88.1454186442307,89.1434609253548,90.1415032064788,91.1061869541042),
 .UNSPECIFIED.);
#470=B_SPLINE_CURVE_WITH_KNOTS('',3,(#14795,#14796,#14797,#14798,#14799,
#14800,#14801,#14802,#14803,#14804),.UNSPECIFIED.,.F.,.F.,(4,1,1,1,1,1,
1,4),(78.539816339745,79.4556542859402,80.4532971467996,81.4509400076591,
82.4485828685185,83.4462257293779,84.4438685902373,84.8230016469245),
 .UNSPECIFIED.);
#471=B_SPLINE_CURVE_WITH_KNOTS('',3,(#14805,#14806,#14807,#14808,#14809,
#14810,#14811,#14812,#14813,#14814),.UNSPECIFIED.,.F.,.F.,(4,1,1,1,1,1,
1,4),(78.539816339745,79.1630381141145,80.1610803952385,81.1591226763625,
82.1571649574865,83.1552072386106,84.1532495197346,84.8230016469246),
 .UNSPECIFIED.);
#472=B_SPLINE_CURVE_WITH_KNOTS('',3,(#14819,#14820,#14821,#14822,#14823,
#14824,#14825,#14826,#14827,#14828,#14829),.UNSPECIFIED.,.F.,.F.,(4,1,1,
1,1,1,1,1,4),(72.2566310325654,72.4721542599244,73.4697971207838,74.4674399816432,
75.4650828425026,76.462725703362,77.4603685642214,78.4580114250808,78.539816339745),
 .UNSPECIFIED.);
#473=B_SPLINE_CURVE_WITH_KNOTS('',3,(#14830,#14831,#14832,#14833,#14834,
#14835,#14836,#14837,#14838,#14839),.UNSPECIFIED.,.F.,.F.,(4,1,1,1,1,1,
1,4),(72.2566310325654,73.1747844273703,74.1728267084943,75.1708689896184,
76.1689112707424,77.1669535518664,78.1649958329905,78.539816339745),
 .UNSPECIFIED.);
#474=B_SPLINE_CURVE_WITH_KNOTS('',3,(#14844,#14845,#14846,#14847,#14848,
#14849,#14850,#14851,#14852,#14853),.UNSPECIFIED.,.F.,.F.,(4,1,1,1,1,1,
1,4),(65.9734457253858,66.486297094768,67.4839399556274,68.4815828164868,
69.4792256773462,70.4768685382056,71.474511399065,72.2566310325654),
 .UNSPECIFIED.);
#475=B_SPLINE_CURVE_WITH_KNOTS('',3,(#14854,#14855,#14856,#14857,#14858,
#14859,#14860,#14861,#14862,#14863,#14864),.UNSPECIFIED.,.F.,.F.,(4,1,1,
1,1,1,1,1,4),(65.9734457253858,66.1884884595021,67.1865307406262,68.1845730217502,
69.1826153028742,70.1806575839982,71.1786998651223,72.1767421462463,72.2566310325654),
 .UNSPECIFIED.);
#476=B_SPLINE_CURVE_WITH_KNOTS('',3,(#14869,#14870,#14871,#14872,#14873,
#14874,#14875,#14876,#14877,#14878),.UNSPECIFIED.,.F.,.F.,(4,1,1,1,1,1,
1,4),(59.6902604182062,60.5004399296115,61.4980827904709,62.4957256513303,
63.4933685121897,64.4910113730492,65.4886542339086,65.9734457253858),
 .UNSPECIFIED.);
#477=B_SPLINE_CURVE_WITH_KNOTS('',3,(#14879,#14880,#14881,#14882,#14883,
#14884,#14885,#14886,#14887,#14888),.UNSPECIFIED.,.F.,.F.,(4,1,1,1,1,1,
1,4),(59.6902604182062,60.200234772758,61.198277053882,62.196319335006,
63.19436161613,64.1924038972541,65.1904461783781,65.9734457253858),
 .UNSPECIFIED.);
#478=B_SPLINE_CURVE_WITH_KNOTS('',3,(#14893,#14894,#14895,#14896,#14897,
#14898,#14899,#14900,#14901,#14902,#14903),.UNSPECIFIED.,.F.,.F.,(4,1,1,
1,1,1,1,1,4),(53.4070751110266,53.5169399035957,54.5145827644551,55.5122256253145,
56.5098684861739,57.5075113470333,58.5051542078927,59.5027970687521,59.6902604182062),
 .UNSPECIFIED.);
#479=B_SPLINE_CURVE_WITH_KNOTS('',3,(#14904,#14905,#14906,#14907,#14908,
#14909,#14910,#14911,#14912,#14913),.UNSPECIFIED.,.F.,.F.,(4,1,1,1,1,1,
1,4),(53.4070751110266,54.2119810860138,55.2100233671378,56.2080656482619,
57.2061079293859,58.2041502105099,59.2021924916339,59.6902604182062),
 .UNSPECIFIED.);
#480=B_SPLINE_CURVE_WITH_KNOTS('',3,(#14918,#14919,#14920,#14921,#14922,
#14923,#14924,#14925,#14926,#14927),.UNSPECIFIED.,.F.,.F.,(4,1,1,1,1,1,
1,4),(47.123889803847,47.5310827384393,48.5287255992987,49.5263684601581,
50.5240113210175,51.5216541818769,52.5192970427363,53.4070751110266),
 .UNSPECIFIED.);
#481=B_SPLINE_CURVE_WITH_KNOTS('',3,(#14928,#14929,#14930,#14931,#14932,
#14933,#14934,#14935,#14936,#14937,#14938),.UNSPECIFIED.,.F.,.F.,(4,1,1,
1,1,1,1,1,4),(47.123889803847,47.2256851181456,48.2237273992696,49.2217696803937,
50.2198119615177,51.2178542426417,52.2158965237657,53.2139388048898,53.4070751110266),
 .UNSPECIFIED.);
#482=B_SPLINE_CURVE_WITH_KNOTS('',3,(#14943,#14944,#14945,#14946,#14947,
#14948,#14949,#14950,#14951,#14952),.UNSPECIFIED.,.F.,.F.,(4,1,1,1,1,1,
1,4),(40.8407044966674,41.5452255732828,42.5428684341422,43.5405112950016,
44.538154155861,45.5357970167204,46.5334398775799,47.123889803847),
 .UNSPECIFIED.);
#483=B_SPLINE_CURVE_WITH_KNOTS('',3,(#14953,#14954,#14955,#14956,#14957,
#14958,#14959,#14960,#14961,#14962),.UNSPECIFIED.,.F.,.F.,(4,1,1,1,1,1,
1,4),(40.8407044966675,41.2374314314014,42.2354737125255,43.2335159936495,
44.2315582747735,45.2296005558975,46.2276428370216,47.123889803847),
 .UNSPECIFIED.);
#484=B_SPLINE_CURVE_WITH_KNOTS('',3,(#14967,#14968,#14969,#14970,#14971,
#14972,#14973,#14974,#14975,#14976,#14977),.UNSPECIFIED.,.F.,.F.,(4,1,1,
1,1,1,1,1,4),(34.5575191894878,34.561725547267,35.5593684081264,36.5570112689858,
37.5546541298452,38.5522969907046,39.549939851564,40.5475827124234,40.8407044966674),
 .UNSPECIFIED.);
#485=B_SPLINE_CURVE_WITH_KNOTS('',3,(#14978,#14979,#14980,#14981,#14982,
#14983,#14984,#14985,#14986,#14987),.UNSPECIFIED.,.F.,.F.,(4,1,1,1,1,1,
1,4),(34.5575191894879,35.2491777446573,36.2472200257813,37.2452623069053,
38.2433045880294,39.2413468691534,40.2393891502774,40.8407044966675),
 .UNSPECIFIED.);
#486=B_SPLINE_CURVE_WITH_KNOTS('',3,(#14992,#14993,#14994,#14995,#14996,
#14997,#14998,#14999,#15000,#15001),.UNSPECIFIED.,.F.,.F.,(4,1,1,1,1,1,
1,4),(28.2743338823082,28.5758683821105,29.5735112429699,30.5711541038294,
31.5687969646888,32.5664398255482,33.5640826864076,34.5575191894878),
 .UNSPECIFIED.);
#487=B_SPLINE_CURVE_WITH_KNOTS('',3,(#15002,#15003,#15004,#15005,#15006,
#15007,#15008,#15009,#15010,#15011),.UNSPECIFIED.,.F.,.F.,(4,1,1,1,1,1,
1,4),(28.2743338823083,29.2609240579131,30.2589663390371,31.2570086201612,
32.2550509012852,33.2530931824092,34.2511354635333,34.5575191894879),
 .UNSPECIFIED.);
#488=B_SPLINE_CURVE_WITH_KNOTS('',3,(#15016,#15017,#15018,#15019,#15020,
#15021,#15022,#15023,#15024,#15025),.UNSPECIFIED.,.F.,.F.,(4,1,1,1,1,1,
1,4),(21.9911485751286,22.5900112169541,23.5876540778135,24.5852969386729,
25.5829397995323,26.5805826603917,27.5782255212511,28.2743338823082),
 .UNSPECIFIED.);
#489=B_SPLINE_CURVE_WITH_KNOTS('',3,(#15026,#15027,#15028,#15029,#15030,
#15031,#15032,#15033,#15034,#15035,#15036),.UNSPECIFIED.,.F.,.F.,(4,1,1,
1,1,1,1,1,4),(21.9911485751287,22.2746280900449,23.272670371169,24.270712652293,
25.268754933417,26.266797214541,27.2648394956651,28.2628817767891,28.2743338823083),
 .UNSPECIFIED.);
#490=B_SPLINE_CURVE_WITH_KNOTS('',3,(#15041,#15042,#15043,#15044,#15045,
#15046,#15047,#15048,#15049,#15050),.UNSPECIFIED.,.F.,.F.,(4,1,1,1,1,1,
1,4),(15.707963267949,16.6041540517977,17.6017969126571,18.5994397735165,
19.5970826343759,20.5947254952353,21.5923683560947,21.9911485751286),
 .UNSPECIFIED.);
#491=B_SPLINE_CURVE_WITH_KNOTS('',3,(#15051,#15052,#15053,#15054,#15055,
#15056,#15057,#15058,#15059,#15060),.UNSPECIFIED.,.F.,.F.,(4,1,1,1,1,1,
1,4),(15.7079632679491,16.2863744033008,17.2844166844248,18.2824589655488,
19.2805012466728,20.2785435277969,21.2765858089209,21.9911485751287),
 .UNSPECIFIED.);
#492=B_SPLINE_CURVE_WITH_KNOTS('',3,(#15063,#15064,#15065,#15066,#15067,
#15068,#15069,#15070,#15071,#15072,#15073,#15074,#15075,#15076,#15077,#15078,
#15079,#15080,#15081,#15082,#15083,#15084,#15085,#15086,#15087,#15088,#15089,
#15090,#15091,#15092,#15093,#15094,#15095,#15096,#15097,#15098,#15099,#15100,
#15101,#15102,#15103,#15104,#15105,#15106,#15107,#15108,#15109,#15110,#15111,
#15112,#15113,#15114,#15115,#15116,#15117,#15118,#15119,#15120,#15121,#15122,
#15123,#15124,#15125,#15126,#15127,#15128,#15129,#15130,#15131,#15132,#15133,
#15134,#15135,#15136,#15137,#15138,#15139,#15140,#15141,#15142,#15143,#15144,
#15145,#15146,#15147,#15148,#15149,#15150,#15151,#15152,#15153,#15154,#15155,
#15156,#15157,#15158,#15159,#15160,#15161,#15162,#15163,#15164,#15165,#15166,
#15167,#15168,#15169,#15170,#15171,#15172,#15173,#15174,#15175,#15176,#15177,
#15178,#15179,#15180,#15181,#15182,#15183),.UNSPECIFIED.,.F.,.F.,(4,3,3,
3,3,3,3,3,3,3,3,3,3,3,3,3,3,3,3,3,3,3,3,3,3,3,3,3,3,3,3,3,3,3,3,3,3,3,3,
3,4),(-0.753008129282056,-0.726412283548368,-0.715911613874471,-0.694893371653716,
-0.683361029549332,-0.673826434412814,-0.652889016486892,-0.639679181765185,
-0.63195159856097,-0.60480408471638,-0.59150990338668,-0.582561183693184,
-0.554067746128576,-0.540494882749548,-0.528208608719221,-0.505843484121927,
-0.4921308028701,-0.483102814228457,-0.456032674248847,-0.436199115577779,
-0.427073928162626,-0.400948091236321,-0.382860905241332,-0.374822254310016,
-0.34584221065474,-0.333939649620793,-0.324058619604945,-0.29393738163796,
-0.278576588250954,-0.269234263278142,-0.238815915606663,-0.225742435796944,
-0.216239773488962,-0.18666367230127,-0.170750005528772,-0.161294486761502,
-0.129614927749849,-0.114924930935507,-0.106250072717365,-0.0979353687381955,
-0.0965360155478562),.UNSPECIFIED.);
#493=B_SPLINE_CURVE_WITH_KNOTS('',3,(#15185,#15186,#15187,#15188,#15189,
#15190,#15191,#15192,#15193,#15194,#15195,#15196,#15197,#15198,#15199,#15200,
#15201,#15202,#15203,#15204,#15205,#15206,#15207,#15208,#15209,#15210,#15211,
#15212,#15213,#15214,#15215,#15216,#15217,#15218,#15219,#15220,#15221),
 .UNSPECIFIED.,.F.,.F.,(4,3,3,3,3,3,3,3,3,3,3,3,4),(-0.204609524178132,
-0.173922074105667,-0.152149392827302,-0.142793959810126,-0.12983323009626,
-0.11308637627832,-0.0998536142809363,-0.090547498816978,-0.0679106241127335,
-0.0514558350659385,-0.042025593252969,-0.0155529233063705,0.),
 .UNSPECIFIED.);
#494=B_SPLINE_CURVE_WITH_KNOTS('',3,(#15224,#15225,#15226,#15227,#15228,
#15229,#15230,#15231,#15232,#15233,#15234,#15235,#15236,#15237,#15238,#15239),
 .UNSPECIFIED.,.F.,.F.,(4,3,3,3,3,4),(-0.0965360155478562,-0.0724020116608921,
-0.0590232605257019,-0.050388474335024,-0.0186937936910934,0.),
 .UNSPECIFIED.);
#495=B_SPLINE_CURVE_WITH_KNOTS('',3,(#16028,#16029,#16030,#16031,#16032,
#16033,#16034,#16035),.UNSPECIFIED.,.F.,.F.,(4,1,1,1,1,4),(11.6159397475006,
12.61358260836,13.6112254692194,14.6088683300789,15.6065111909383,15.707963267949),
 .UNSPECIFIED.);
#496=B_SPLINE_CURVE_WITH_KNOTS('',3,(#16036,#16037,#16038,#16039,#16040,
#16041,#16042,#16043,#16044,#16045,#16046,#16047,#16048,#16049,#16050,#16051,
#16052,#16053,#16054,#16055,#16056,#16057,#16058,#16059,#16060,#16061,#16062,
#16063,#16064,#16065,#16066,#16067,#16068,#16069,#16070,#16071,#16072,#16073,
#16074,#16075,#16076,#16077,#16078,#16079,#16080,#16081,#16082,#16083,#16084),
 .UNSPECIFIED.,.F.,.F.,(4,3,3,3,3,3,3,3,3,3,3,3,3,3,3,3,4),(-0.275362278356892,
-0.263988733943187,-0.242277787653762,-0.228409792083558,-0.208856161945484,
-0.197709057767663,-0.168075464588018,-0.150222803571495,-0.140083955862437,
-0.125365894046572,-0.0997819296507484,-0.0889593225835958,-0.0667194919376969,
-0.0511923416312717,-0.0404361839568205,-0.0141940669149386,0.),
 .UNSPECIFIED.);
#497=B_SPLINE_CURVE_WITH_KNOTS('',3,(#16085,#16086,#16087,#16088,#16089,
#16090,#16091,#16092,#16093,#16094,#16095,#16096,#16097,#16098,#16099,#16100,
#16101,#16102,#16103),.UNSPECIFIED.,.F.,.F.,(4,3,3,3,3,3,4),(-191.027404416132,
-190.549786424147,-189.552143563287,-188.554500702428,-187.556857841568,
-186.559214980709,-186.304397428656),.UNSPECIFIED.);
#498=B_SPLINE_CURVE_WITH_KNOTS('',3,(#16106,#16107,#16108,#16109,#16110,
#16111,#16112,#16113,#16114),.UNSPECIFIED.,.F.,.F.,(4,1,1,1,1,1,4),(10.3752088276283,
11.2961629976806,12.2942052788047,13.2922475599287,14.2902898410527,15.2883321221767,
15.7079632679491),.UNSPECIFIED.);
#499=B_SPLINE_CURVE_WITH_KNOTS('',3,(#16908,#16909,#16910,#16911,#16912,
#16913,#16914,#16915,#16916,#16917,#16918,#16919,#16920,#16921,#16922,#16923,
#16924,#16925,#16926,#16927,#16928,#16929),.UNSPECIFIED.,.F.,.F.,(4,3,3,
3,3,3,3,4),(183.335115714669,183.639779726821,184.637822007945,185.635864289069,
186.633906570193,187.631948851317,188.629991132441,188.954231742812),
 .UNSPECIFIED.);
#500=B_SPLINE_CURVE_WITH_KNOTS('',3,(#16930,#16931,#16932,#16933,#16934,
#16935,#16936,#16937,#16938,#16939,#16940,#16941,#16942,#16943,#16944,#16945,
#16946,#16947,#16948,#16949,#16950,#16951,#16952,#16953,#16954,#16955,#16956,
#16957,#16958,#16959,#16960,#16961,#16962,#16963,#16964,#16965,#16966,#16967,
#16968,#16969,#16970,#16971,#16972,#16973,#16974,#16975,#16976,#16977,#16978,
#16979,#16980,#16981),.UNSPECIFIED.,.F.,.F.,(4,3,3,3,3,3,3,3,3,3,3,3,3,
3,3,3,3,4),(-0.276631791712714,-0.267404104599176,-0.245529112929484,-0.233826742508505,
-0.212230201958684,-0.201819484750363,-0.173281546649687,-0.162756755581661,
-0.152537502224722,-0.140478169692516,-0.120739781640826,-0.110641775261762,
-0.100726383882944,-0.0755447879122082,-0.0587891884452614,-0.0493012364577666,
-0.0182848522583483,0.),.UNSPECIFIED.);
#559=SHAPE_REPRESENTATION_RELATIONSHIP('SRR','None',#18630,#568);
#568=ADVANCED_BREP_SHAPE_REPRESENTATION('',(#586),#18576);
#577=STYLED_ITEM('',(#18685),#586);
#586=MANIFOLD_SOLID_BREP('Body1',#6549);
#633=FACE_BOUND('',#1526,.T.);
#634=FACE_BOUND('',#1529,.T.);
#764=PLANE('',#7017);
#765=PLANE('',#7018);
#766=PLANE('',#7019);
#767=PLANE('',#7020);
#768=PLANE('',#7021);
#769=PLANE('',#7022);
#770=PLANE('',#7023);
#771=PLANE('',#7024);
#772=PLANE('',#7028);
#773=PLANE('',#7029);
#1034=FACE_OUTER_BOUND('',#1453,.T.);
#1035=FACE_OUTER_BOUND('',#1454,.T.);
#1036=FACE_OUTER_BOUND('',#1455,.T.);
#1037=FACE_OUTER_BOUND('',#1456,.T.);
#1038=FACE_OUTER_BOUND('',#1457,.T.);
#1039=FACE_OUTER_BOUND('',#1458,.T.);
#1040=FACE_OUTER_BOUND('',#1459,.T.);
#1041=FACE_OUTER_BOUND('',#1460,.T.);
#1042=FACE_OUTER_BOUND('',#1461,.T.);
#1043=FACE_OUTER_BOUND('',#1462,.T.);
#1044=FACE_OUTER_BOUND('',#1463,.T.);
#1045=FACE_OUTER_BOUND('',#1464,.T.);
#1046=FACE_OUTER_BOUND('',#1465,.T.);
#1047=FACE_OUTER_BOUND('',#1466,.T.);
#1048=FACE_OUTER_BOUND('',#1467,.T.);
#1049=FACE_OUTER_BOUND('',#1468,.T.);
#1050=FACE_OUTER_BOUND('',#1469,.T.);
#1051=FACE_OUTER_BOUND('',#1470,.T.);
#1052=FACE_OUTER_BOUND('',#1471,.T.);
#1053=FACE_OUTER_BOUND('',#1472,.T.);
#1054=FACE_OUTER_BOUND('',#1473,.T.);
#1055=FACE_OUTER_BOUND('',#1474,.T.);
#1056=FACE_OUTER_BOUND('',#1475,.T.);
#1057=FACE_OUTER_BOUND('',#1476,.T.);
#1058=FACE_OUTER_BOUND('',#1477,.T.);
#1059=FACE_OUTER_BOUND('',#1478,.T.);
#1060=FACE_OUTER_BOUND('',#1479,.T.);
#1061=FACE_OUTER_BOUND('',#1480,.T.);
#1062=FACE_OUTER_BOUND('',#1481,.T.);
#1063=FACE_OUTER_BOUND('',#1482,.T.);
#1064=FACE_OUTER_BOUND('',#1483,.T.);
#1065=FACE_OUTER_BOUND('',#1484,.T.);
#1066=FACE_OUTER_BOUND('',#1485,.T.);
#1067=FACE_OUTER_BOUND('',#1486,.T.);
#1068=FACE_OUTER_BOUND('',#1487,.T.);
#1069=FACE_OUTER_BOUND('',#1488,.T.);
#1070=FACE_OUTER_BOUND('',#1489,.T.);
#1071=FACE_OUTER_BOUND('',#1490,.T.);
#1072=FACE_OUTER_BOUND('',#1491,.T.);
#1073=FACE_OUTER_BOUND('',#1492,.T.);
#1074=FACE_OUTER_BOUND('',#1493,.T.);
#1075=FACE_OUTER_BOUND('',#1494,.T.);
#1076=FACE_OUTER_BOUND('',#1495,.T.);
#1077=FACE_OUTER_BOUND('',#1496,.T.);
#1078=FACE_OUTER_BOUND('',#1497,.T.);
#1079=FACE_OUTER_BOUND('',#1498,.T.);
#1080=FACE_OUTER_BOUND('',#1499,.T.);
#1081=FACE_OUTER_BOUND('',#1500,.T.);
#1082=FACE_OUTER_BOUND('',#1501,.T.);
#1083=FACE_OUTER_BOUND('',#1502,.T.);
#1084=FACE_OUTER_BOUND('',#1503,.T.);
#1085=FACE_OUTER_BOUND('',#1504,.T.);
#1086=FACE_OUTER_BOUND('',#1505,.T.);
#1087=FACE_OUTER_BOUND('',#1506,.T.);
#1088=FACE_OUTER_BOUND('',#1507,.T.);
#1089=FACE_OUTER_BOUND('',#1508,.T.);
#1090=FACE_OUTER_BOUND('',#1509,.T.);
#1091=FACE_OUTER_BOUND('',#1510,.T.);
#1092=FACE_OUTER_BOUND('',#1511,.T.);
#1093=FACE_OUTER_BOUND('',#1512,.T.);
#1094=FACE_OUTER_BOUND('',#1513,.T.);
#1095=FACE_OUTER_BOUND('',#1514,.T.);
#1096=FACE_OUTER_BOUND('',#1515,.T.);
#1097=FACE_OUTER_BOUND('',#1516,.T.);
#1098=FACE_OUTER_BOUND('',#1517,.T.);
#1099=FACE_OUTER_BOUND('',#1518,.T.);
#1100=FACE_OUTER_BOUND('',#1519,.T.);
#1101=FACE_OUTER_BOUND('',#1520,.T.);
#1102=FACE_OUTER_BOUND('',#1521,.T.);
#1103=FACE_OUTER_BOUND('',#1522,.T.);
#1104=FACE_OUTER_BOUND('',#1523,.T.);
#1105=FACE_OUTER_BOUND('',#1524,.T.);
#1106=FACE_OUTER_BOUND('',#1525,.T.);
#1107=FACE_OUTER_BOUND('',#1527,.T.);
#1108=FACE_OUTER_BOUND('',#1528,.T.);
#1109=FACE_OUTER_BOUND('',#1530,.T.);
#1453=EDGE_LOOP('',(#5330,#5331,#5332,#5333));
#1454=EDGE_LOOP('',(#5334,#5335,#5336,#5337));
#1455=EDGE_LOOP('',(#5338,#5339,#5340,#5341));
#1456=EDGE_LOOP('',(#5342,#5343,#5344,#5345));
#1457=EDGE_LOOP('',(#5346,#5347,#5348,#5349));
#1458=EDGE_LOOP('',(#5350,#5351,#5352,#5353));
#1459=EDGE_LOOP('',(#5354,#5355,#5356,#5357));
#1460=EDGE_LOOP('',(#5358,#5359,#5360,#5361));
#1461=EDGE_LOOP('',(#5362,#5363,#5364,#5365));
#1462=EDGE_LOOP('',(#5366,#5367,#5368,#5369));
#1463=EDGE_LOOP('',(#5370,#5371,#5372,#5373));
#1464=EDGE_LOOP('',(#5374,#5375,#5376,#5377));
#1465=EDGE_LOOP('',(#5378,#5379,#5380,#5381));
#1466=EDGE_LOOP('',(#5382,#5383,#5384,#5385));
#1467=EDGE_LOOP('',(#5386,#5387,#5388,#5389));
#1468=EDGE_LOOP('',(#5390,#5391,#5392,#5393));
#1469=EDGE_LOOP('',(#5394,#5395,#5396,#5397));
#1470=EDGE_LOOP('',(#5398,#5399,#5400,#5401));
#1471=EDGE_LOOP('',(#5402,#5403,#5404,#5405));
#1472=EDGE_LOOP('',(#5406,#5407,#5408,#5409));
#1473=EDGE_LOOP('',(#5410,#5411,#5412,#5413));
#1474=EDGE_LOOP('',(#5414,#5415,#5416,#5417));
#1475=EDGE_LOOP('',(#5418,#5419,#5420,#5421));
#1476=EDGE_LOOP('',(#5422,#5423,#5424,#5425));
#1477=EDGE_LOOP('',(#5426,#5427,#5428,#5429));
#1478=EDGE_LOOP('',(#5430,#5431,#5432,#5433));
#1479=EDGE_LOOP('',(#5434,#5435,#5436,#5437));
#1480=EDGE_LOOP('',(#5438,#5439,#5440,#5441));
#1481=EDGE_LOOP('',(#5442,#5443,#5444,#5445));
#1482=EDGE_LOOP('',(#5446,#5447,#5448,#5449));
#1483=EDGE_LOOP('',(#5450,#5451,#5452,#5453));
#1484=EDGE_LOOP('',(#5454,#5455,#5456,#5457));
#1485=EDGE_LOOP('',(#5458,#5459,#5460,#5461));
#1486=EDGE_LOOP('',(#5462,#5463,#5464,#5465));
#1487=EDGE_LOOP('',(#5466,#5467,#5468,#5469));
#1488=EDGE_LOOP('',(#5470,#5471,#5472,#5473));
#1489=EDGE_LOOP('',(#5474,#5475,#5476,#5477));
#1490=EDGE_LOOP('',(#5478,#5479,#5480,#5481));
#1491=EDGE_LOOP('',(#5482,#5483,#5484,#5485));
#1492=EDGE_LOOP('',(#5486,#5487,#5488,#5489));
#1493=EDGE_LOOP('',(#5490,#5491,#5492,#5493));
#1494=EDGE_LOOP('',(#5494,#5495,#5496,#5497));
#1495=EDGE_LOOP('',(#5498,#5499,#5500,#5501));
#1496=EDGE_LOOP('',(#5502,#5503,#5504,#5505));
#1497=EDGE_LOOP('',(#5506,#5507,#5508,#5509));
#1498=EDGE_LOOP('',(#5510,#5511,#5512,#5513));
#1499=EDGE_LOOP('',(#5514,#5515,#5516,#5517));
#1500=EDGE_LOOP('',(#5518,#5519,#5520,#5521));
#1501=EDGE_LOOP('',(#5522,#5523,#5524,#5525));
#1502=EDGE_LOOP('',(#5526,#5527,#5528,#5529));
#1503=EDGE_LOOP('',(#5530,#5531,#5532,#5533));
#1504=EDGE_LOOP('',(#5534,#5535,#5536,#5537));
#1505=EDGE_LOOP('',(#5538,#5539,#5540,#5541));
#1506=EDGE_LOOP('',(#5542,#5543,#5544,#5545));
#1507=EDGE_LOOP('',(#5546,#5547,#5548,#5549));
#1508=EDGE_LOOP('',(#5550,#5551,#5552,#5553));
#1509=EDGE_LOOP('',(#5554,#5555,#5556,#5557));
#1510=EDGE_LOOP('',(#5558,#5559,#5560,#5561));
#1511=EDGE_LOOP('',(#5562,#5563,#5564,#5565));
#1512=EDGE_LOOP('',(#5566,#5567,#5568,#5569));
#1513=EDGE_LOOP('',(#5570,#5571,#5572,#5573,#5574,#5575,#5576,#5577));
#1514=EDGE_LOOP('',(#5578,#5579,#5580,#5581,#5582,#5583,#5584,#5585,#5586,
#5587,#5588,#5589,#5590,#5591,#5592,#5593,#5594,#5595,#5596,#5597,#5598,
#5599,#5600,#5601,#5602,#5603,#5604,#5605,#5606,#5607,#5608,#5609,#5610,
#5611,#5612,#5613,#5614,#5615,#5616,#5617,#5618,#5619,#5620,#5621,#5622,
#5623,#5624,#5625,#5626,#5627,#5628,#5629,#5630,#5631,#5632,#5633,#5634,
#5635,#5636,#5637,#5638,#5639,#5640,#5641));
#1515=EDGE_LOOP('',(#5642,#5643,#5644,#5645));
#1516=EDGE_LOOP('',(#5646,#5647,#5648,#5649,#5650,#5651,#5652,#5653,#5654,
#5655,#5656,#5657,#5658,#5659,#5660,#5661,#5662,#5663,#5664,#5665,#5666,
#5667,#5668,#5669,#5670,#5671,#5672,#5673,#5674,#5675,#5676,#5677,#5678,
#5679,#5680,#5681,#5682,#5683,#5684,#5685,#5686,#5687,#5688,#5689,#5690,
#5691,#5692,#5693,#5694,#5695,#5696,#5697,#5698,#5699,#5700,#5701,#5702,
#5703,#5704,#5705,#5706,#5707,#5708,#5709,#5710));
#1517=EDGE_LOOP('',(#5711,#5712,#5713,#5714));
#1518=EDGE_LOOP('',(#5715,#5716,#5717,#5718));
#1519=EDGE_LOOP('',(#5719,#5720,#5721,#5722));
#1520=EDGE_LOOP('',(#5723,#5724,#5725,#5726));
#1521=EDGE_LOOP('',(#5727,#5728,#5729,#5730));
#1522=EDGE_LOOP('',(#5731,#5732,#5733,#5734));
#1523=EDGE_LOOP('',(#5735,#5736,#5737,#5738));
#1524=EDGE_LOOP('',(#5739,#5740,#5741,#5742,#5743,#5744));
#1525=EDGE_LOOP('',(#5745));
#1526=EDGE_LOOP('',(#5746,#5747,#5748,#5749));
#1527=EDGE_LOOP('',(#5750,#5751,#5752,#5753));
#1528=EDGE_LOOP('',(#5754));
#1529=EDGE_LOOP('',(#5755,#5756,#5757,#5758,#5759,#5760));
#1530=EDGE_LOOP('',(#5761));
#1890=LINE('',#12865,#2297);
#1891=LINE('',#12889,#2298);
#1892=LINE('',#12937,#2299);
#1893=LINE('',#12985,#2300);
#1894=LINE('',#13036,#2301);
#1895=LINE('',#13084,#2302);
#1896=LINE('',#13132,#2303);
#1897=LINE('',#13180,#2304);
#1898=LINE('',#13234,#2305);
#1899=LINE('',#13282,#2306);
#1900=LINE('',#13330,#2307);
#1901=LINE('',#13384,#2308);
#1902=LINE('',#13432,#2309);
#1903=LINE('',#13480,#2310);
#1904=LINE('',#13528,#2311);
#1905=LINE('',#13582,#2312);
#1906=LINE('',#13630,#2313);
#1907=LINE('',#13678,#2314);
#1908=LINE('',#13732,#2315);
#1909=LINE('',#13780,#2316);
#1910=LINE('',#13828,#2317);
#1911=LINE('',#13882,#2318);
#1912=LINE('',#13930,#2319);
#1913=LINE('',#13978,#2320);
#1914=LINE('',#14026,#2321);
#1915=LINE('',#14080,#2322);
#1916=LINE('',#14128,#2323);
#1917=LINE('',#14176,#2324);
#1918=LINE('',#14230,#2325);
#1919=LINE('',#14278,#2326);
#1920=LINE('',#14326,#2327);
#1921=LINE('',#14352,#2328);
#1922=LINE('',#14376,#2329);
#1923=LINE('',#14400,#2330);
#1924=LINE('',#14425,#2331);
#1925=LINE('',#14450,#2332);
#1926=LINE('',#14474,#2333);
#1927=LINE('',#14499,#2334);
#1928=LINE('',#14524,#2335);
#1929=LINE('',#14548,#2336);
#1930=LINE('',#14572,#2337);
#1931=LINE('',#14597,#2338);
#1932=LINE('',#14622,#2339);
#1933=LINE('',#14646,#2340);
#1934=LINE('',#14671,#2341);
#1935=LINE('',#14696,#2342);
#1936=LINE('',#14720,#2343);
#1937=LINE('',#14745,#2344);
#1938=LINE('',#14770,#2345);
#1939=LINE('',#14794,#2346);
#1940=LINE('',#14818,#2347);
#1941=LINE('',#14843,#2348);
#1942=LINE('',#14868,#2349);
#1943=LINE('',#14892,#2350);
#1944=LINE('',#14917,#2351);
#1945=LINE('',#14942,#2352);
#1946=LINE('',#14966,#2353);
#1947=LINE('',#14991,#2354);
#1948=LINE('',#15015,#2355);
#1949=LINE('',#15040,#2356);
#1950=LINE('',#15241,#2357);
#1951=LINE('',#16986,#2358);
#1952=LINE('',#16988,#2359);
#1953=LINE('',#16990,#2360);
#1954=LINE('',#16991,#2361);
#1955=LINE('',#16994,#2362);
#1956=LINE('',#16996,#2363);
#1957=LINE('',#16997,#2364);
#1958=LINE('',#17000,#2365);
#1959=LINE('',#17002,#2366);
#1960=LINE('',#17003,#2367);
#1961=LINE('',#17006,#2368);
#1962=LINE('',#17008,#2369);
#1963=LINE('',#17009,#2370);
#1964=LINE('',#17012,#2371);
#1965=LINE('',#17014,#2372);
#1966=LINE('',#17015,#2373);
#1967=LINE('',#17017,#2374);
#1968=LINE('',#17018,#2375);
#1969=LINE('',#17025,#2376);
#2297=VECTOR('',#8009,0.15);
#2298=VECTOR('',#8014,0.15);
#2299=VECTOR('',#8017,0.15);
#2300=VECTOR('',#8020,0.15);
#2301=VECTOR('',#8023,0.15);
#2302=VECTOR('',#8026,0.15);
#2303=VECTOR('',#8029,0.15);
#2304=VECTOR('',#8032,0.15);
#2305=VECTOR('',#8035,0.15);
#2306=VECTOR('',#8038,0.15);
#2307=VECTOR('',#8041,0.15);
#2308=VECTOR('',#8044,0.15);
#2309=VECTOR('',#8047,0.15);
#2310=VECTOR('',#8050,0.15);
#2311=VECTOR('',#8053,0.15);
#2312=VECTOR('',#8056,0.15);
#2313=VECTOR('',#8059,0.15);
#2314=VECTOR('',#8062,0.15);
#2315=VECTOR('',#8065,0.15);
#2316=VECTOR('',#8068,0.15);
#2317=VECTOR('',#8071,0.15);
#2318=VECTOR('',#8074,0.15);
#2319=VECTOR('',#8077,0.15);
#2320=VECTOR('',#8080,0.15);
#2321=VECTOR('',#8083,0.15);
#2322=VECTOR('',#8086,0.15);
#2323=VECTOR('',#8089,0.15);
#2324=VECTOR('',#8092,0.15);
#2325=VECTOR('',#8095,0.15);
#2326=VECTOR('',#8098,0.15);
#2327=VECTOR('',#8101,0.117775);
#2328=VECTOR('',#8106,0.117775);
#2329=VECTOR('',#8109,0.117775);
#2330=VECTOR('',#8112,0.117775);
#2331=VECTOR('',#8115,0.117775);
#2332=VECTOR('',#8118,0.117775);
#2333=VECTOR('',#8121,0.117775);
#2334=VECTOR('',#8124,0.117775);
#2335=VECTOR('',#8127,0.117775);
#2336=VECTOR('',#8130,0.117775);
#2337=VECTOR('',#8133,0.117775);
#2338=VECTOR('',#8136,0.117775);
#2339=VECTOR('',#8139,0.117775);
#2340=VECTOR('',#8142,0.117775);
#2341=VECTOR('',#8145,0.117775);
#2342=VECTOR('',#8148,0.117775);
#2343=VECTOR('',#8151,0.117775);
#2344=VECTOR('',#8154,0.117775);
#2345=VECTOR('',#8157,0.117775);
#2346=VECTOR('',#8160,0.117775);
#2347=VECTOR('',#8163,0.117775);
#2348=VECTOR('',#8166,0.117775);
#2349=VECTOR('',#8169,0.117775);
#2350=VECTOR('',#8172,0.117775);
#2351=VECTOR('',#8175,0.117775);
#2352=VECTOR('',#8178,0.117775);
#2353=VECTOR('',#8181,0.117775);
#2354=VECTOR('',#8184,0.117775);
#2355=VECTOR('',#8187,0.117775);
#2356=VECTOR('',#8190,0.117775);
#2357=VECTOR('',#8195,0.1);
#2358=VECTOR('',#8206,1.);
#2359=VECTOR('',#8207,1.);
#2360=VECTOR('',#8208,1.);
#2361=VECTOR('',#8209,1.);
#2362=VECTOR('',#8212,1.);
#2363=VECTOR('',#8213,1.);
#2364=VECTOR('',#8214,1.);
#2365=VECTOR('',#8217,1.);
#2366=VECTOR('',#8218,1.);
#2367=VECTOR('',#8219,1.);
#2368=VECTOR('',#8222,1.);
#2369=VECTOR('',#8223,1.);
#2370=VECTOR('',#8224,1.);
#2371=VECTOR('',#8227,1.);
#2372=VECTOR('',#8228,1.);
#2373=VECTOR('',#8229,1.);
#2374=VECTOR('',#8232,1.);
#2375=VECTOR('',#8233,1.);
#2376=VECTOR('',#8242,0.275);
#2537=CIRCLE('',#6950,0.14635);
#2538=CIRCLE('',#6981,0.117775);
#2539=CIRCLE('',#7012,0.14635);
#2540=CIRCLE('',#7013,0.05);
#2541=CIRCLE('',#7015,0.117775);
#2542=CIRCLE('',#7025,0.275);
#2543=CIRCLE('',#7027,0.275);
#2961=VERTEX_POINT('',#12863);
#2962=VERTEX_POINT('',#12864);
#2963=VERTEX_POINT('',#12866);
#2964=VERTEX_POINT('',#12877);
#2965=VERTEX_POINT('',#12887);
#2966=VERTEX_POINT('',#12888);
#2967=VERTEX_POINT('',#12935);
#2968=VERTEX_POINT('',#12936);
#2969=VERTEX_POINT('',#12983);
#2970=VERTEX_POINT('',#12984);
#2971=VERTEX_POINT('',#13034);
#2972=VERTEX_POINT('',#13035);
#2973=VERTEX_POINT('',#13082);
#2974=VERTEX_POINT('',#13083);
#2975=VERTEX_POINT('',#13130);
#2976=VERTEX_POINT('',#13131);
#2977=VERTEX_POINT('',#13178);
#2978=VERTEX_POINT('',#13179);
#2979=VERTEX_POINT('',#13232);
#2980=VERTEX_POINT('',#13233);
#2981=VERTEX_POINT('',#13280);
#2982=VERTEX_POINT('',#13281);
#2983=VERTEX_POINT('',#13328);
#2984=VERTEX_POINT('',#13329);
#2985=VERTEX_POINT('',#13382);
#2986=VERTEX_POINT('',#13383);
#2987=VERTEX_POINT('',#13430);
#2988=VERTEX_POINT('',#13431);
#2989=VERTEX_POINT('',#13478);
#2990=VERTEX_POINT('',#13479);
#2991=VERTEX_POINT('',#13526);
#2992=VERTEX_POINT('',#13527);
#2993=VERTEX_POINT('',#13580);
#2994=VERTEX_POINT('',#13581);
#2995=VERTEX_POINT('',#13628);
#2996=VERTEX_POINT('',#13629);
#2997=VERTEX_POINT('',#13676);
#2998=VERTEX_POINT('',#13677);
#2999=VERTEX_POINT('',#13730);
#3000=VERTEX_POINT('',#13731);
#3001=VERTEX_POINT('',#13778);
#3002=VERTEX_POINT('',#13779);
#3003=VERTEX_POINT('',#13826);
#3004=VERTEX_POINT('',#13827);
#3005=VERTEX_POINT('',#13880);
#3006=VERTEX_POINT('',#13881);
#3007=VERTEX_POINT('',#13928);
#3008=VERTEX_POINT('',#13929);
#3009=VERTEX_POINT('',#13976);
#3010=VERTEX_POINT('',#13977);
#3011=VERTEX_POINT('',#14024);
#3012=VERTEX_POINT('',#14025);
#3013=VERTEX_POINT('',#14078);
#3014=VERTEX_POINT('',#14079);
#3015=VERTEX_POINT('',#14126);
#3016=VERTEX_POINT('',#14127);
#3017=VERTEX_POINT('',#14174);
#3018=VERTEX_POINT('',#14175);
#3019=VERTEX_POINT('',#14228);
#3020=VERTEX_POINT('',#14229);
#3021=VERTEX_POINT('',#14276);
#3022=VERTEX_POINT('',#14277);
#3023=VERTEX_POINT('',#14324);
#3024=VERTEX_POINT('',#14325);
#3025=VERTEX_POINT('',#14327);
#3026=VERTEX_POINT('',#14338);
#3027=VERTEX_POINT('',#14350);
#3028=VERTEX_POINT('',#14351);
#3029=VERTEX_POINT('',#14374);
#3030=VERTEX_POINT('',#14375);
#3031=VERTEX_POINT('',#14398);
#3032=VERTEX_POINT('',#14399);
#3033=VERTEX_POINT('',#14423);
#3034=VERTEX_POINT('',#14424);
#3035=VERTEX_POINT('',#14448);
#3036=VERTEX_POINT('',#14449);
#3037=VERTEX_POINT('',#14472);
#3038=VERTEX_POINT('',#14473);
#3039=VERTEX_POINT('',#14497);
#3040=VERTEX_POINT('',#14498);
#3041=VERTEX_POINT('',#14522);
#3042=VERTEX_POINT('',#14523);
#3043=VERTEX_POINT('',#14546);
#3044=VERTEX_POINT('',#14547);
#3045=VERTEX_POINT('',#14570);
#3046=VERTEX_POINT('',#14571);
#3047=VERTEX_POINT('',#14595);
#3048=VERTEX_POINT('',#14596);
#3049=VERTEX_POINT('',#14620);
#3050=VERTEX_POINT('',#14621);
#3051=VERTEX_POINT('',#14644);
#3052=VERTEX_POINT('',#14645);
#3053=VERTEX_POINT('',#14669);
#3054=VERTEX_POINT('',#14670);
#3055=VERTEX_POINT('',#14694);
#3056=VERTEX_POINT('',#14695);
#3057=VERTEX_POINT('',#14718);
#3058=VERTEX_POINT('',#14719);
#3059=VERTEX_POINT('',#14743);
#3060=VERTEX_POINT('',#14744);
#3061=VERTEX_POINT('',#14768);
#3062=VERTEX_POINT('',#14769);
#3063=VERTEX_POINT('',#14792);
#3064=VERTEX_POINT('',#14793);
#3065=VERTEX_POINT('',#14816);
#3066=VERTEX_POINT('',#14817);
#3067=VERTEX_POINT('',#14841);
#3068=VERTEX_POINT('',#14842);
#3069=VERTEX_POINT('',#14866);
#3070=VERTEX_POINT('',#14867);
#3071=VERTEX_POINT('',#14890);
#3072=VERTEX_POINT('',#14891);
#3073=VERTEX_POINT('',#14915);
#3074=VERTEX_POINT('',#14916);
#3075=VERTEX_POINT('',#14940);
#3076=VERTEX_POINT('',#14941);
#3077=VERTEX_POINT('',#14964);
#3078=VERTEX_POINT('',#14965);
#3079=VERTEX_POINT('',#14989);
#3080=VERTEX_POINT('',#14990);
#3081=VERTEX_POINT('',#15013);
#3082=VERTEX_POINT('',#15014);
#3083=VERTEX_POINT('',#15038);
#3084=VERTEX_POINT('',#15039);
#3085=VERTEX_POINT('',#15062);
#3086=VERTEX_POINT('',#15184);
#3087=VERTEX_POINT('',#15222);
#3088=VERTEX_POINT('',#15240);
#3089=VERTEX_POINT('',#16027);
#3090=VERTEX_POINT('',#16105);
#3091=VERTEX_POINT('',#16984);
#3092=VERTEX_POINT('',#16985);
#3093=VERTEX_POINT('',#16987);
#3094=VERTEX_POINT('',#16989);
#3095=VERTEX_POINT('',#16993);
#3096=VERTEX_POINT('',#16995);
#3097=VERTEX_POINT('',#16999);
#3098=VERTEX_POINT('',#17001);
#3099=VERTEX_POINT('',#17005);
#3100=VERTEX_POINT('',#17007);
#3101=VERTEX_POINT('',#17011);
#3102=VERTEX_POINT('',#17013);
#3103=VERTEX_POINT('',#17021);
#3104=VERTEX_POINT('',#17024);
#3788=EDGE_CURVE('',#2961,#2962,#1890,.T.);
#3789=EDGE_CURVE('',#2961,#2963,#372,.T.);
#3790=EDGE_CURVE('',#2963,#2964,#2537,.F.);
#3791=EDGE_CURVE('',#2964,#2962,#373,.T.);
#3792=EDGE_CURVE('',#2965,#2966,#1891,.T.);
#3793=EDGE_CURVE('',#2965,#2961,#374,.T.);
#3794=EDGE_CURVE('',#2962,#2966,#375,.T.);
#3795=EDGE_CURVE('',#2967,#2968,#1892,.T.);
#3796=EDGE_CURVE('',#2967,#2965,#376,.T.);
#3797=EDGE_CURVE('',#2966,#2968,#377,.T.);
#3798=EDGE_CURVE('',#2969,#2970,#1893,.T.);
#3799=EDGE_CURVE('',#2969,#2967,#378,.T.);
#3800=EDGE_CURVE('',#2968,#2970,#379,.T.);
#3801=EDGE_CURVE('',#2971,#2972,#1894,.T.);
#3802=EDGE_CURVE('',#2971,#2969,#380,.T.);
#3803=EDGE_CURVE('',#2970,#2972,#381,.T.);
#3804=EDGE_CURVE('',#2973,#2974,#1895,.T.);
#3805=EDGE_CURVE('',#2973,#2971,#382,.T.);
#3806=EDGE_CURVE('',#2972,#2974,#383,.T.);
#3807=EDGE_CURVE('',#2975,#2976,#1896,.T.);
#3808=EDGE_CURVE('',#2975,#2973,#384,.T.);
#3809=EDGE_CURVE('',#2974,#2976,#385,.T.);
#3810=EDGE_CURVE('',#2977,#2978,#1897,.T.);
#3811=EDGE_CURVE('',#2977,#2975,#386,.T.);
#3812=EDGE_CURVE('',#2976,#2978,#387,.T.);
#3813=EDGE_CURVE('',#2979,#2980,#1898,.T.);
#3814=EDGE_CURVE('',#2979,#2977,#388,.T.);
#3815=EDGE_CURVE('',#2978,#2980,#389,.T.);
#3816=EDGE_CURVE('',#2981,#2982,#1899,.T.);
#3817=EDGE_CURVE('',#2981,#2979,#390,.T.);
#3818=EDGE_CURVE('',#2980,#2982,#391,.T.);
#3819=EDGE_CURVE('',#2983,#2984,#1900,.T.);
#3820=EDGE_CURVE('',#2983,#2981,#392,.T.);
#3821=EDGE_CURVE('',#2982,#2984,#393,.T.);
#3822=EDGE_CURVE('',#2985,#2986,#1901,.T.);
#3823=EDGE_CURVE('',#2985,#2983,#394,.T.);
#3824=EDGE_CURVE('',#2984,#2986,#395,.T.);
#3825=EDGE_CURVE('',#2987,#2988,#1902,.T.);
#3826=EDGE_CURVE('',#2987,#2985,#396,.T.);
#3827=EDGE_CURVE('',#2986,#2988,#397,.T.);
#3828=EDGE_CURVE('',#2989,#2990,#1903,.T.);
#3829=EDGE_CURVE('',#2989,#2987,#398,.T.);
#3830=EDGE_CURVE('',#2988,#2990,#399,.T.);
#3831=EDGE_CURVE('',#2991,#2992,#1904,.T.);
#3832=EDGE_CURVE('',#2991,#2989,#400,.T.);
#3833=EDGE_CURVE('',#2990,#2992,#401,.T.);
#3834=EDGE_CURVE('',#2993,#2994,#1905,.T.);
#3835=EDGE_CURVE('',#2993,#2991,#402,.T.);
#3836=EDGE_CURVE('',#2992,#2994,#403,.T.);
#3837=EDGE_CURVE('',#2995,#2996,#1906,.T.);
#3838=EDGE_CURVE('',#2995,#2993,#404,.T.);
#3839=EDGE_CURVE('',#2994,#2996,#405,.T.);
#3840=EDGE_CURVE('',#2997,#2998,#1907,.T.);
#3841=EDGE_CURVE('',#2997,#2995,#406,.T.);
#3842=EDGE_CURVE('',#2996,#2998,#407,.T.);
#3843=EDGE_CURVE('',#2999,#3000,#1908,.T.);
#3844=EDGE_CURVE('',#2999,#2997,#408,.T.);
#3845=EDGE_CURVE('',#2998,#3000,#409,.T.);
#3846=EDGE_CURVE('',#3001,#3002,#1909,.T.);
#3847=EDGE_CURVE('',#3001,#2999,#410,.T.);
#3848=EDGE_CURVE('',#3000,#3002,#411,.T.);
#3849=EDGE_CURVE('',#3003,#3004,#1910,.T.);
#3850=EDGE_CURVE('',#3003,#3001,#412,.T.);
#3851=EDGE_CURVE('',#3002,#3004,#413,.T.);
#3852=EDGE_CURVE('',#3005,#3006,#1911,.T.);
#3853=EDGE_CURVE('',#3005,#3003,#414,.T.);
#3854=EDGE_CURVE('',#3004,#3006,#415,.T.);
#3855=EDGE_CURVE('',#3007,#3008,#1912,.T.);
#3856=EDGE_CURVE('',#3007,#3005,#416,.T.);
#3857=EDGE_CURVE('',#3006,#3008,#417,.T.);
#3858=EDGE_CURVE('',#3009,#3010,#1913,.T.);
#3859=EDGE_CURVE('',#3009,#3007,#418,.T.);
#3860=EDGE_CURVE('',#3008,#3010,#419,.T.);
#3861=EDGE_CURVE('',#3011,#3012,#1914,.T.);
#3862=EDGE_CURVE('',#3011,#3009,#420,.T.);
#3863=EDGE_CURVE('',#3010,#3012,#421,.T.);
#3864=EDGE_CURVE('',#3013,#3014,#1915,.T.);
#3865=EDGE_CURVE('',#3013,#3011,#422,.T.);
#3866=EDGE_CURVE('',#3012,#3014,#423,.T.);
#3867=EDGE_CURVE('',#3015,#3016,#1916,.T.);
#3868=EDGE_CURVE('',#3015,#3013,#424,.T.);
#3869=EDGE_CURVE('',#3014,#3016,#425,.T.);
#3870=EDGE_CURVE('',#3017,#3018,#1917,.T.);
#3871=EDGE_CURVE('',#3017,#3015,#426,.T.);
#3872=EDGE_CURVE('',#3016,#3018,#427,.T.);
#3873=EDGE_CURVE('',#3019,#3020,#1918,.T.);
#3874=EDGE_CURVE('',#3019,#3017,#428,.T.);
#3875=EDGE_CURVE('',#3018,#3020,#429,.T.);
#3876=EDGE_CURVE('',#3021,#3022,#1919,.T.);
#3877=EDGE_CURVE('',#3021,#3019,#430,.T.);
#3878=EDGE_CURVE('',#3020,#3022,#431,.T.);
#3879=EDGE_CURVE('',#3023,#3024,#1920,.T.);
#3880=EDGE_CURVE('',#3023,#3025,#432,.T.);
#3881=EDGE_CURVE('',#3025,#3026,#2538,.T.);
#3882=EDGE_CURVE('',#3024,#3026,#433,.T.);
#3883=EDGE_CURVE('',#3027,#3028,#1921,.T.);
#3884=EDGE_CURVE('',#3027,#3023,#434,.T.);
#3885=EDGE_CURVE('',#3028,#3024,#435,.T.);
#3886=EDGE_CURVE('',#3029,#3030,#1922,.T.);
#3887=EDGE_CURVE('',#3029,#3027,#436,.T.);
#3888=EDGE_CURVE('',#3030,#3028,#437,.T.);
#3889=EDGE_CURVE('',#3031,#3032,#1923,.T.);
#3890=EDGE_CURVE('',#3031,#3029,#438,.T.);
#3891=EDGE_CURVE('',#3032,#3030,#439,.T.);
#3892=EDGE_CURVE('',#3033,#3034,#1924,.T.);
#3893=EDGE_CURVE('',#3033,#3031,#440,.T.);
#3894=EDGE_CURVE('',#3034,#3032,#441,.T.);
#3895=EDGE_CURVE('',#3035,#3036,#1925,.T.);
#3896=EDGE_CURVE('',#3035,#3033,#442,.T.);
#3897=EDGE_CURVE('',#3036,#3034,#443,.T.);
#3898=EDGE_CURVE('',#3037,#3038,#1926,.T.);
#3899=EDGE_CURVE('',#3037,#3035,#444,.T.);
#3900=EDGE_CURVE('',#3038,#3036,#445,.T.);
#3901=EDGE_CURVE('',#3039,#3040,#1927,.T.);
#3902=EDGE_CURVE('',#3039,#3037,#446,.T.);
#3903=EDGE_CURVE('',#3040,#3038,#447,.T.);
#3904=EDGE_CURVE('',#3041,#3042,#1928,.T.);
#3905=EDGE_CURVE('',#3041,#3039,#448,.T.);
#3906=EDGE_CURVE('',#3042,#3040,#449,.T.);
#3907=EDGE_CURVE('',#3043,#3044,#1929,.T.);
#3908=EDGE_CURVE('',#3043,#3041,#450,.T.);
#3909=EDGE_CURVE('',#3044,#3042,#451,.T.);
#3910=EDGE_CURVE('',#3045,#3046,#1930,.T.);
#3911=EDGE_CURVE('',#3045,#3043,#452,.T.);
#3912=EDGE_CURVE('',#3046,#3044,#453,.T.);
#3913=EDGE_CURVE('',#3047,#3048,#1931,.T.);
#3914=EDGE_CURVE('',#3047,#3045,#454,.T.);
#3915=EDGE_CURVE('',#3048,#3046,#455,.T.);
#3916=EDGE_CURVE('',#3049,#3050,#1932,.T.);
#3917=EDGE_CURVE('',#3049,#3047,#456,.T.);
#3918=EDGE_CURVE('',#3050,#3048,#457,.T.);
#3919=EDGE_CURVE('',#3051,#3052,#1933,.T.);
#3920=EDGE_CURVE('',#3051,#3049,#458,.T.);
#3921=EDGE_CURVE('',#3052,#3050,#459,.T.);
#3922=EDGE_CURVE('',#3053,#3054,#1934,.T.);
#3923=EDGE_CURVE('',#3053,#3051,#460,.T.);
#3924=EDGE_CURVE('',#3054,#3052,#461,.T.);
#3925=EDGE_CURVE('',#3055,#3056,#1935,.T.);
#3926=EDGE_CURVE('',#3055,#3053,#462,.T.);
#3927=EDGE_CURVE('',#3056,#3054,#463,.T.);
#3928=EDGE_CURVE('',#3057,#3058,#1936,.T.);
#3929=EDGE_CURVE('',#3057,#3055,#464,.T.);
#3930=EDGE_CURVE('',#3058,#3056,#465,.T.);
#3931=EDGE_CURVE('',#3059,#3060,#1937,.T.);
#3932=EDGE_CURVE('',#3059,#3057,#466,.T.);
#3933=EDGE_CURVE('',#3060,#3058,#467,.T.);
#3934=EDGE_CURVE('',#3061,#3062,#1938,.T.);
#3935=EDGE_CURVE('',#3061,#3059,#468,.T.);
#3936=EDGE_CURVE('',#3062,#3060,#469,.T.);
#3937=EDGE_CURVE('',#3063,#3064,#1939,.T.);
#3938=EDGE_CURVE('',#3063,#3061,#470,.T.);
#3939=EDGE_CURVE('',#3064,#3062,#471,.T.);
#3940=EDGE_CURVE('',#3065,#3066,#1940,.T.);
#3941=EDGE_CURVE('',#3065,#3063,#472,.T.);
#3942=EDGE_CURVE('',#3066,#3064,#473,.T.);
#3943=EDGE_CURVE('',#3067,#3068,#1941,.T.);
#3944=EDGE_CURVE('',#3067,#3065,#474,.T.);
#3945=EDGE_CURVE('',#3068,#3066,#475,.T.);
#3946=EDGE_CURVE('',#3069,#3070,#1942,.T.);
#3947=EDGE_CURVE('',#3069,#3067,#476,.T.);
#3948=EDGE_CURVE('',#3070,#3068,#477,.T.);
#3949=EDGE_CURVE('',#3071,#3072,#1943,.T.);
#3950=EDGE_CURVE('',#3071,#3069,#478,.T.);
#3951=EDGE_CURVE('',#3072,#3070,#479,.T.);
#3952=EDGE_CURVE('',#3073,#3074,#1944,.T.);
#3953=EDGE_CURVE('',#3073,#3071,#480,.T.);
#3954=EDGE_CURVE('',#3074,#3072,#481,.T.);
#3955=EDGE_CURVE('',#3075,#3076,#1945,.T.);
#3956=EDGE_CURVE('',#3075,#3073,#482,.T.);
#3957=EDGE_CURVE('',#3076,#3074,#483,.T.);
#3958=EDGE_CURVE('',#3077,#3078,#1946,.T.);
#3959=EDGE_CURVE('',#3077,#3075,#484,.T.);
#3960=EDGE_CURVE('',#3078,#3076,#485,.T.);
#3961=EDGE_CURVE('',#3079,#3080,#1947,.T.);
#3962=EDGE_CURVE('',#3079,#3077,#486,.T.);
#3963=EDGE_CURVE('',#3080,#3078,#487,.T.);
#3964=EDGE_CURVE('',#3081,#3082,#1948,.T.);
#3965=EDGE_CURVE('',#3081,#3079,#488,.T.);
#3966=EDGE_CURVE('',#3082,#3080,#489,.T.);
#3967=EDGE_CURVE('',#3083,#3084,#1949,.T.);
#3968=EDGE_CURVE('',#3083,#3081,#490,.T.);
#3969=EDGE_CURVE('',#3084,#3082,#491,.T.);
#3970=EDGE_CURVE('',#3026,#3085,#492,.T.);
#3971=EDGE_CURVE('',#3086,#3025,#493,.T.);
#3972=EDGE_CURVE('',#3087,#3086,#2539,.T.);
#3973=EDGE_CURVE('',#3085,#3087,#494,.T.);
#3974=EDGE_CURVE('',#3085,#3088,#1950,.T.);
#3975=EDGE_CURVE('',#3088,#3088,#2540,.T.);
#3976=EDGE_CURVE('',#3089,#3083,#495,.T.);
#3977=EDGE_CURVE('',#2963,#3089,#496,.T.);
#3978=EDGE_CURVE('',#3086,#3021,#497,.T.);
#3979=EDGE_CURVE('',#3090,#3084,#498,.T.);
#3980=EDGE_CURVE('',#3089,#3090,#2541,.T.);
#3981=EDGE_CURVE('',#3022,#3087,#499,.T.);
#3982=EDGE_CURVE('',#3090,#2964,#500,.T.);
#3983=EDGE_CURVE('',#3091,#3092,#1951,.T.);
#3984=EDGE_CURVE('',#3091,#3093,#1952,.T.);
#3985=EDGE_CURVE('',#3093,#3094,#1953,.T.);
#3986=EDGE_CURVE('',#3092,#3094,#1954,.T.);
#3987=EDGE_CURVE('',#3095,#3091,#1955,.T.);
#3988=EDGE_CURVE('',#3095,#3096,#1956,.T.);
#3989=EDGE_CURVE('',#3096,#3093,#1957,.T.);
#3990=EDGE_CURVE('',#3097,#3095,#1958,.T.);
#3991=EDGE_CURVE('',#3097,#3098,#1959,.T.);
#3992=EDGE_CURVE('',#3098,#3096,#1960,.T.);
#3993=EDGE_CURVE('',#3099,#3097,#1961,.T.);
#3994=EDGE_CURVE('',#3099,#3100,#1962,.T.);
#3995=EDGE_CURVE('',#3100,#3098,#1963,.T.);
#3996=EDGE_CURVE('',#3101,#3099,#1964,.T.);
#3997=EDGE_CURVE('',#3101,#3102,#1965,.T.);
#3998=EDGE_CURVE('',#3102,#3100,#1966,.T.);
#3999=EDGE_CURVE('',#3092,#3101,#1967,.T.);
#4000=EDGE_CURVE('',#3094,#3102,#1968,.T.);
#4001=EDGE_CURVE('',#3103,#3103,#2542,.T.);
#4002=EDGE_CURVE('',#3103,#3104,#1969,.T.);
#4003=EDGE_CURVE('',#3104,#3104,#2543,.T.);
#5330=ORIENTED_EDGE('',*,*,#3788,.F.);
#5331=ORIENTED_EDGE('',*,*,#3789,.T.);
#5332=ORIENTED_EDGE('',*,*,#3790,.T.);
#5333=ORIENTED_EDGE('',*,*,#3791,.T.);
#5334=ORIENTED_EDGE('',*,*,#3792,.F.);
#5335=ORIENTED_EDGE('',*,*,#3793,.T.);
#5336=ORIENTED_EDGE('',*,*,#3788,.T.);
#5337=ORIENTED_EDGE('',*,*,#3794,.T.);
#5338=ORIENTED_EDGE('',*,*,#3795,.F.);
#5339=ORIENTED_EDGE('',*,*,#3796,.T.);
#5340=ORIENTED_EDGE('',*,*,#3792,.T.);
#5341=ORIENTED_EDGE('',*,*,#3797,.T.);
#5342=ORIENTED_EDGE('',*,*,#3798,.F.);
#5343=ORIENTED_EDGE('',*,*,#3799,.T.);
#5344=ORIENTED_EDGE('',*,*,#3795,.T.);
#5345=ORIENTED_EDGE('',*,*,#3800,.T.);
#5346=ORIENTED_EDGE('',*,*,#3801,.F.);
#5347=ORIENTED_EDGE('',*,*,#3802,.T.);
#5348=ORIENTED_EDGE('',*,*,#3798,.T.);
#5349=ORIENTED_EDGE('',*,*,#3803,.T.);
#5350=ORIENTED_EDGE('',*,*,#3804,.F.);
#5351=ORIENTED_EDGE('',*,*,#3805,.T.);
#5352=ORIENTED_EDGE('',*,*,#3801,.T.);
#5353=ORIENTED_EDGE('',*,*,#3806,.T.);
#5354=ORIENTED_EDGE('',*,*,#3807,.F.);
#5355=ORIENTED_EDGE('',*,*,#3808,.T.);
#5356=ORIENTED_EDGE('',*,*,#3804,.T.);
#5357=ORIENTED_EDGE('',*,*,#3809,.T.);
#5358=ORIENTED_EDGE('',*,*,#3810,.F.);
#5359=ORIENTED_EDGE('',*,*,#3811,.T.);
#5360=ORIENTED_EDGE('',*,*,#3807,.T.);
#5361=ORIENTED_EDGE('',*,*,#3812,.T.);
#5362=ORIENTED_EDGE('',*,*,#3813,.F.);
#5363=ORIENTED_EDGE('',*,*,#3814,.T.);
#5364=ORIENTED_EDGE('',*,*,#3810,.T.);
#5365=ORIENTED_EDGE('',*,*,#3815,.T.);
#5366=ORIENTED_EDGE('',*,*,#3816,.F.);
#5367=ORIENTED_EDGE('',*,*,#3817,.T.);
#5368=ORIENTED_EDGE('',*,*,#3813,.T.);
#5369=ORIENTED_EDGE('',*,*,#3818,.T.);
#5370=ORIENTED_EDGE('',*,*,#3819,.F.);
#5371=ORIENTED_EDGE('',*,*,#3820,.T.);
#5372=ORIENTED_EDGE('',*,*,#3816,.T.);
#5373=ORIENTED_EDGE('',*,*,#3821,.T.);
#5374=ORIENTED_EDGE('',*,*,#3822,.F.);
#5375=ORIENTED_EDGE('',*,*,#3823,.T.);
#5376=ORIENTED_EDGE('',*,*,#3819,.T.);
#5377=ORIENTED_EDGE('',*,*,#3824,.T.);
#5378=ORIENTED_EDGE('',*,*,#3825,.F.);
#5379=ORIENTED_EDGE('',*,*,#3826,.T.);
#5380=ORIENTED_EDGE('',*,*,#3822,.T.);
#5381=ORIENTED_EDGE('',*,*,#3827,.T.);
#5382=ORIENTED_EDGE('',*,*,#3828,.F.);
#5383=ORIENTED_EDGE('',*,*,#3829,.T.);
#5384=ORIENTED_EDGE('',*,*,#3825,.T.);
#5385=ORIENTED_EDGE('',*,*,#3830,.T.);
#5386=ORIENTED_EDGE('',*,*,#3831,.F.);
#5387=ORIENTED_EDGE('',*,*,#3832,.T.);
#5388=ORIENTED_EDGE('',*,*,#3828,.T.);
#5389=ORIENTED_EDGE('',*,*,#3833,.T.);
#5390=ORIENTED_EDGE('',*,*,#3834,.F.);
#5391=ORIENTED_EDGE('',*,*,#3835,.T.);
#5392=ORIENTED_EDGE('',*,*,#3831,.T.);
#5393=ORIENTED_EDGE('',*,*,#3836,.T.);
#5394=ORIENTED_EDGE('',*,*,#3837,.F.);
#5395=ORIENTED_EDGE('',*,*,#3838,.T.);
#5396=ORIENTED_EDGE('',*,*,#3834,.T.);
#5397=ORIENTED_EDGE('',*,*,#3839,.T.);
#5398=ORIENTED_EDGE('',*,*,#3840,.F.);
#5399=ORIENTED_EDGE('',*,*,#3841,.T.);
#5400=ORIENTED_EDGE('',*,*,#3837,.T.);
#5401=ORIENTED_EDGE('',*,*,#3842,.T.);
#5402=ORIENTED_EDGE('',*,*,#3843,.F.);
#5403=ORIENTED_EDGE('',*,*,#3844,.T.);
#5404=ORIENTED_EDGE('',*,*,#3840,.T.);
#5405=ORIENTED_EDGE('',*,*,#3845,.T.);
#5406=ORIENTED_EDGE('',*,*,#3846,.F.);
#5407=ORIENTED_EDGE('',*,*,#3847,.T.);
#5408=ORIENTED_EDGE('',*,*,#3843,.T.);
#5409=ORIENTED_EDGE('',*,*,#3848,.T.);
#5410=ORIENTED_EDGE('',*,*,#3849,.F.);
#5411=ORIENTED_EDGE('',*,*,#3850,.T.);
#5412=ORIENTED_EDGE('',*,*,#3846,.T.);
#5413=ORIENTED_EDGE('',*,*,#3851,.T.);
#5414=ORIENTED_EDGE('',*,*,#3852,.F.);
#5415=ORIENTED_EDGE('',*,*,#3853,.T.);
#5416=ORIENTED_EDGE('',*,*,#3849,.T.);
#5417=ORIENTED_EDGE('',*,*,#3854,.T.);
#5418=ORIENTED_EDGE('',*,*,#3855,.F.);
#5419=ORIENTED_EDGE('',*,*,#3856,.T.);
#5420=ORIENTED_EDGE('',*,*,#3852,.T.);
#5421=ORIENTED_EDGE('',*,*,#3857,.T.);
#5422=ORIENTED_EDGE('',*,*,#3858,.F.);
#5423=ORIENTED_EDGE('',*,*,#3859,.T.);
#5424=ORIENTED_EDGE('',*,*,#3855,.T.);
#5425=ORIENTED_EDGE('',*,*,#3860,.T.);
#5426=ORIENTED_EDGE('',*,*,#3861,.F.);
#5427=ORIENTED_EDGE('',*,*,#3862,.T.);
#5428=ORIENTED_EDGE('',*,*,#3858,.T.);
#5429=ORIENTED_EDGE('',*,*,#3863,.T.);
#5430=ORIENTED_EDGE('',*,*,#3864,.F.);
#5431=ORIENTED_EDGE('',*,*,#3865,.T.);
#5432=ORIENTED_EDGE('',*,*,#3861,.T.);
#5433=ORIENTED_EDGE('',*,*,#3866,.T.);
#5434=ORIENTED_EDGE('',*,*,#3867,.F.);
#5435=ORIENTED_EDGE('',*,*,#3868,.T.);
#5436=ORIENTED_EDGE('',*,*,#3864,.T.);
#5437=ORIENTED_EDGE('',*,*,#3869,.T.);
#5438=ORIENTED_EDGE('',*,*,#3870,.F.);
#5439=ORIENTED_EDGE('',*,*,#3871,.T.);
#5440=ORIENTED_EDGE('',*,*,#3867,.T.);
#5441=ORIENTED_EDGE('',*,*,#3872,.T.);
#5442=ORIENTED_EDGE('',*,*,#3873,.F.);
#5443=ORIENTED_EDGE('',*,*,#3874,.T.);
#5444=ORIENTED_EDGE('',*,*,#3870,.T.);
#5445=ORIENTED_EDGE('',*,*,#3875,.T.);
#5446=ORIENTED_EDGE('',*,*,#3876,.F.);
#5447=ORIENTED_EDGE('',*,*,#3877,.T.);
#5448=ORIENTED_EDGE('',*,*,#3873,.T.);
#5449=ORIENTED_EDGE('',*,*,#3878,.T.);
#5450=ORIENTED_EDGE('',*,*,#3879,.F.);
#5451=ORIENTED_EDGE('',*,*,#3880,.T.);
#5452=ORIENTED_EDGE('',*,*,#3881,.T.);
#5453=ORIENTED_EDGE('',*,*,#3882,.F.);
#5454=ORIENTED_EDGE('',*,*,#3883,.F.);
#5455=ORIENTED_EDGE('',*,*,#3884,.T.);
#5456=ORIENTED_EDGE('',*,*,#3879,.T.);
#5457=ORIENTED_EDGE('',*,*,#3885,.F.);
#5458=ORIENTED_EDGE('',*,*,#3886,.F.);
#5459=ORIENTED_EDGE('',*,*,#3887,.T.);
#5460=ORIENTED_EDGE('',*,*,#3883,.T.);
#5461=ORIENTED_EDGE('',*,*,#3888,.F.);
#5462=ORIENTED_EDGE('',*,*,#3889,.F.);
#5463=ORIENTED_EDGE('',*,*,#3890,.T.);
#5464=ORIENTED_EDGE('',*,*,#3886,.T.);
#5465=ORIENTED_EDGE('',*,*,#3891,.F.);
#5466=ORIENTED_EDGE('',*,*,#3892,.F.);
#5467=ORIENTED_EDGE('',*,*,#3893,.T.);
#5468=ORIENTED_EDGE('',*,*,#3889,.T.);
#5469=ORIENTED_EDGE('',*,*,#3894,.F.);
#5470=ORIENTED_EDGE('',*,*,#3895,.F.);
#5471=ORIENTED_EDGE('',*,*,#3896,.T.);
#5472=ORIENTED_EDGE('',*,*,#3892,.T.);
#5473=ORIENTED_EDGE('',*,*,#3897,.F.);
#5474=ORIENTED_EDGE('',*,*,#3898,.F.);
#5475=ORIENTED_EDGE('',*,*,#3899,.T.);
#5476=ORIENTED_EDGE('',*,*,#3895,.T.);
#5477=ORIENTED_EDGE('',*,*,#3900,.F.);
#5478=ORIENTED_EDGE('',*,*,#3901,.F.);
#5479=ORIENTED_EDGE('',*,*,#3902,.T.);
#5480=ORIENTED_EDGE('',*,*,#3898,.T.);
#5481=ORIENTED_EDGE('',*,*,#3903,.F.);
#5482=ORIENTED_EDGE('',*,*,#3904,.F.);
#5483=ORIENTED_EDGE('',*,*,#3905,.T.);
#5484=ORIENTED_EDGE('',*,*,#3901,.T.);
#5485=ORIENTED_EDGE('',*,*,#3906,.F.);
#5486=ORIENTED_EDGE('',*,*,#3907,.F.);
#5487=ORIENTED_EDGE('',*,*,#3908,.T.);
#5488=ORIENTED_EDGE('',*,*,#3904,.T.);
#5489=ORIENTED_EDGE('',*,*,#3909,.F.);
#5490=ORIENTED_EDGE('',*,*,#3910,.F.);
#5491=ORIENTED_EDGE('',*,*,#3911,.T.);
#5492=ORIENTED_EDGE('',*,*,#3907,.T.);
#5493=ORIENTED_EDGE('',*,*,#3912,.F.);
#5494=ORIENTED_EDGE('',*,*,#3913,.F.);
#5495=ORIENTED_EDGE('',*,*,#3914,.T.);
#5496=ORIENTED_EDGE('',*,*,#3910,.T.);
#5497=ORIENTED_EDGE('',*,*,#3915,.F.);
#5498=ORIENTED_EDGE('',*,*,#3916,.F.);
#5499=ORIENTED_EDGE('',*,*,#3917,.T.);
#5500=ORIENTED_EDGE('',*,*,#3913,.T.);
#5501=ORIENTED_EDGE('',*,*,#3918,.F.);
#5502=ORIENTED_EDGE('',*,*,#3919,.F.);
#5503=ORIENTED_EDGE('',*,*,#3920,.T.);
#5504=ORIENTED_EDGE('',*,*,#3916,.T.);
#5505=ORIENTED_EDGE('',*,*,#3921,.F.);
#5506=ORIENTED_EDGE('',*,*,#3922,.F.);
#5507=ORIENTED_EDGE('',*,*,#3923,.T.);
#5508=ORIENTED_EDGE('',*,*,#3919,.T.);
#5509=ORIENTED_EDGE('',*,*,#3924,.F.);
#5510=ORIENTED_EDGE('',*,*,#3925,.F.);
#5511=ORIENTED_EDGE('',*,*,#3926,.T.);
#5512=ORIENTED_EDGE('',*,*,#3922,.T.);
#5513=ORIENTED_EDGE('',*,*,#3927,.F.);
#5514=ORIENTED_EDGE('',*,*,#3928,.F.);
#5515=ORIENTED_EDGE('',*,*,#3929,.T.);
#5516=ORIENTED_EDGE('',*,*,#3925,.T.);
#5517=ORIENTED_EDGE('',*,*,#3930,.F.);
#5518=ORIENTED_EDGE('',*,*,#3931,.F.);
#5519=ORIENTED_EDGE('',*,*,#3932,.T.);
#5520=ORIENTED_EDGE('',*,*,#3928,.T.);
#5521=ORIENTED_EDGE('',*,*,#3933,.F.);
#5522=ORIENTED_EDGE('',*,*,#3934,.F.);
#5523=ORIENTED_EDGE('',*,*,#3935,.T.);
#5524=ORIENTED_EDGE('',*,*,#3931,.T.);
#5525=ORIENTED_EDGE('',*,*,#3936,.F.);
#5526=ORIENTED_EDGE('',*,*,#3937,.F.);
#5527=ORIENTED_EDGE('',*,*,#3938,.T.);
#5528=ORIENTED_EDGE('',*,*,#3934,.T.);
#5529=ORIENTED_EDGE('',*,*,#3939,.F.);
#5530=ORIENTED_EDGE('',*,*,#3940,.F.);
#5531=ORIENTED_EDGE('',*,*,#3941,.T.);
#5532=ORIENTED_EDGE('',*,*,#3937,.T.);
#5533=ORIENTED_EDGE('',*,*,#3942,.F.);
#5534=ORIENTED_EDGE('',*,*,#3943,.F.);
#5535=ORIENTED_EDGE('',*,*,#3944,.T.);
#5536=ORIENTED_EDGE('',*,*,#3940,.T.);
#5537=ORIENTED_EDGE('',*,*,#3945,.F.);
#5538=ORIENTED_EDGE('',*,*,#3946,.F.);
#5539=ORIENTED_EDGE('',*,*,#3947,.T.);
#5540=ORIENTED_EDGE('',*,*,#3943,.T.);
#5541=ORIENTED_EDGE('',*,*,#3948,.F.);
#5542=ORIENTED_EDGE('',*,*,#3949,.F.);
#5543=ORIENTED_EDGE('',*,*,#3950,.T.);
#5544=ORIENTED_EDGE('',*,*,#3946,.T.);
#5545=ORIENTED_EDGE('',*,*,#3951,.F.);
#5546=ORIENTED_EDGE('',*,*,#3952,.F.);
#5547=ORIENTED_EDGE('',*,*,#3953,.T.);
#5548=ORIENTED_EDGE('',*,*,#3949,.T.);
#5549=ORIENTED_EDGE('',*,*,#3954,.F.);
#5550=ORIENTED_EDGE('',*,*,#3955,.F.);
#5551=ORIENTED_EDGE('',*,*,#3956,.T.);
#5552=ORIENTED_EDGE('',*,*,#3952,.T.);
#5553=ORIENTED_EDGE('',*,*,#3957,.F.);
#5554=ORIENTED_EDGE('',*,*,#3958,.F.);
#5555=ORIENTED_EDGE('',*,*,#3959,.T.);
#5556=ORIENTED_EDGE('',*,*,#3955,.T.);
#5557=ORIENTED_EDGE('',*,*,#3960,.F.);
#5558=ORIENTED_EDGE('',*,*,#3961,.F.);
#5559=ORIENTED_EDGE('',*,*,#3962,.T.);
#5560=ORIENTED_EDGE('',*,*,#3958,.T.);
#5561=ORIENTED_EDGE('',*,*,#3963,.F.);
#5562=ORIENTED_EDGE('',*,*,#3964,.F.);
#5563=ORIENTED_EDGE('',*,*,#3965,.T.);
#5564=ORIENTED_EDGE('',*,*,#3961,.T.);
#5565=ORIENTED_EDGE('',*,*,#3966,.F.);
#5566=ORIENTED_EDGE('',*,*,#3967,.F.);
#5567=ORIENTED_EDGE('',*,*,#3968,.T.);
#5568=ORIENTED_EDGE('',*,*,#3964,.T.);
#5569=ORIENTED_EDGE('',*,*,#3969,.F.);
#5570=ORIENTED_EDGE('',*,*,#3970,.F.);
#5571=ORIENTED_EDGE('',*,*,#3881,.F.);
#5572=ORIENTED_EDGE('',*,*,#3971,.F.);
#5573=ORIENTED_EDGE('',*,*,#3972,.F.);
#5574=ORIENTED_EDGE('',*,*,#3973,.F.);
#5575=ORIENTED_EDGE('',*,*,#3974,.T.);
#5576=ORIENTED_EDGE('',*,*,#3975,.F.);
#5577=ORIENTED_EDGE('',*,*,#3974,.F.);
#5578=ORIENTED_EDGE('',*,*,#3971,.T.);
#5579=ORIENTED_EDGE('',*,*,#3880,.F.);
#5580=ORIENTED_EDGE('',*,*,#3884,.F.);
#5581=ORIENTED_EDGE('',*,*,#3887,.F.);
#5582=ORIENTED_EDGE('',*,*,#3890,.F.);
#5583=ORIENTED_EDGE('',*,*,#3893,.F.);
#5584=ORIENTED_EDGE('',*,*,#3896,.F.);
#5585=ORIENTED_EDGE('',*,*,#3899,.F.);
#5586=ORIENTED_EDGE('',*,*,#3902,.F.);
#5587=ORIENTED_EDGE('',*,*,#3905,.F.);
#5588=ORIENTED_EDGE('',*,*,#3908,.F.);
#5589=ORIENTED_EDGE('',*,*,#3911,.F.);
#5590=ORIENTED_EDGE('',*,*,#3914,.F.);
#5591=ORIENTED_EDGE('',*,*,#3917,.F.);
#5592=ORIENTED_EDGE('',*,*,#3920,.F.);
#5593=ORIENTED_EDGE('',*,*,#3923,.F.);
#5594=ORIENTED_EDGE('',*,*,#3926,.F.);
#5595=ORIENTED_EDGE('',*,*,#3929,.F.);
#5596=ORIENTED_EDGE('',*,*,#3932,.F.);
#5597=ORIENTED_EDGE('',*,*,#3935,.F.);
#5598=ORIENTED_EDGE('',*,*,#3938,.F.);
#5599=ORIENTED_EDGE('',*,*,#3941,.F.);
#5600=ORIENTED_EDGE('',*,*,#3944,.F.);
#5601=ORIENTED_EDGE('',*,*,#3947,.F.);
#5602=ORIENTED_EDGE('',*,*,#3950,.F.);
#5603=ORIENTED_EDGE('',*,*,#3953,.F.);
#5604=ORIENTED_EDGE('',*,*,#3956,.F.);
#5605=ORIENTED_EDGE('',*,*,#3959,.F.);
#5606=ORIENTED_EDGE('',*,*,#3962,.F.);
#5607=ORIENTED_EDGE('',*,*,#3965,.F.);
#5608=ORIENTED_EDGE('',*,*,#3968,.F.);
#5609=ORIENTED_EDGE('',*,*,#3976,.F.);
#5610=ORIENTED_EDGE('',*,*,#3977,.F.);
#5611=ORIENTED_EDGE('',*,*,#3789,.F.);
#5612=ORIENTED_EDGE('',*,*,#3793,.F.);
#5613=ORIENTED_EDGE('',*,*,#3796,.F.);
#5614=ORIENTED_EDGE('',*,*,#3799,.F.);
#5615=ORIENTED_EDGE('',*,*,#3802,.F.);
#5616=ORIENTED_EDGE('',*,*,#3805,.F.);
#5617=ORIENTED_EDGE('',*,*,#3808,.F.);
#5618=ORIENTED_EDGE('',*,*,#3811,.F.);
#5619=ORIENTED_EDGE('',*,*,#3814,.F.);
#5620=ORIENTED_EDGE('',*,*,#3817,.F.);
#5621=ORIENTED_EDGE('',*,*,#3820,.F.);
#5622=ORIENTED_EDGE('',*,*,#3823,.F.);
#5623=ORIENTED_EDGE('',*,*,#3826,.F.);
#5624=ORIENTED_EDGE('',*,*,#3829,.F.);
#5625=ORIENTED_EDGE('',*,*,#3832,.F.);
#5626=ORIENTED_EDGE('',*,*,#3835,.F.);
#5627=ORIENTED_EDGE('',*,*,#3838,.F.);
#5628=ORIENTED_EDGE('',*,*,#3841,.F.);
#5629=ORIENTED_EDGE('',*,*,#3844,.F.);
#5630=ORIENTED_EDGE('',*,*,#3847,.F.);
#5631=ORIENTED_EDGE('',*,*,#3850,.F.);
#5632=ORIENTED_EDGE('',*,*,#3853,.F.);
#5633=ORIENTED_EDGE('',*,*,#3856,.F.);
#5634=ORIENTED_EDGE('',*,*,#3859,.F.);
#5635=ORIENTED_EDGE('',*,*,#3862,.F.);
#5636=ORIENTED_EDGE('',*,*,#3865,.F.);
#5637=ORIENTED_EDGE('',*,*,#3868,.F.);
#5638=ORIENTED_EDGE('',*,*,#3871,.F.);
#5639=ORIENTED_EDGE('',*,*,#3874,.F.);
#5640=ORIENTED_EDGE('',*,*,#3877,.F.);
#5641=ORIENTED_EDGE('',*,*,#3978,.F.);
#5642=ORIENTED_EDGE('',*,*,#3967,.T.);
#5643=ORIENTED_EDGE('',*,*,#3979,.F.);
#5644=ORIENTED_EDGE('',*,*,#3980,.F.);
#5645=ORIENTED_EDGE('',*,*,#3976,.T.);
#5646=ORIENTED_EDGE('',*,*,#3970,.T.);
#5647=ORIENTED_EDGE('',*,*,#3973,.T.);
#5648=ORIENTED_EDGE('',*,*,#3981,.F.);
#5649=ORIENTED_EDGE('',*,*,#3878,.F.);
#5650=ORIENTED_EDGE('',*,*,#3875,.F.);
#5651=ORIENTED_EDGE('',*,*,#3872,.F.);
#5652=ORIENTED_EDGE('',*,*,#3869,.F.);
#5653=ORIENTED_EDGE('',*,*,#3866,.F.);
#5654=ORIENTED_EDGE('',*,*,#3863,.F.);
#5655=ORIENTED_EDGE('',*,*,#3860,.F.);
#5656=ORIENTED_EDGE('',*,*,#3857,.F.);
#5657=ORIENTED_EDGE('',*,*,#3854,.F.);
#5658=ORIENTED_EDGE('',*,*,#3851,.F.);
#5659=ORIENTED_EDGE('',*,*,#3848,.F.);
#5660=ORIENTED_EDGE('',*,*,#3845,.F.);
#5661=ORIENTED_EDGE('',*,*,#3842,.F.);
#5662=ORIENTED_EDGE('',*,*,#3839,.F.);
#5663=ORIENTED_EDGE('',*,*,#3836,.F.);
#5664=ORIENTED_EDGE('',*,*,#3833,.F.);
#5665=ORIENTED_EDGE('',*,*,#3830,.F.);
#5666=ORIENTED_EDGE('',*,*,#3827,.F.);
#5667=ORIENTED_EDGE('',*,*,#3824,.F.);
#5668=ORIENTED_EDGE('',*,*,#3821,.F.);
#5669=ORIENTED_EDGE('',*,*,#3818,.F.);
#5670=ORIENTED_EDGE('',*,*,#3815,.F.);
#5671=ORIENTED_EDGE('',*,*,#3812,.F.);
#5672=ORIENTED_EDGE('',*,*,#3809,.F.);
#5673=ORIENTED_EDGE('',*,*,#3806,.F.);
#5674=ORIENTED_EDGE('',*,*,#3803,.F.);
#5675=ORIENTED_EDGE('',*,*,#3800,.F.);
#5676=ORIENTED_EDGE('',*,*,#3797,.F.);
#5677=ORIENTED_EDGE('',*,*,#3794,.F.);
#5678=ORIENTED_EDGE('',*,*,#3791,.F.);
#5679=ORIENTED_EDGE('',*,*,#3982,.F.);
#5680=ORIENTED_EDGE('',*,*,#3979,.T.);
#5681=ORIENTED_EDGE('',*,*,#3969,.T.);
#5682=ORIENTED_EDGE('',*,*,#3966,.T.);
#5683=ORIENTED_EDGE('',*,*,#3963,.T.);
#5684=ORIENTED_EDGE('',*,*,#3960,.T.);
#5685=ORIENTED_EDGE('',*,*,#3957,.T.);
#5686=ORIENTED_EDGE('',*,*,#3954,.T.);
#5687=ORIENTED_EDGE('',*,*,#3951,.T.);
#5688=ORIENTED_EDGE('',*,*,#3948,.T.);
#5689=ORIENTED_EDGE('',*,*,#3945,.T.);
#5690=ORIENTED_EDGE('',*,*,#3942,.T.);
#5691=ORIENTED_EDGE('',*,*,#3939,.T.);
#5692=ORIENTED_EDGE('',*,*,#3936,.T.);
#5693=ORIENTED_EDGE('',*,*,#3933,.T.);
#5694=ORIENTED_EDGE('',*,*,#3930,.T.);
#5695=ORIENTED_EDGE('',*,*,#3927,.T.);
#5696=ORIENTED_EDGE('',*,*,#3924,.T.);
#5697=ORIENTED_EDGE('',*,*,#3921,.T.);
#5698=ORIENTED_EDGE('',*,*,#3918,.T.);
#5699=ORIENTED_EDGE('',*,*,#3915,.T.);
#5700=ORIENTED_EDGE('',*,*,#3912,.T.);
#5701=ORIENTED_EDGE('',*,*,#3909,.T.);
#5702=ORIENTED_EDGE('',*,*,#3906,.T.);
#5703=ORIENTED_EDGE('',*,*,#3903,.T.);
#5704=ORIENTED_EDGE('',*,*,#3900,.T.);
#5705=ORIENTED_EDGE('',*,*,#3897,.T.);
#5706=ORIENTED_EDGE('',*,*,#3894,.T.);
#5707=ORIENTED_EDGE('',*,*,#3891,.T.);
#5708=ORIENTED_EDGE('',*,*,#3888,.T.);
#5709=ORIENTED_EDGE('',*,*,#3885,.T.);
#5710=ORIENTED_EDGE('',*,*,#3882,.T.);
#5711=ORIENTED_EDGE('',*,*,#3876,.T.);
#5712=ORIENTED_EDGE('',*,*,#3981,.T.);
#5713=ORIENTED_EDGE('',*,*,#3972,.T.);
#5714=ORIENTED_EDGE('',*,*,#3978,.T.);
#5715=ORIENTED_EDGE('',*,*,#3983,.F.);
#5716=ORIENTED_EDGE('',*,*,#3984,.T.);
#5717=ORIENTED_EDGE('',*,*,#3985,.T.);
#5718=ORIENTED_EDGE('',*,*,#3986,.F.);
#5719=ORIENTED_EDGE('',*,*,#3987,.F.);
#5720=ORIENTED_EDGE('',*,*,#3988,.T.);
#5721=ORIENTED_EDGE('',*,*,#3989,.T.);
#5722=ORIENTED_EDGE('',*,*,#3984,.F.);
#5723=ORIENTED_EDGE('',*,*,#3990,.F.);
#5724=ORIENTED_EDGE('',*,*,#3991,.T.);
#5725=ORIENTED_EDGE('',*,*,#3992,.T.);
#5726=ORIENTED_EDGE('',*,*,#3988,.F.);
#5727=ORIENTED_EDGE('',*,*,#3993,.F.);
#5728=ORIENTED_EDGE('',*,*,#3994,.T.);
#5729=ORIENTED_EDGE('',*,*,#3995,.T.);
#5730=ORIENTED_EDGE('',*,*,#3991,.F.);
#5731=ORIENTED_EDGE('',*,*,#3996,.F.);
#5732=ORIENTED_EDGE('',*,*,#3997,.T.);
#5733=ORIENTED_EDGE('',*,*,#3998,.T.);
#5734=ORIENTED_EDGE('',*,*,#3994,.F.);
#5735=ORIENTED_EDGE('',*,*,#3999,.F.);
#5736=ORIENTED_EDGE('',*,*,#3986,.T.);
#5737=ORIENTED_EDGE('',*,*,#4000,.T.);
#5738=ORIENTED_EDGE('',*,*,#3997,.F.);
#5739=ORIENTED_EDGE('',*,*,#4000,.F.);
#5740=ORIENTED_EDGE('',*,*,#3985,.F.);
#5741=ORIENTED_EDGE('',*,*,#3989,.F.);
#5742=ORIENTED_EDGE('',*,*,#3992,.F.);
#5743=ORIENTED_EDGE('',*,*,#3995,.F.);
#5744=ORIENTED_EDGE('',*,*,#3998,.F.);
#5745=ORIENTED_EDGE('',*,*,#4001,.T.);
#5746=ORIENTED_EDGE('',*,*,#3977,.T.);
#5747=ORIENTED_EDGE('',*,*,#3980,.T.);
#5748=ORIENTED_EDGE('',*,*,#3982,.T.);
#5749=ORIENTED_EDGE('',*,*,#3790,.F.);
#5750=ORIENTED_EDGE('',*,*,#4001,.F.);
#5751=ORIENTED_EDGE('',*,*,#4002,.T.);
#5752=ORIENTED_EDGE('',*,*,#4003,.T.);
#5753=ORIENTED_EDGE('',*,*,#4002,.F.);
#5754=ORIENTED_EDGE('',*,*,#4003,.F.);
#5755=ORIENTED_EDGE('',*,*,#3983,.T.);
#5756=ORIENTED_EDGE('',*,*,#3999,.T.);
#5757=ORIENTED_EDGE('',*,*,#3996,.T.);
#5758=ORIENTED_EDGE('',*,*,#3993,.T.);
#5759=ORIENTED_EDGE('',*,*,#3990,.T.);
#5760=ORIENTED_EDGE('',*,*,#3987,.T.);
#5761=ORIENTED_EDGE('',*,*,#3975,.T.);
#6079=CYLINDRICAL_SURFACE('',#6949,0.14635);
#6080=CYLINDRICAL_SURFACE('',#6951,0.14635);
#6081=CYLINDRICAL_SURFACE('',#6952,0.14635);
#6082=CYLINDRICAL_SURFACE('',#6953,0.14635);
#6083=CYLINDRICAL_SURFACE('',#6954,0.14635);
#6084=CYLINDRICAL_SURFACE('',#6955,0.14635);
#6085=CYLINDRICAL_SURFACE('',#6956,0.14635);
#6086=CYLINDRICAL_SURFACE('',#6957,0.14635);
#6087=CYLINDRICAL_SURFACE('',#6958,0.14635);
#6088=CYLINDRICAL_SURFACE('',#6959,0.14635);
#6089=CYLINDRICAL_SURFACE('',#6960,0.14635);
#6090=CYLINDRICAL_SURFACE('',#6961,0.14635);
#6091=CYLINDRICAL_SURFACE('',#6962,0.14635);
#6092=CYLINDRICAL_SURFACE('',#6963,0.14635);
#6093=CYLINDRICAL_SURFACE('',#6964,0.14635);
#6094=CYLINDRICAL_SURFACE('',#6965,0.14635);
#6095=CYLINDRICAL_SURFACE('',#6966,0.14635);
#6096=CYLINDRICAL_SURFACE('',#6967,0.14635);
#6097=CYLINDRICAL_SURFACE('',#6968,0.14635);
#6098=CYLINDRICAL_SURFACE('',#6969,0.14635);
#6099=CYLINDRICAL_SURFACE('',#6970,0.14635);
#6100=CYLINDRICAL_SURFACE('',#6971,0.14635);
#6101=CYLINDRICAL_SURFACE('',#6972,0.14635);
#6102=CYLINDRICAL_SURFACE('',#6973,0.14635);
#6103=CYLINDRICAL_SURFACE('',#6974,0.14635);
#6104=CYLINDRICAL_SURFACE('',#6975,0.14635);
#6105=CYLINDRICAL_SURFACE('',#6976,0.14635);
#6106=CYLINDRICAL_SURFACE('',#6977,0.14635);
#6107=CYLINDRICAL_SURFACE('',#6978,0.14635);
#6108=CYLINDRICAL_SURFACE('',#6979,0.14635);
#6109=CYLINDRICAL_SURFACE('',#6980,0.117775);
#6110=CYLINDRICAL_SURFACE('',#6982,0.117775);
#6111=CYLINDRICAL_SURFACE('',#6983,0.117775);
#6112=CYLINDRICAL_SURFACE('',#6984,0.117775);
#6113=CYLINDRICAL_SURFACE('',#6985,0.117775);
#6114=CYLINDRICAL_SURFACE('',#6986,0.117775);
#6115=CYLINDRICAL_SURFACE('',#6987,0.117775);
#6116=CYLINDRICAL_SURFACE('',#6988,0.117775);
#6117=CYLINDRICAL_SURFACE('',#6989,0.117775);
#6118=CYLINDRICAL_SURFACE('',#6990,0.117775);
#6119=CYLINDRICAL_SURFACE('',#6991,0.117775);
#6120=CYLINDRICAL_SURFACE('',#6992,0.117775);
#6121=CYLINDRICAL_SURFACE('',#6993,0.117775);
#6122=CYLINDRICAL_SURFACE('',#6994,0.117775);
#6123=CYLINDRICAL_SURFACE('',#6995,0.117775);
#6124=CYLINDRICAL_SURFACE('',#6996,0.117775);
#6125=CYLINDRICAL_SURFACE('',#6997,0.117775);
#6126=CYLINDRICAL_SURFACE('',#6998,0.117775);
#6127=CYLINDRICAL_SURFACE('',#6999,0.117775);
#6128=CYLINDRICAL_SURFACE('',#7000,0.117775);
#6129=CYLINDRICAL_SURFACE('',#7001,0.117775);
#6130=CYLINDRICAL_SURFACE('',#7002,0.117775);
#6131=CYLINDRICAL_SURFACE('',#7003,0.117775);
#6132=CYLINDRICAL_SURFACE('',#7004,0.117775);
#6133=CYLINDRICAL_SURFACE('',#7005,0.117775);
#6134=CYLINDRICAL_SURFACE('',#7006,0.117775);
#6135=CYLINDRICAL_SURFACE('',#7007,0.117775);
#6136=CYLINDRICAL_SURFACE('',#7008,0.117775);
#6137=CYLINDRICAL_SURFACE('',#7009,0.117775);
#6138=CYLINDRICAL_SURFACE('',#7010,0.117775);
#6139=CYLINDRICAL_SURFACE('',#7014,0.117775);
#6140=CYLINDRICAL_SURFACE('',#7016,0.14635);
#6141=CYLINDRICAL_SURFACE('',#7026,0.275);
#6406=ADVANCED_FACE('',(#1034),#6079,.T.);
#6407=ADVANCED_FACE('',(#1035),#6080,.T.);
#6408=ADVANCED_FACE('',(#1036),#6081,.T.);
#6409=ADVANCED_FACE('',(#1037),#6082,.T.);
#6410=ADVANCED_FACE('',(#1038),#6083,.T.);
#6411=ADVANCED_FACE('',(#1039),#6084,.T.);
#6412=ADVANCED_FACE('',(#1040),#6085,.T.);
#6413=ADVANCED_FACE('',(#1041),#6086,.T.);
#6414=ADVANCED_FACE('',(#1042),#6087,.T.);
#6415=ADVANCED_FACE('',(#1043),#6088,.T.);
#6416=ADVANCED_FACE('',(#1044),#6089,.T.);
#6417=ADVANCED_FACE('',(#1045),#6090,.T.);
#6418=ADVANCED_FACE('',(#1046),#6091,.T.);
#6419=ADVANCED_FACE('',(#1047),#6092,.T.);
#6420=ADVANCED_FACE('',(#1048),#6093,.T.);
#6421=ADVANCED_FACE('',(#1049),#6094,.T.);
#6422=ADVANCED_FACE('',(#1050),#6095,.T.);
#6423=ADVANCED_FACE('',(#1051),#6096,.T.);
#6424=ADVANCED_FACE('',(#1052),#6097,.T.);
#6425=ADVANCED_FACE('',(#1053),#6098,.T.);
#6426=ADVANCED_FACE('',(#1054),#6099,.T.);
#6427=ADVANCED_FACE('',(#1055),#6100,.T.);
#6428=ADVANCED_FACE('',(#1056),#6101,.T.);
#6429=ADVANCED_FACE('',(#1057),#6102,.T.);
#6430=ADVANCED_FACE('',(#1058),#6103,.T.);
#6431=ADVANCED_FACE('',(#1059),#6104,.T.);
#6432=ADVANCED_FACE('',(#1060),#6105,.T.);
#6433=ADVANCED_FACE('',(#1061),#6106,.T.);
#6434=ADVANCED_FACE('',(#1062),#6107,.T.);
#6435=ADVANCED_FACE('',(#1063),#6108,.T.);
#6436=ADVANCED_FACE('',(#1064),#6109,.T.);
#6437=ADVANCED_FACE('',(#1065),#6110,.T.);
#6438=ADVANCED_FACE('',(#1066),#6111,.T.);
#6439=ADVANCED_FACE('',(#1067),#6112,.T.);
#6440=ADVANCED_FACE('',(#1068),#6113,.T.);
#6441=ADVANCED_FACE('',(#1069),#6114,.T.);
#6442=ADVANCED_FACE('',(#1070),#6115,.T.);
#6443=ADVANCED_FACE('',(#1071),#6116,.T.);
#6444=ADVANCED_FACE('',(#1072),#6117,.T.);
#6445=ADVANCED_FACE('',(#1073),#6118,.T.);
#6446=ADVANCED_FACE('',(#1074),#6119,.T.);
#6447=ADVANCED_FACE('',(#1075),#6120,.T.);
#6448=ADVANCED_FACE('',(#1076),#6121,.T.);
#6449=ADVANCED_FACE('',(#1077),#6122,.T.);
#6450=ADVANCED_FACE('',(#1078),#6123,.T.);
#6451=ADVANCED_FACE('',(#1079),#6124,.T.);
#6452=ADVANCED_FACE('',(#1080),#6125,.T.);
#6453=ADVANCED_FACE('',(#1081),#6126,.T.);
#6454=ADVANCED_FACE('',(#1082),#6127,.T.);
#6455=ADVANCED_FACE('',(#1083),#6128,.T.);
#6456=ADVANCED_FACE('',(#1084),#6129,.T.);
#6457=ADVANCED_FACE('',(#1085),#6130,.T.);
#6458=ADVANCED_FACE('',(#1086),#6131,.T.);
#6459=ADVANCED_FACE('',(#1087),#6132,.T.);
#6460=ADVANCED_FACE('',(#1088),#6133,.T.);
#6461=ADVANCED_FACE('',(#1089),#6134,.T.);
#6462=ADVANCED_FACE('',(#1090),#6135,.T.);
#6463=ADVANCED_FACE('',(#1091),#6136,.T.);
#6464=ADVANCED_FACE('',(#1092),#6137,.T.);
#6465=ADVANCED_FACE('',(#1093),#6138,.T.);
#6466=ADVANCED_FACE('',(#1094),#75,.T.);
#6467=ADVANCED_FACE('',(#1095),#156,.F.);
#6468=ADVANCED_FACE('',(#1096),#6139,.T.);
#6469=ADVANCED_FACE('',(#1097),#157,.F.);
#6470=ADVANCED_FACE('',(#1098),#6140,.T.);
#6471=ADVANCED_FACE('',(#1099),#764,.F.);
#6472=ADVANCED_FACE('',(#1100),#765,.F.);
#6473=ADVANCED_FACE('',(#1101),#766,.F.);
#6474=ADVANCED_FACE('',(#1102),#767,.F.);
#6475=ADVANCED_FACE('',(#1103),#768,.F.);
#6476=ADVANCED_FACE('',(#1104),#769,.F.);
#6477=ADVANCED_FACE('',(#1105),#770,.F.);
#6478=ADVANCED_FACE('',(#1106,#633),#771,.T.);
#6479=ADVANCED_FACE('',(#1107),#6141,.T.);
#6480=ADVANCED_FACE('',(#1108,#634),#772,.F.);
#6481=ADVANCED_FACE('',(#1109),#773,.T.);
#6549=CLOSED_SHELL('',(#6406,#6407,#6408,#6409,#6410,#6411,#6412,#6413,
#6414,#6415,#6416,#6417,#6418,#6419,#6420,#6421,#6422,#6423,#6424,#6425,
#6426,#6427,#6428,#6429,#6430,#6431,#6432,#6433,#6434,#6435,#6436,#6437,
#6438,#6439,#6440,#6441,#6442,#6443,#6444,#6445,#6446,#6447,#6448,#6449,
#6450,#6451,#6452,#6453,#6454,#6455,#6456,#6457,#6458,#6459,#6460,#6461,
#6462,#6463,#6464,#6465,#6466,#6467,#6468,#6469,#6470,#6471,#6472,#6473,
#6474,#6475,#6476,#6477,#6478,#6479,#6480,#6481));
#6948=AXIS2_PLACEMENT_3D('',#12861,#8005,#8006);
#6949=AXIS2_PLACEMENT_3D('',#12862,#8007,#8008);
#6950=AXIS2_PLACEMENT_3D('',#12878,#8010,#8011);
#6951=AXIS2_PLACEMENT_3D('',#12886,#8012,#8013);
#6952=AXIS2_PLACEMENT_3D('',#12934,#8015,#8016);
#6953=AXIS2_PLACEMENT_3D('',#12982,#8018,#8019);
#6954=AXIS2_PLACEMENT_3D('',#13033,#8021,#8022);
#6955=AXIS2_PLACEMENT_3D('',#13081,#8024,#8025);
#6956=AXIS2_PLACEMENT_3D('',#13129,#8027,#8028);
#6957=AXIS2_PLACEMENT_3D('',#13177,#8030,#8031);
#6958=AXIS2_PLACEMENT_3D('',#13231,#8033,#8034);
#6959=AXIS2_PLACEMENT_3D('',#13279,#8036,#8037);
#6960=AXIS2_PLACEMENT_3D('',#13327,#8039,#8040);
#6961=AXIS2_PLACEMENT_3D('',#13381,#8042,#8043);
#6962=AXIS2_PLACEMENT_3D('',#13429,#8045,#8046);
#6963=AXIS2_PLACEMENT_3D('',#13477,#8048,#8049);
#6964=AXIS2_PLACEMENT_3D('',#13525,#8051,#8052);
#6965=AXIS2_PLACEMENT_3D('',#13579,#8054,#8055);
#6966=AXIS2_PLACEMENT_3D('',#13627,#8057,#8058);
#6967=AXIS2_PLACEMENT_3D('',#13675,#8060,#8061);
#6968=AXIS2_PLACEMENT_3D('',#13729,#8063,#8064);
#6969=AXIS2_PLACEMENT_3D('',#13777,#8066,#8067);
#6970=AXIS2_PLACEMENT_3D('',#13825,#8069,#8070);
#6971=AXIS2_PLACEMENT_3D('',#13879,#8072,#8073);
#6972=AXIS2_PLACEMENT_3D('',#13927,#8075,#8076);
#6973=AXIS2_PLACEMENT_3D('',#13975,#8078,#8079);
#6974=AXIS2_PLACEMENT_3D('',#14023,#8081,#8082);
#6975=AXIS2_PLACEMENT_3D('',#14077,#8084,#8085);
#6976=AXIS2_PLACEMENT_3D('',#14125,#8087,#8088);
#6977=AXIS2_PLACEMENT_3D('',#14173,#8090,#8091);
#6978=AXIS2_PLACEMENT_3D('',#14227,#8093,#8094);
#6979=AXIS2_PLACEMENT_3D('',#14275,#8096,#8097);
#6980=AXIS2_PLACEMENT_3D('',#14323,#8099,#8100);
#6981=AXIS2_PLACEMENT_3D('',#14339,#8102,#8103);
#6982=AXIS2_PLACEMENT_3D('',#14349,#8104,#8105);
#6983=AXIS2_PLACEMENT_3D('',#14373,#8107,#8108);
#6984=AXIS2_PLACEMENT_3D('',#14397,#8110,#8111);
#6985=AXIS2_PLACEMENT_3D('',#14422,#8113,#8114);
#6986=AXIS2_PLACEMENT_3D('',#14447,#8116,#8117);
#6987=AXIS2_PLACEMENT_3D('',#14471,#8119,#8120);
#6988=AXIS2_PLACEMENT_3D('',#14496,#8122,#8123);
#6989=AXIS2_PLACEMENT_3D('',#14521,#8125,#8126);
#6990=AXIS2_PLACEMENT_3D('',#14545,#8128,#8129);
#6991=AXIS2_PLACEMENT_3D('',#14569,#8131,#8132);
#6992=AXIS2_PLACEMENT_3D('',#14594,#8134,#8135);
#6993=AXIS2_PLACEMENT_3D('',#14619,#8137,#8138);
#6994=AXIS2_PLACEMENT_3D('',#14643,#8140,#8141);
#6995=AXIS2_PLACEMENT_3D('',#14668,#8143,#8144);
#6996=AXIS2_PLACEMENT_3D('',#14693,#8146,#8147);
#6997=AXIS2_PLACEMENT_3D('',#14717,#8149,#8150);
#6998=AXIS2_PLACEMENT_3D('',#14742,#8152,#8153);
#6999=AXIS2_PLACEMENT_3D('',#14767,#8155,#8156);
#7000=AXIS2_PLACEMENT_3D('',#14791,#8158,#8159);
#7001=AXIS2_PLACEMENT_3D('',#14815,#8161,#8162);
#7002=AXIS2_PLACEMENT_3D('',#14840,#8164,#8165);
#7003=AXIS2_PLACEMENT_3D('',#14865,#8167,#8168);
#7004=AXIS2_PLACEMENT_3D('',#14889,#8170,#8171);
#7005=AXIS2_PLACEMENT_3D('',#14914,#8173,#8174);
#7006=AXIS2_PLACEMENT_3D('',#14939,#8176,#8177);
#7007=AXIS2_PLACEMENT_3D('',#14963,#8179,#8180);
#7008=AXIS2_PLACEMENT_3D('',#14988,#8182,#8183);
#7009=AXIS2_PLACEMENT_3D('',#15012,#8185,#8186);
#7010=AXIS2_PLACEMENT_3D('',#15037,#8188,#8189);
#7011=AXIS2_PLACEMENT_3D('',#15061,#8191,#8192);
#7012=AXIS2_PLACEMENT_3D('',#15223,#8193,#8194);
#7013=AXIS2_PLACEMENT_3D('',#15242,#8196,#8197);
#7014=AXIS2_PLACEMENT_3D('',#16104,#8198,#8199);
#7015=AXIS2_PLACEMENT_3D('',#16115,#8200,#8201);
#7016=AXIS2_PLACEMENT_3D('',#16982,#8202,#8203);
#7017=AXIS2_PLACEMENT_3D('',#16983,#8204,#8205);
#7018=AXIS2_PLACEMENT_3D('',#16992,#8210,#8211);
#7019=AXIS2_PLACEMENT_3D('',#16998,#8215,#8216);
#7020=AXIS2_PLACEMENT_3D('',#17004,#8220,#8221);
#7021=AXIS2_PLACEMENT_3D('',#17010,#8225,#8226);
#7022=AXIS2_PLACEMENT_3D('',#17016,#8230,#8231);
#7023=AXIS2_PLACEMENT_3D('',#17019,#8234,#8235);
#7024=AXIS2_PLACEMENT_3D('',#17020,#8236,#8237);
#7025=AXIS2_PLACEMENT_3D('',#17022,#8238,#8239);
#7026=AXIS2_PLACEMENT_3D('',#17023,#8240,#8241);
#7027=AXIS2_PLACEMENT_3D('',#17026,#8243,#8244);
#7028=AXIS2_PLACEMENT_3D('',#17027,#8245,#8246);
#7029=AXIS2_PLACEMENT_3D('',#17028,#8247,#8248);
#8005=DIRECTION('axis',(0.,0.,1.));
#8006=DIRECTION('refdir',(1.,0.,0.));
#8007=DIRECTION('center_axis',(0.,0.,1.));
#8008=DIRECTION('ref_axis',(1.,0.,0.));
#8009=DIRECTION('',(0.,0.,-1.));
#8010=DIRECTION('center_axis',(0.,0.,-1.));
#8011=DIRECTION('ref_axis',(1.,0.,0.));
#8012=DIRECTION('center_axis',(0.,0.,1.));
#8013=DIRECTION('ref_axis',(1.,0.,0.));
#8014=DIRECTION('',(0.,0.,-1.));
#8015=DIRECTION('center_axis',(0.,0.,1.));
#8016=DIRECTION('ref_axis',(1.,0.,0.));
#8017=DIRECTION('',(0.,0.,-1.));
#8018=DIRECTION('center_axis',(0.,0.,1.));
#8019=DIRECTION('ref_axis',(1.,0.,0.));
#8020=DIRECTION('',(0.,0.,-1.));
#8021=DIRECTION('center_axis',(0.,0.,1.));
#8022=DIRECTION('ref_axis',(1.,0.,0.));
#8023=DIRECTION('',(0.,0.,-1.));
#8024=DIRECTION('center_axis',(0.,0.,1.));
#8025=DIRECTION('ref_axis',(1.,0.,0.));
#8026=DIRECTION('',(0.,0.,-1.));
#8027=DIRECTION('center_axis',(0.,0.,1.));
#8028=DIRECTION('ref_axis',(1.,0.,0.));
#8029=DIRECTION('',(0.,0.,-1.));
#8030=DIRECTION('center_axis',(0.,0.,1.));
#8031=DIRECTION('ref_axis',(1.,0.,0.));
#8032=DIRECTION('',(0.,0.,-1.));
#8033=DIRECTION('center_axis',(0.,0.,1.));
#8034=DIRECTION('ref_axis',(1.,0.,0.));
#8035=DIRECTION('',(0.,0.,-1.));
#8036=DIRECTION('center_axis',(0.,0.,1.));
#8037=DIRECTION('ref_axis',(1.,0.,0.));
#8038=DIRECTION('',(0.,0.,-1.));
#8039=DIRECTION('center_axis',(0.,0.,1.));
#8040=DIRECTION('ref_axis',(1.,0.,0.));
#8041=DIRECTION('',(0.,0.,-1.));
#8042=DIRECTION('center_axis',(0.,0.,1.));
#8043=DIRECTION('ref_axis',(1.,0.,0.));
#8044=DIRECTION('',(0.,0.,-1.));
#8045=DIRECTION('center_axis',(0.,0.,1.));
#8046=DIRECTION('ref_axis',(1.,0.,0.));
#8047=DIRECTION('',(0.,0.,-1.));
#8048=DIRECTION('center_axis',(0.,0.,1.));
#8049=DIRECTION('ref_axis',(1.,0.,0.));
#8050=DIRECTION('',(0.,0.,-1.));
#8051=DIRECTION('center_axis',(0.,0.,1.));
#8052=DIRECTION('ref_axis',(1.,0.,0.));
#8053=DIRECTION('',(0.,0.,-1.));
#8054=DIRECTION('center_axis',(0.,0.,1.));
#8055=DIRECTION('ref_axis',(1.,0.,0.));
#8056=DIRECTION('',(0.,0.,-1.));
#8057=DIRECTION('center_axis',(0.,0.,1.));
#8058=DIRECTION('ref_axis',(1.,0.,0.));
#8059=DIRECTION('',(0.,0.,-1.));
#8060=DIRECTION('center_axis',(0.,0.,1.));
#8061=DIRECTION('ref_axis',(1.,0.,0.));
#8062=DIRECTION('',(0.,0.,-1.));
#8063=DIRECTION('center_axis',(0.,0.,1.));
#8064=DIRECTION('ref_axis',(1.,0.,0.));
#8065=DIRECTION('',(0.,0.,-1.));
#8066=DIRECTION('center_axis',(0.,0.,1.));
#8067=DIRECTION('ref_axis',(1.,0.,0.));
#8068=DIRECTION('',(0.,0.,-1.));
#8069=DIRECTION('center_axis',(0.,0.,1.));
#8070=DIRECTION('ref_axis',(1.,0.,0.));
#8071=DIRECTION('',(0.,0.,-1.));
#8072=DIRECTION('center_axis',(0.,0.,1.));
#8073=DIRECTION('ref_axis',(1.,0.,0.));
#8074=DIRECTION('',(0.,0.,-1.));
#8075=DIRECTION('center_axis',(0.,0.,1.));
#8076=DIRECTION('ref_axis',(1.,0.,0.));
#8077=DIRECTION('',(0.,0.,-1.));
#8078=DIRECTION('center_axis',(0.,0.,1.));
#8079=DIRECTION('ref_axis',(1.,0.,0.));
#8080=DIRECTION('',(0.,0.,-1.));
#8081=DIRECTION('center_axis',(0.,0.,1.));
#8082=DIRECTION('ref_axis',(1.,0.,0.));
#8083=DIRECTION('',(0.,0.,-1.));
#8084=DIRECTION('center_axis',(0.,0.,1.));
#8085=DIRECTION('ref_axis',(1.,0.,0.));
#8086=DIRECTION('',(0.,0.,-1.));
#8087=DIRECTION('center_axis',(0.,0.,1.));
#8088=DIRECTION('ref_axis',(1.,0.,0.));
#8089=DIRECTION('',(0.,0.,-1.));
#8090=DIRECTION('center_axis',(0.,0.,1.));
#8091=DIRECTION('ref_axis',(1.,0.,0.));
#8092=DIRECTION('',(0.,0.,-1.));
#8093=DIRECTION('center_axis',(0.,0.,1.));
#8094=DIRECTION('ref_axis',(1.,0.,0.));
#8095=DIRECTION('',(0.,0.,-1.));
#8096=DIRECTION('center_axis',(0.,0.,1.));
#8097=DIRECTION('ref_axis',(1.,0.,0.));
#8098=DIRECTION('',(0.,0.,-1.));
#8099=DIRECTION('center_axis',(0.,0.,1.));
#8100=DIRECTION('ref_axis',(1.,-2.42503376499884E-13,0.));
#8101=DIRECTION('',(0.,0.,1.));
#8102=DIRECTION('center_axis',(0.,0.,-1.));
#8103=DIRECTION('ref_axis',(1.,-2.42503376499884E-13,0.));
#8104=DIRECTION('center_axis',(0.,0.,1.));
#8105=DIRECTION('ref_axis',(1.,-2.42503376499884E-13,0.));
#8106=DIRECTION('',(0.,0.,1.));
#8107=DIRECTION('center_axis',(0.,0.,1.));
#8108=DIRECTION('ref_axis',(1.,-2.42503376499884E-13,0.));
#8109=DIRECTION('',(0.,0.,1.));
#8110=DIRECTION('center_axis',(0.,0.,1.));
#8111=DIRECTION('ref_axis',(1.,-2.42503376499884E-13,0.));
#8112=DIRECTION('',(0.,0.,1.));
#8113=DIRECTION('center_axis',(0.,0.,1.));
#8114=DIRECTION('ref_axis',(1.,-2.42503376499884E-13,0.));
#8115=DIRECTION('',(0.,0.,1.));
#8116=DIRECTION('center_axis',(0.,0.,1.));
#8117=DIRECTION('ref_axis',(1.,-2.42503376499884E-13,0.));
#8118=DIRECTION('',(0.,0.,1.));
#8119=DIRECTION('center_axis',(0.,0.,1.));
#8120=DIRECTION('ref_axis',(1.,-2.42503376499884E-13,0.));
#8121=DIRECTION('',(0.,0.,1.));
#8122=DIRECTION('center_axis',(0.,0.,1.));
#8123=DIRECTION('ref_axis',(1.,-2.42503376499884E-13,0.));
#8124=DIRECTION('',(0.,0.,1.));
#8125=DIRECTION('center_axis',(0.,0.,1.));
#8126=DIRECTION('ref_axis',(1.,-2.42503376499884E-13,0.));
#8127=DIRECTION('',(0.,0.,1.));
#8128=DIRECTION('center_axis',(0.,0.,1.));
#8129=DIRECTION('ref_axis',(1.,-2.42503376499884E-13,0.));
#8130=DIRECTION('',(0.,0.,1.));
#8131=DIRECTION('center_axis',(0.,0.,1.));
#8132=DIRECTION('ref_axis',(1.,-2.42503376499884E-13,0.));
#8133=DIRECTION('',(0.,0.,1.));
#8134=DIRECTION('center_axis',(0.,0.,1.));
#8135=DIRECTION('ref_axis',(1.,-2.42503376499884E-13,0.));
#8136=DIRECTION('',(0.,0.,1.));
#8137=DIRECTION('center_axis',(0.,0.,1.));
#8138=DIRECTION('ref_axis',(1.,-2.42503376499884E-13,0.));
#8139=DIRECTION('',(0.,0.,1.));
#8140=DIRECTION('center_axis',(0.,0.,1.));
#8141=DIRECTION('ref_axis',(1.,-2.42503376499884E-13,0.));
#8142=DIRECTION('',(0.,0.,1.));
#8143=DIRECTION('center_axis',(0.,0.,1.));
#8144=DIRECTION('ref_axis',(1.,-2.42503376499884E-13,0.));
#8145=DIRECTION('',(0.,0.,1.));
#8146=DIRECTION('center_axis',(0.,0.,1.));
#8147=DIRECTION('ref_axis',(1.,-2.42503376499884E-13,0.));
#8148=DIRECTION('',(0.,0.,1.));
#8149=DIRECTION('center_axis',(0.,0.,1.));
#8150=DIRECTION('ref_axis',(1.,-2.42503376499884E-13,0.));
#8151=DIRECTION('',(0.,0.,1.));
#8152=DIRECTION('center_axis',(0.,0.,1.));
#8153=DIRECTION('ref_axis',(1.,-2.42503376499884E-13,0.));
#8154=DIRECTION('',(0.,0.,1.));
#8155=DIRECTION('center_axis',(0.,0.,1.));
#8156=DIRECTION('ref_axis',(1.,-2.42503376499884E-13,0.));
#8157=DIRECTION('',(0.,0.,1.));
#8158=DIRECTION('center_axis',(0.,0.,1.));
#8159=DIRECTION('ref_axis',(1.,-2.42503376499884E-13,0.));
#8160=DIRECTION('',(0.,0.,1.));
#8161=DIRECTION('center_axis',(0.,0.,1.));
#8162=DIRECTION('ref_axis',(1.,-2.42503376499884E-13,0.));
#8163=DIRECTION('',(0.,0.,1.));
#8164=DIRECTION('center_axis',(0.,0.,1.));
#8165=DIRECTION('ref_axis',(1.,-2.42503376499884E-13,0.));
#8166=DIRECTION('',(0.,0.,1.));
#8167=DIRECTION('center_axis',(0.,0.,1.));
#8168=DIRECTION('ref_axis',(1.,-2.42503376499884E-13,0.));
#8169=DIRECTION('',(0.,0.,1.));
#8170=DIRECTION('center_axis',(0.,0.,1.));
#8171=DIRECTION('ref_axis',(1.,-2.42503376499884E-13,0.));
#8172=DIRECTION('',(0.,0.,1.));
#8173=DIRECTION('center_axis',(0.,0.,1.));
#8174=DIRECTION('ref_axis',(1.,-2.42503376499884E-13,0.));
#8175=DIRECTION('',(0.,0.,1.));
#8176=DIRECTION('center_axis',(0.,0.,1.));
#8177=DIRECTION('ref_axis',(1.,-2.42503376499884E-13,0.));
#8178=DIRECTION('',(0.,0.,1.));
#8179=DIRECTION('center_axis',(0.,0.,1.));
#8180=DIRECTION('ref_axis',(1.,-2.42503376499884E-13,0.));
#8181=DIRECTION('',(0.,0.,1.));
#8182=DIRECTION('center_axis',(0.,0.,1.));
#8183=DIRECTION('ref_axis',(1.,-2.42503376499884E-13,0.));
#8184=DIRECTION('',(0.,0.,1.));
#8185=DIRECTION('center_axis',(0.,0.,1.));
#8186=DIRECTION('ref_axis',(1.,-2.42503376499884E-13,0.));
#8187=DIRECTION('',(0.,0.,1.));
#8188=DIRECTION('center_axis',(0.,0.,1.));
#8189=DIRECTION('ref_axis',(1.,-2.42503376499884E-13,0.));
#8190=DIRECTION('',(0.,0.,1.));
#8191=DIRECTION('center_axis',(0.,0.,-1.));
#8192=DIRECTION('ref_axis',(1.,0.,0.));
#8193=DIRECTION('center_axis',(0.,0.,-1.));
#8194=DIRECTION('ref_axis',(1.,0.,0.));
#8195=DIRECTION('',(0.707106781186547,8.65956056235493E-17,0.707106781186548));
#8196=DIRECTION('center_axis',(0.,0.,1.));
#8197=DIRECTION('ref_axis',(1.,0.,0.));
#8198=DIRECTION('center_axis',(0.,0.,1.));
#8199=DIRECTION('ref_axis',(1.,-2.42503376499884E-13,0.));
#8200=DIRECTION('center_axis',(0.,0.,-1.));
#8201=DIRECTION('ref_axis',(1.,-2.42503376499884E-13,0.));
#8202=DIRECTION('center_axis',(0.,0.,1.));
#8203=DIRECTION('ref_axis',(1.,0.,0.));
#8204=DIRECTION('center_axis',(-1.92296268638356E-16,-1.,0.));
#8205=DIRECTION('ref_axis',(1.,-1.92296268638356E-16,0.));
#8206=DIRECTION('',(1.,-1.92296268638356E-16,0.));
#8207=DIRECTION('',(0.,0.,1.));
#8208=DIRECTION('',(1.,-1.92296268638356E-16,0.));
#8209=DIRECTION('',(0.,0.,1.));
#8210=DIRECTION('center_axis',(-0.866025403784439,-0.5,0.));
#8211=DIRECTION('ref_axis',(0.5,-0.866025403784439,0.));
#8212=DIRECTION('',(0.5,-0.866025403784439,0.));
#8213=DIRECTION('',(0.,0.,1.));
#8214=DIRECTION('',(0.5,-0.866025403784439,0.));
#8215=DIRECTION('center_axis',(-0.866025403784439,0.5,0.));
#8216=DIRECTION('ref_axis',(-0.5,-0.866025403784439,0.));
#8217=DIRECTION('',(-0.5,-0.866025403784439,0.));
#8218=DIRECTION('',(0.,0.,1.));
#8219=DIRECTION('',(-0.5,-0.866025403784438,0.));
#8220=DIRECTION('center_axis',(1.92296268638356E-16,1.,0.));
#8221=DIRECTION('ref_axis',(-1.,1.92296268638356E-16,0.));
#8222=DIRECTION('',(-1.,1.92296268638356E-16,0.));
#8223=DIRECTION('',(0.,0.,1.));
#8224=DIRECTION('',(-1.,1.92296268638356E-16,0.));
#8225=DIRECTION('center_axis',(0.866025403784439,0.5,0.));
#8226=DIRECTION('ref_axis',(-0.5,0.866025403784439,0.));
#8227=DIRECTION('',(-0.5,0.866025403784439,0.));
#8228=DIRECTION('',(0.,0.,1.));
#8229=DIRECTION('',(-0.5,0.866025403784439,0.));
#8230=DIRECTION('center_axis',(0.866025403784439,-0.5,0.));
#8231=DIRECTION('ref_axis',(0.5,0.866025403784439,0.));
#8232=DIRECTION('',(0.5,0.866025403784439,0.));
#8233=DIRECTION('',(0.5,0.866025403784439,0.));
#8234=DIRECTION('center_axis',(0.,0.,1.));
#8235=DIRECTION('ref_axis',(1.,0.,0.));
#8236=DIRECTION('center_axis',(0.,0.,1.));
#8237=DIRECTION('ref_axis',(1.,0.,0.));
#8238=DIRECTION('center_axis',(0.,0.,1.));
#8239=DIRECTION('ref_axis',(1.,0.,0.));
#8240=DIRECTION('center_axis',(0.,0.,1.));
#8241=DIRECTION('ref_axis',(1.,0.,0.));
#8242=DIRECTION('',(0.,0.,-1.));
#8243=DIRECTION('center_axis',(0.,0.,1.));
#8244=DIRECTION('ref_axis',(1.,0.,0.));
#8245=DIRECTION('center_axis',(0.,0.,1.));
#8246=DIRECTION('ref_axis',(1.,0.,0.));
#8247=DIRECTION('center_axis',(0.,0.,1.));
#8248=DIRECTION('ref_axis',(1.,0.,0.));
#12861=CARTESIAN_POINT('',(0.,0.,0.));
#12862=CARTESIAN_POINT('Origin',(0.,0.,0.));
#12863=CARTESIAN_POINT('',(-0.14652705620645,9.44412402177196E-5,0.0160655045842905));
#12864=CARTESIAN_POINT('',(-0.146479946776166,0.000162062070299865,0.00893449541571059));
#12865=CARTESIAN_POINT('',(-0.14635,-1.79227059055215E-17,0.));
#12866=CARTESIAN_POINT('',(0.0634007094575209,0.131904027763685,0.));
#12867=CARTESIAN_POINT('Ctrl Pts',(-0.14652705620645,9.44412402177196E-5,
0.0160655045842905));
#12868=CARTESIAN_POINT('Ctrl Pts',(-0.146560923555419,0.00502618404349199,
0.0157963945919035));
#12869=CARTESIAN_POINT('Ctrl Pts',(-0.146333578783787,0.00995455679532004,
0.0155272845995164));
#12870=CARTESIAN_POINT('Ctrl Pts',(-0.14583475180505,0.0148550342388422,
0.0152581746071293));
#12871=CARTESIAN_POINT('Ctrl Pts',(-0.140929468554047,0.0630445487404258,
0.0126118447280274));
#12872=CARTESIAN_POINT('Ctrl Pts',(-0.10977174472993,0.108536575508351,
0.0099655148489255));
#12873=CARTESIAN_POINT('Ctrl Pts',(-0.0666135938566871,0.13056551637767,
0.00731918496982359));
#12874=CARTESIAN_POINT('Ctrl Pts',(-0.0268248419338395,0.150874636338504,
0.00487945664654906));
#12875=CARTESIAN_POINT('Ctrl Pts',(0.0231637104697219,0.151241233100125,
0.00243972832327453));
#12876=CARTESIAN_POINT('Ctrl Pts',(0.0635546915223951,0.132092229195826,
-2.16840434497101E-19));
#12877=CARTESIAN_POINT('',(-0.0634007094575146,0.131904027763688,0.));
#12878=CARTESIAN_POINT('Origin',(0.,0.,0.));
#12879=CARTESIAN_POINT('Ctrl Pts',(-0.0634007094575145,0.131904027763688,
-3.88578058618805E-16));
#12880=CARTESIAN_POINT('Ctrl Pts',(-0.107282641710421,0.110811831533068,
0.00264738937425961));
#12881=CARTESIAN_POINT('Ctrl Pts',(-0.139432201149969,0.0662847592091173,
0.00529477874851962));
#12882=CARTESIAN_POINT('Ctrl Pts',(-0.145436119191498,0.0182745223106641,
0.00794216812277962));
#12883=CARTESIAN_POINT('Ctrl Pts',(-0.146186273512714,0.0122759249909008,
0.00827294388708994));
#12884=CARTESIAN_POINT('Ctrl Pts',(-0.146528267289359,0.00622295186417552,
0.00860371965140026));
#12885=CARTESIAN_POINT('Ctrl Pts',(-0.146479946776166,0.000162062070299865,
0.00893449541571059));
#12886=CARTESIAN_POINT('Origin',(0.,0.,0.));
#12887=CARTESIAN_POINT('',(-0.146148830924315,7.59978318484386E-5,0.0660655045842905));
#12888=CARTESIAN_POINT('',(-0.146133770585873,6.2751561688711E-5,0.0589344954157103));
#12889=CARTESIAN_POINT('',(-0.14635,-1.79227059055215E-17,0.));
#12890=CARTESIAN_POINT('Ctrl Pts',(-0.146148830924315,7.59978318484386E-5,
0.0660655045842905));
#12891=CARTESIAN_POINT('Ctrl Pts',(-0.146240443598182,0.0195917497831913,
0.0650077071998482));
#12892=CARTESIAN_POINT('Ctrl Pts',(-0.142607114239671,0.0390747476468127,
0.0639499098154059));
#12893=CARTESIAN_POINT('Ctrl Pts',(-0.135087779856993,0.056920264102034,
0.0628921124309636));
#12894=CARTESIAN_POINT('Ctrl Pts',(-0.116276389754784,0.10156503643559,
0.0602457825518617));
#12895=CARTESIAN_POINT('Ctrl Pts',(-0.073143724514267,0.135961331060063,
0.0575994526727599));
#12896=CARTESIAN_POINT('Ctrl Pts',(-0.025432083612881,0.144366623974243,
0.054953122793658));
#12897=CARTESIAN_POINT('Ctrl Pts',(0.0222795572885053,0.152771916888423,
0.0523067929145561));
#12898=CARTESIAN_POINT('Ctrl Pts',(0.0745701738507606,0.135186208092309,
0.0496604630354541));
#12899=CARTESIAN_POINT('Ctrl Pts',(0.107505148494886,0.0996564726649905,
0.0470141331563522));
#12900=CARTESIAN_POINT('Ctrl Pts',(0.140440123139012,0.0641267372376721,
0.0443678032772503));
#12901=CARTESIAN_POINT('Ctrl Pts',(0.154019455865009,0.010652975179149,
0.0417214733981484));
#12902=CARTESIAN_POINT('Ctrl Pts',(0.14202839331759,-0.0362847016460775,
0.0390751435190465));
#12903=CARTESIAN_POINT('Ctrl Pts',(0.130037330770172,-0.0832223784713041,
0.0364288136399446));
#12904=CARTESIAN_POINT('Ctrl Pts',(0.0924758729493388,-0.123623970063234,
0.0337824837608427));
#12905=CARTESIAN_POINT('Ctrl Pts',(0.0465351214488668,-0.139005253038876,
0.0311361538817407));
#12906=CARTESIAN_POINT('Ctrl Pts',(0.000594369948394902,-0.154386536014517,
0.0284898240026388));
#12907=CARTESIAN_POINT('Ctrl Pts',(-0.0537256752317158,-0.144747510373871,
0.025843494123537));
#12908=CARTESIAN_POINT('Ctrl Pts',(-0.0915592764828275,-0.114484496435928,
0.0231971642444351));
#12909=CARTESIAN_POINT('Ctrl Pts',(-0.125545511528741,-0.0872989822136326,
0.0208199443577202));
#12910=CARTESIAN_POINT('Ctrl Pts',(-0.146227884351973,-0.0434707826450544,
0.0184427244710054));
#12911=CARTESIAN_POINT('Ctrl Pts',(-0.14652705620645,9.44412402177196E-5,
0.0160655045842905));
#12912=CARTESIAN_POINT('Ctrl Pts',(-0.146479946776166,0.000162062070299865,
0.00893449541571059));
#12913=CARTESIAN_POINT('Ctrl Pts',(-0.146141530330399,-0.0422858476614564,
0.0112511090256603));
#12914=CARTESIAN_POINT('Ctrl Pts',(-0.126658161292025,-0.0851220706608281,
0.0135677226356099));
#12915=CARTESIAN_POINT('Ctrl Pts',(-0.0941604943243988,-0.112386678841155,
0.0158843362455596));
#12916=CARTESIAN_POINT('Ctrl Pts',(-0.0570226747722624,-0.143544241621566,
0.0185317256198196));
#12917=CARTESIAN_POINT('Ctrl Pts',(-0.00288875902448078,-0.154365965709432,
0.0211791149940796));
#12918=CARTESIAN_POINT('Ctrl Pts',(0.0434083729543798,-0.140002007265973,
0.0238265043683396));
#12919=CARTESIAN_POINT('Ctrl Pts',(0.0897055049332404,-0.125638048822514,
0.0264738937425996));
#12920=CARTESIAN_POINT('Ctrl Pts',(0.12816585314318,-0.0860884078477292,
0.0291212831168596));
#12921=CARTESIAN_POINT('Ctrl Pts',(0.141191617966992,-0.0394144013492358,
0.0317686724911196));
#12922=CARTESIAN_POINT('Ctrl Pts',(0.154217382790803,0.00725960514925768,
0.0344160618653796));
#12923=CARTESIAN_POINT('Ctrl Pts',(0.141808564228487,0.0610579771714599,
0.0370634512396396));
#12924=CARTESIAN_POINT('Ctrl Pts',(0.109639063769471,0.0973098477439542,
0.0397108406138996));
#12925=CARTESIAN_POINT('Ctrl Pts',(0.0774695633104545,0.133561718316448,
0.0423582299881596));
#12926=CARTESIAN_POINT('Ctrl Pts',(0.0255393809547383,0.152267087439235,
0.0450056193624196));
#12927=CARTESIAN_POINT('Ctrl Pts',(-0.0223595433272462,0.144872892294413,
0.0476530087366796));
#12928=CARTESIAN_POINT('Ctrl Pts',(-0.070258467609231,0.137478697149591,
0.0503003981109396));
#12929=CARTESIAN_POINT('Ctrl Pts',(-0.114126133817484,0.10398493773716,
0.0529477874851996));
#12930=CARTESIAN_POINT('Ctrl Pts',(-0.133871661545403,0.059725601630819,
0.0555951768594596));
#12931=CARTESIAN_POINT('Ctrl Pts',(-0.142173753131161,0.0411165744656389,
0.0567082830448765));
#12932=CARTESIAN_POINT('Ctrl Pts',(-0.146211489678532,0.0206043892842972,
0.0578213892302934));
#12933=CARTESIAN_POINT('Ctrl Pts',(-0.146133770585873,6.2751561688711E-5,
0.0589344954157103));
#12934=CARTESIAN_POINT('Origin',(0.,0.,0.));
#12935=CARTESIAN_POINT('',(-0.146252097264499,-0.000124487410312429,0.116065504584291));
#12936=CARTESIAN_POINT('',(-0.146276374479508,-0.000129480650117819,0.10893449541571));
#12937=CARTESIAN_POINT('',(-0.14635,-1.79227059055215E-17,0.));
#12938=CARTESIAN_POINT('Ctrl Pts',(-0.146252097264499,-0.000124487410312429,
0.116065504584291));
#12939=CARTESIAN_POINT('Ctrl Pts',(-0.145977101830714,0.0338815411246725,
0.114219019807793));
#12940=CARTESIAN_POINT('Ctrl Pts',(-0.134160879762789,0.0680598926014691,
0.112372535031295));
#12941=CARTESIAN_POINT('Ctrl Pts',(-0.112484833627769,0.0939988017516943,
0.110526050254798));
#12942=CARTESIAN_POINT('Ctrl Pts',(-0.0814193359437304,0.131173714423195,
0.107879720375696));
#12943=CARTESIAN_POINT('Ctrl Pts',(-0.0301019434218634,0.151424966146533,
0.105233390496594));
#12944=CARTESIAN_POINT('Ctrl Pts',(0.0179785702873004,0.145483266051774,
0.102587060617492));
#12945=CARTESIAN_POINT('Ctrl Pts',(0.0660590839964643,0.139541565957016,
0.0999407307383904));
#12946=CARTESIAN_POINT('Ctrl Pts',(0.110902718892925,0.107406914044162,
0.0972944008592884));
#12947=CARTESIAN_POINT('Ctrl Pts',(0.131983829661647,0.0637877973597534,
0.0946480709801865));
#12948=CARTESIAN_POINT('Ctrl Pts',(0.15306494043037,0.0201686806753445,
0.0920017411010846));
#12949=CARTESIAN_POINT('Ctrl Pts',(0.150383527071356,-0.0349349007806195,
0.0893554112219828));
#12950=CARTESIAN_POINT('Ctrl Pts',(0.125166930059577,-0.0763010783846813,
0.0867090813428809));
#12951=CARTESIAN_POINT('Ctrl Pts',(0.0999503330477985,-0.117667255988743,
0.084062751463779));
#12952=CARTESIAN_POINT('Ctrl Pts',(0.0521985523832557,-0.145296029740903,
0.081416421584677));
#12953=CARTESIAN_POINT('Ctrl Pts',(0.00376830011669856,-0.146541450754272,
0.0787700917055751));
#12954=CARTESIAN_POINT('Ctrl Pts',(-0.0446619521498586,-0.147786871767642,
0.0761237618264732));
#12955=CARTESIAN_POINT('Ctrl Pts',(-0.09377067601843,-0.122648940042221,
0.0734774319473713));
#12956=CARTESIAN_POINT('Ctrl Pts',(-0.121079980470766,-0.0826333491581908,
0.0708311020682694));
#12957=CARTESIAN_POINT('Ctrl Pts',(-0.137473143648068,-0.0586128871159229,
0.0692425695736098));
#12958=CARTESIAN_POINT('Ctrl Pts',(-0.146011252866834,-0.02923151094855,
0.0676540370789502));
#12959=CARTESIAN_POINT('Ctrl Pts',(-0.146148830924315,7.59978318484386E-5,
0.0660655045842905));
#12960=CARTESIAN_POINT('Ctrl Pts',(-0.146133770585873,6.2751561688711E-5,
0.0589344954157103));
#12961=CARTESIAN_POINT('Ctrl Pts',(-0.146026644150963,-0.0282514289199324,
0.0604687786045534));
#12962=CARTESIAN_POINT('Ctrl Pts',(-0.138100435392092,-0.0566215672018456,
0.0620030617933965));
#12963=CARTESIAN_POINT('Ctrl Pts',(-0.122745086057252,-0.0801407530065182,
0.0635373449822396));
#12964=CARTESIAN_POINT('Ctrl Pts',(-0.0962495935935968,-0.120722858737265,
0.0661847343564996));
#12965=CARTESIAN_POINT('Ctrl Pts',(-0.0476352194187008,-0.146862157398507,
0.0688321237307596));
#12966=CARTESIAN_POINT('Ctrl Pts',(0.00082938917649622,-0.146587691816784,
0.0714795131050196));
#12967=CARTESIAN_POINT('Ctrl Pts',(0.0492939977716932,-0.146313226235061,
0.0741269024792796));
#12968=CARTESIAN_POINT('Ctrl Pts',(0.0976088407871913,-0.119624996410372,
0.0767742918535397));
#12969=CARTESIAN_POINT('Ctrl Pts',(0.123643642180798,-0.0787464320231966,
0.0794216812277997));
#12970=CARTESIAN_POINT('Ctrl Pts',(0.149678443574405,-0.0378678676360213,
0.0820690706020596));
#12971=CARTESIAN_POINT('Ctrl Pts',(0.153433203346121,0.0172010313136401,
0.0847164599763195));
#12972=CARTESIAN_POINT('Ctrl Pts',(0.133187835944515,0.06123527443138,0.0873638493505795));
#12973=CARTESIAN_POINT('Ctrl Pts',(0.11294246854291,0.10526951754912,0.0900112387248395));
#12974=CARTESIAN_POINT('Ctrl Pts',(0.0686969739679828,0.138269104834938,
0.0926586280990997));
#12975=CARTESIAN_POINT('Ctrl Pts',(0.0207181735233275,0.145118849380084,
0.0953060174733597));
#12976=CARTESIAN_POINT('Ctrl Pts',(-0.027260626921328,0.151968593925229,
0.0979534068476197));
#12977=CARTESIAN_POINT('Ctrl Pts',(-0.0789727332357116,0.132668495729702,
0.10060079622188));
#12978=CARTESIAN_POINT('Ctrl Pts',(-0.110731403441959,0.0960588230543748,
0.10324818559614));
#12979=CARTESIAN_POINT('Ctrl Pts',(-0.133469481440122,0.0698475998711364,
0.105143622202663));
#12980=CARTESIAN_POINT('Ctrl Pts',(-0.145979327216774,0.0347634013028336,
0.107039058809187));
#12981=CARTESIAN_POINT('Ctrl Pts',(-0.146276374479508,-0.000129480650117819,
0.10893449541571));
#12982=CARTESIAN_POINT('Origin',(0.,0.,0.));
#12983=CARTESIAN_POINT('',(-0.146589818999335,-3.81787486967988E-6,0.166065504584291));
#12984=CARTESIAN_POINT('',(-0.146589453522336,1.04004190909306E-5,0.15893449541571));
#12985=CARTESIAN_POINT('',(-0.14635,-1.79227059055215E-17,0.));
#12986=CARTESIAN_POINT('Ctrl Pts',(-0.146589818999335,-3.81787486967988E-6,
0.166065504584291));
#12987=CARTESIAN_POINT('Ctrl Pts',(-0.146571339149733,0.0482382848470949,
0.163430332415738));
#12988=CARTESIAN_POINT('Ctrl Pts',(-0.120433071521034,0.0964975486977609,
0.160795160247185));
#12989=CARTESIAN_POINT('Ctrl Pts',(-0.0800107885095625,0.122828684230981,
0.158159988078632));
#12990=CARTESIAN_POINT('Ctrl Pts',(-0.0394173515450545,0.149271309704865,
0.15551365819953));
#12991=CARTESIAN_POINT('Ctrl Pts',(0.0155813181737399,0.153599719825856,
0.152867328320428));
#12992=CARTESIAN_POINT('Ctrl Pts',(0.0598114643267532,0.133832733731537,
0.150220998441327));
#12993=CARTESIAN_POINT('Ctrl Pts',(0.104041610479766,0.114065747637217,
0.147574668562225));
#12994=CARTESIAN_POINT('Ctrl Pts',(0.137503233066998,0.0702033653275883,
0.144928338683123));
#12995=CARTESIAN_POINT('Ctrl Pts',(0.144880420813362,0.0223220882221681,
0.142282008804021));
#12996=CARTESIAN_POINT('Ctrl Pts',(0.152257608559726,-0.0255591888832524,
0.139635678924919));
#12997=CARTESIAN_POINT('Ctrl Pts',(0.133550361465222,-0.077459360784464,
0.136989349045817));
#12998=CARTESIAN_POINT('Ctrl Pts',(0.0973212811704284,-0.109622900294719,
0.134343019166715));
#12999=CARTESIAN_POINT('Ctrl Pts',(0.0610922008756344,-0.141786439804975,
0.131696689287613));
#13000=CARTESIAN_POINT('Ctrl Pts',(0.00734128738055008,-0.154213346924274,
0.129050359408511));
#13001=CARTESIAN_POINT('Ctrl Pts',(-0.0393288211819405,-0.141215634503184,
0.126404029529409));
#13002=CARTESIAN_POINT('Ctrl Pts',(-0.0859989297444312,-0.128217922082094,
0.123757699650308));
#13003=CARTESIAN_POINT('Ctrl Pts',(-0.125588233374328,-0.0897955901206149,
0.121111369771206));
#13004=CARTESIAN_POINT('Ctrl Pts',(-0.139976083766172,-0.043535137330043,
0.118465039892104));
#13005=CARTESIAN_POINT('Ctrl Pts',(-0.144324767489921,-0.0295530571287048,
0.117665194789499));
#13006=CARTESIAN_POINT('Ctrl Pts',(-0.146371217526823,-0.0148549394177889,
0.116865349686895));
#13007=CARTESIAN_POINT('Ctrl Pts',(-0.146252097264499,-0.000124487410312429,
0.116065504584291));
#13008=CARTESIAN_POINT('Ctrl Pts',(-0.146276374479508,-0.000129480650117819,
0.10893449541571));
#13009=CARTESIAN_POINT('Ctrl Pts',(-0.14639421831063,-0.0139720956278579,
0.109686448183447));
#13010=CARTESIAN_POINT('Ctrl Pts',(-0.14458995413065,-0.0277846002915201,
0.110438400951183));
#13011=CARTESIAN_POINT('Ctrl Pts',(-0.140739671041232,-0.041001045008257,
0.11119035371892));
#13012=CARTESIAN_POINT('Ctrl Pts',(-0.127184034336146,-0.0875319932404337,
0.11383774309318));
#13013=CARTESIAN_POINT('Ctrl Pts',(-0.0882675268278623,-0.12667464254966,
0.11648513246744));
#13014=CARTESIAN_POINT('Ctrl Pts',(-0.0418159243469935,-0.140499695546946,
0.1191325218417));
#13015=CARTESIAN_POINT('Ctrl Pts',(0.00463567813387508,-0.154324748544231,
0.12177991121596));
#13016=CARTESIAN_POINT('Ctrl Pts',(0.0586223755873289,-0.142832205229577,
0.12442730059022));
#13017=CARTESIAN_POINT('Ctrl Pts',(0.0954154960694136,-0.111286216216264,
0.12707468996448));
#13018=CARTESIAN_POINT('Ctrl Pts',(0.132208616551499,-0.0797402272029501,
0.12972207933874));
#13019=CARTESIAN_POINT('Ctrl Pts',(0.151808160062214,-0.0281407924909768,
0.132369468712999));
#13020=CARTESIAN_POINT('Ctrl Pts',(0.145236524363737,0.0198768833792122,
0.135016858087259));
#13021=CARTESIAN_POINT('Ctrl Pts',(0.138664888665259,0.0678945592494009,
0.13766424746152));
#13022=CARTESIAN_POINT('Ctrl Pts',(0.105922073757589,0.112330476277805,
0.14031163683578));
#13023=CARTESIAN_POINT('Ctrl Pts',(0.062005973158836,0.132830708741579,
0.14295902621004));
#13024=CARTESIAN_POINT('Ctrl Pts',(0.0180898725600832,0.153330941205352,
0.1456064155843));
#13025=CARTESIAN_POINT('Ctrl Pts',(-0.0369995137297515,0.149895489104495,
0.14825380495856));
#13026=CARTESIAN_POINT('Ctrl Pts',(-0.0780284182758478,0.124097962381086,
0.15090119433282));
#13027=CARTESIAN_POINT('Ctrl Pts',(-0.119057322821944,0.0983004356576776,
0.153548583707079));
#13028=CARTESIAN_POINT('Ctrl Pts',(-0.146025745624302,0.0501408343117172,
0.15619597308134));
#13029=CARTESIAN_POINT('Ctrl Pts',(-0.14658076309025,0.00167873146180186,
0.1588433624556));
#13030=CARTESIAN_POINT('Ctrl Pts',(-0.146587131676737,0.00112264969450139,
0.15887374010897));
#13031=CARTESIAN_POINT('Ctrl Pts',(-0.146590022522527,0.000566528098114988,
0.15890411776234));
#13032=CARTESIAN_POINT('Ctrl Pts',(-0.146589453522336,1.04004190909306E-5,
0.15893449541571));
#13033=CARTESIAN_POINT('Origin',(0.,0.,0.));
#13034=CARTESIAN_POINT('',(-0.146263250741535,0.000126870157254357,0.21606550458429));
#13035=CARTESIAN_POINT('',(-0.146245769975643,0.000123264779366826,0.20893449541571));
#13036=CARTESIAN_POINT('',(-0.14635,-1.79227059055215E-17,0.));
#13037=CARTESIAN_POINT('Ctrl Pts',(-0.146263250741535,0.000126870157254357,
0.21606550458429));
#13038=CARTESIAN_POINT('Ctrl Pts',(-0.146381923100139,0.0144435832128767,
0.215287974902784));
#13039=CARTESIAN_POINT('Ctrl Pts',(-0.144450237714319,0.0287289633064517,
0.214510445221278));
#13040=CARTESIAN_POINT('Ctrl Pts',(-0.140337374518256,0.0423560295890773,
0.213732915539772));
#13041=CARTESIAN_POINT('Ctrl Pts',(-0.126339204386259,0.0887358830222778,
0.21108658566067));
#13042=CARTESIAN_POINT('Ctrl Pts',(-0.0870745347363382,0.127489909020004,
0.208440255781569));
#13043=CARTESIAN_POINT('Ctrl Pts',(-0.0405154226099946,0.140879780169064,
0.205793925902467));
#13044=CARTESIAN_POINT('Ctrl Pts',(0.00604368951634975,0.154269651318124,
0.203147596023365));
#13045=CARTESIAN_POINT('Ctrl Pts',(0.0598972441191175,0.142295367618517,
0.200501266144263));
#13046=CARTESIAN_POINT('Ctrl Pts',(0.0963956219934077,0.110437747119808,
0.197854936265161));
#13047=CARTESIAN_POINT('Ctrl Pts',(0.132893999867697,0.0785801266211,0.195208606386059));
#13048=CARTESIAN_POINT('Ctrl Pts',(0.15203720101351,0.0268391693232909,
0.192562276506957));
#13049=CARTESIAN_POINT('Ctrl Pts',(0.145063081087281,-0.0211024746124516,
0.189915946627855));
#13050=CARTESIAN_POINT('Ctrl Pts',(0.138088961161051,-0.0690441185481943,
0.187269616748753));
#13051=CARTESIAN_POINT('Ctrl Pts',(0.10499752016278,-0.11318644912187,0.184623286869651));
#13052=CARTESIAN_POINT('Ctrl Pts',(0.060935231264163,-0.133324827106958,
0.181976956990549));
#13053=CARTESIAN_POINT('Ctrl Pts',(0.0168729423655461,-0.153463205092045,
0.179330627111448));
#13054=CARTESIAN_POINT('Ctrl Pts',(-0.0381601944334158,-0.149597630488544,
0.176684297232346));
#13055=CARTESIAN_POINT('Ctrl Pts',(-0.0789746466099193,-0.123497437688695,
0.174037967353244));
#13056=CARTESIAN_POINT('Ctrl Pts',(-0.119961184605052,-0.0972871987457574,
0.171380479763593));
#13057=CARTESIAN_POINT('Ctrl Pts',(-0.146608455341797,-0.0486544490602708,
0.168722992173942));
#13058=CARTESIAN_POINT('Ctrl Pts',(-0.146589818999335,-3.81787486967988E-6,
0.166065504584291));
#13059=CARTESIAN_POINT('Ctrl Pts',(-0.146589453522336,1.04004190909306E-5,
0.15893449541571));
#13060=CARTESIAN_POINT('Ctrl Pts',(-0.146540434588914,-0.0478995759235739,
0.1615515071366));
#13061=CARTESIAN_POINT('Ctrl Pts',(-0.120813506558866,-0.0958546957256878,
0.16416851885749));
#13062=CARTESIAN_POINT('Ctrl Pts',(-0.0808500697395765,-0.122278388912248,
0.16678553057838));
#13063=CARTESIAN_POINT('Ctrl Pts',(-0.0404227467934142,-0.149008802082514,
0.16943291995264));
#13064=CARTESIAN_POINT('Ctrl Pts',(0.0145735112284506,-0.153705024069172,
0.1720803093269));
#13065=CARTESIAN_POINT('Ctrl Pts',(0.0589475933459444,-0.134215943447351,
0.17472769870116));
#13066=CARTESIAN_POINT('Ctrl Pts',(0.103321675463438,-0.11472686282553,
0.17737508807542));
#13067=CARTESIAN_POINT('Ctrl Pts',(0.137073581676561,-0.0710524795952304,
0.18002247744968));
#13068=CARTESIAN_POINT('Ctrl Pts',(0.144743205110219,-0.0231979049720499,
0.18266986682394));
#13069=CARTESIAN_POINT('Ctrl Pts',(0.152412828543877,0.024656669651131,
0.1853172561982));
#13070=CARTESIAN_POINT('Ctrl Pts',(0.13400016919807,0.0766914356671922,
0.18796464557246));
#13071=CARTESIAN_POINT('Ctrl Pts',(0.0979391709064228,0.109071797518936,
0.19061203494672));
#13072=CARTESIAN_POINT('Ctrl Pts',(0.0618781726147763,0.141452159370678,
0.19325942432098));
#13073=CARTESIAN_POINT('Ctrl Pts',(0.00816883537729064,0.154178117058104,
0.195906813695239));
#13074=CARTESIAN_POINT('Ctrl Pts',(-0.0385872054932313,0.1414205281901,
0.198554203069499));
#13075=CARTESIAN_POINT('Ctrl Pts',(-0.0853432463637543,0.128662939322095,
0.201201592443759));
#13076=CARTESIAN_POINT('Ctrl Pts',(-0.125145990867313,0.0904218038986596,
0.20384898181802));
#13077=CARTESIAN_POINT('Ctrl Pts',(-0.139763737461459,0.0442135263146365,
0.20649637119228));
#13078=CARTESIAN_POINT('Ctrl Pts',(-0.144251162244238,0.030028291356252,
0.207309079266757));
#13079=CARTESIAN_POINT('Ctrl Pts',(-0.146365162502875,0.0150922359825044,
0.208121787341234));
#13080=CARTESIAN_POINT('Ctrl Pts',(-0.146245769975643,0.000123264779366826,
0.20893449541571));
#13081=CARTESIAN_POINT('Origin',(0.,0.,0.));
#13082=CARTESIAN_POINT('',(-0.146142672279203,-7.01165389862951E-5,0.266065504584291));
#13083=CARTESIAN_POINT('',(-0.146150215784492,-7.74481165901552E-5,0.258934495415711));
#13084=CARTESIAN_POINT('',(-0.14635,-1.79227059055215E-17,0.));
#13085=CARTESIAN_POINT('Ctrl Pts',(-0.146142672279203,-7.01165389862951E-5,
0.266065504584291));
#13086=CARTESIAN_POINT('Ctrl Pts',(-0.146017527260215,0.028828671850369,
0.264499287510729));
#13087=CARTESIAN_POINT('Ctrl Pts',(-0.137733916992107,0.0577936173630845,
0.262933070437168));
#13088=CARTESIAN_POINT('Ctrl Pts',(-0.121770841384076,0.0816117278206753,
0.261366853363607));
#13089=CARTESIAN_POINT('Ctrl Pts',(-0.0947991242083451,0.121855560193383,
0.258720523484505));
#13090=CARTESIAN_POINT('Ctrl Pts',(-0.0459036471244643,0.147405924851771,
0.256074193605403));
#13091=CARTESIAN_POINT('Ctrl Pts',(0.0025353607453442,0.146568017913755,
0.253427863726301));
#13092=CARTESIAN_POINT('Ctrl Pts',(0.050974368615152,0.145730110975738,
0.250781533847199));
#13093=CARTESIAN_POINT('Ctrl Pts',(0.0989569072708876,0.118503932441319,
0.248135203968097));
#13094=CARTESIAN_POINT('Ctrl Pts',(0.124520613871998,0.0773513325689396,
0.245488874088995));
#13095=CARTESIAN_POINT('Ctrl Pts',(0.150084320473109,0.0361987326965595,
0.242842544209893));
#13096=CARTESIAN_POINT('Ctrl Pts',(0.153229195019594,-0.0188802885137813,
0.240196214330791));
#13097=CARTESIAN_POINT('Ctrl Pts',(0.132515778953886,-0.0626751965094481,
0.237549884451689));
#13098=CARTESIAN_POINT('Ctrl Pts',(0.111802362888177,-0.106470104505115,
0.234903554572587));
#13099=CARTESIAN_POINT('Ctrl Pts',(0.0672306562102751,-0.138980899286108,
0.232257224693486));
#13100=CARTESIAN_POINT('Ctrl Pts',(0.0192018303028616,-0.145326878595667,
0.229610894814384));
#13101=CARTESIAN_POINT('Ctrl Pts',(-0.0288269956045516,-0.151672857905225,
0.226964564935282));
#13102=CARTESIAN_POINT('Ctrl Pts',(-0.0803129407414762,-0.131854021743351,
0.22431823505618));
#13103=CARTESIAN_POINT('Ctrl Pts',(-0.111690078002902,-0.0949417632280756,
0.221671905177078));
#13104=CARTESIAN_POINT('Ctrl Pts',(-0.133848162215005,-0.0688748557907962,
0.219803104979482));
#13105=CARTESIAN_POINT('Ctrl Pts',(-0.145978020566425,-0.0342834897603843,
0.217934304781886));
#13106=CARTESIAN_POINT('Ctrl Pts',(-0.146263250741535,0.000126870157254357,
0.21606550458429));
#13107=CARTESIAN_POINT('Ctrl Pts',(-0.146245769975643,0.000123264779366826,
0.20893449541571));
#13108=CARTESIAN_POINT('Ctrl Pts',(-0.145976242399967,-0.03366905549635,
0.210769176715493));
#13109=CARTESIAN_POINT('Ctrl Pts',(-0.134324750276972,-0.067629123606452,
0.212603858015276));
#13110=CARTESIAN_POINT('Ctrl Pts',(-0.112902327433,-0.0934976078712483,
0.214438539315059));
#13111=CARTESIAN_POINT('Ctrl Pts',(-0.0819904221256615,-0.130825044728502,
0.217085928689319));
#13112=CARTESIAN_POINT('Ctrl Pts',(-0.0307338628262512,-0.151304498698398,
0.21973331806358));
#13113=CARTESIAN_POINT('Ctrl Pts',(0.0173892134168267,-0.145555327884408,
0.22238070743784));
#13114=CARTESIAN_POINT('Ctrl Pts',(0.0655122896599044,-0.139806157070418,
0.2250280968121));
#13115=CARTESIAN_POINT('Ctrl Pts',(0.11050188284665,-0.107828361472542,
0.22767548618636));
#13116=CARTESIAN_POINT('Ctrl Pts',(0.131750448317205,-0.0642694140823833,
0.23032287556062));
#13117=CARTESIAN_POINT('Ctrl Pts',(0.15299901378776,-0.020710466692225,
0.232970264934879));
#13118=CARTESIAN_POINT('Ctrl Pts',(0.150506551542124,0.0344296324902152,
0.23561765430914));
#13119=CARTESIAN_POINT('Ctrl Pts',(0.125414737320077,0.0758938856636754,
0.2382650436834));
#13120=CARTESIAN_POINT('Ctrl Pts',(0.10032292309803,0.117358138837136,0.24091243305766));
#13121=CARTESIAN_POINT('Ctrl Pts',(0.0526317568995709,0.145146546001616,
0.24355982243192));
#13122=CARTESIAN_POINT('Ctrl Pts',(0.00418624259284972,0.146530589268381,
0.24620721180618));
#13123=CARTESIAN_POINT('Ctrl Pts',(-0.0442592717138715,0.147914632535146,
0.24885460118044));
#13124=CARTESIAN_POINT('Ctrl Pts',(-0.0934591341288551,0.122894311904195,
0.2515019905547));
#13125=CARTESIAN_POINT('Ctrl Pts',(-0.120877280418781,0.082930219442967,
0.25414937992896));
#13126=CARTESIAN_POINT('Ctrl Pts',(-0.137396572682769,0.0588520590724165,
0.255744418424543));
#13127=CARTESIAN_POINT('Ctrl Pts',(-0.146009100715185,0.0293493086505574,
0.257339456920127));
#13128=CARTESIAN_POINT('Ctrl Pts',(-0.146150215784492,-7.74481165901552E-5,
0.258934495415711));
#13129=CARTESIAN_POINT('Origin',(0.,0.,0.));
#13130=CARTESIAN_POINT('',(-0.146519404976022,-8.97763884284003E-5,0.316065504584291));
#13131=CARTESIAN_POINT('',(-0.146528765763263,-8.45393868379275E-5,0.30893449541571));
#13132=CARTESIAN_POINT('',(-0.14635,-1.79227059055215E-17,0.));
#13133=CARTESIAN_POINT('Ctrl Pts',(-0.146519404976022,-8.97763884284003E-5,
0.316065504584291));
#13134=CARTESIAN_POINT('Ctrl Pts',(-0.146208092107557,0.043076445171776,
0.313710600118674));
#13135=CARTESIAN_POINT('Ctrl Pts',(-0.125958424314353,0.0864965766126209,
0.311355695653057));
#13136=CARTESIAN_POINT('Ctrl Pts',(-0.0925183485457987,0.1137056160074,
0.309000791187441));
#13137=CARTESIAN_POINT('Ctrl Pts',(-0.0549399784004991,0.144281843189175,
0.306354461308339));
#13138=CARTESIAN_POINT('Ctrl Pts',(-0.00070450021881692,0.154386382754941,
0.303708131429237));
#13139=CARTESIAN_POINT('Ctrl Pts',(0.0453636543616171,0.139394227973128,
0.301061801550135));
#13140=CARTESIAN_POINT('Ctrl Pts',(0.0914318089420511,0.124402073191315,
0.298415471671033));
#13141=CARTESIAN_POINT('Ctrl Pts',(0.129332639921237,0.0843132240619223,
0.295769141791931));
#13142=CARTESIAN_POINT('Ctrl Pts',(0.141718340675246,0.0374769775398043,
0.293122811912829));
#13143=CARTESIAN_POINT('Ctrl Pts',(0.154104041429255,-0.00935926898231351,
0.290476482033727));
#13144=CARTESIAN_POINT('Ctrl Pts',(0.140974611958088,-0.0629429128971569,
0.287830152154626));
#13145=CARTESIAN_POINT('Ctrl Pts',(0.108339598692885,-0.0987478773661917,
0.285183822275524));
#13146=CARTESIAN_POINT('Ctrl Pts',(0.0757045854276824,-0.134552841835227,
0.282537492396422));
#13147=CARTESIAN_POINT('Ctrl Pts',(0.0235639883684441,-0.152579126858453,
0.27989116251732));
#13148=CARTESIAN_POINT('Ctrl Pts',(-0.0242166208952047,-0.144575818177467,
0.277244832638218));
#13149=CARTESIAN_POINT('Ctrl Pts',(-0.0719972301588528,-0.136572509496481,
0.274598502759116));
#13150=CARTESIAN_POINT('Ctrl Pts',(-0.115417851626912,-0.102539607111283,
0.271952172880014));
#13151=CARTESIAN_POINT('Ctrl Pts',(-0.13460418372715,-0.0580545058751705,
0.269305843000912));
#13152=CARTESIAN_POINT('Ctrl Pts',(-0.142435181350113,-0.0398976888130428,
0.268225730195372));
#13153=CARTESIAN_POINT('Ctrl Pts',(-0.146228976240411,-0.0199996345674016,
0.267145617389831));
#13154=CARTESIAN_POINT('Ctrl Pts',(-0.146142672279203,-7.01165389862951E-5,
0.266065504584291));
#13155=CARTESIAN_POINT('Ctrl Pts',(-0.146150215784492,-7.74481165901552E-5,
0.258934495415711));
#13156=CARTESIAN_POINT('Ctrl Pts',(-0.146243318595233,-0.0194921979337541,
0.259986846294387));
#13157=CARTESIAN_POINT('Ctrl Pts',(-0.142648899141753,-0.0388738684647463,
0.261039197173063));
#13158=CARTESIAN_POINT('Ctrl Pts',(-0.135204796371803,-0.0566427511368837,
0.26209154805174));
#13159=CARTESIAN_POINT('Ctrl Pts',(-0.116477735870028,-0.101343764964001,
0.264738937426));
#13160=CARTESIAN_POINT('Ctrl Pts',(-0.0733871847016099,-0.135837928326728,
0.26738632680026));
#13161=CARTESIAN_POINT('Ctrl Pts',(-0.0256708287318585,-0.144325142544676,
0.27003371617452));
#13162=CARTESIAN_POINT('Ctrl Pts',(0.0220455272378925,-0.152812356762624,
0.27268110554878));
#13163=CARTESIAN_POINT('Ctrl Pts',(0.0743876880089763,-0.135292621835792,
0.27532849492304));
#13164=CARTESIAN_POINT('Ctrl Pts',(0.10738025529095,-0.0997908762961729,
0.2779758842973));
#13165=CARTESIAN_POINT('Ctrl Pts',(0.140372822572925,-0.0642891307565533,
0.280623273671559));
#13166=CARTESIAN_POINT('Ctrl Pts',(0.154015796365789,-0.010805374604146,
0.283270663045819));
#13167=CARTESIAN_POINT('Ctrl Pts',(0.142059993874458,0.0361620845457957,
0.285918052420079));
#13168=CARTESIAN_POINT('Ctrl Pts',(0.130104191383128,0.0831295436957373,
0.288565441794339));
#13169=CARTESIAN_POINT('Ctrl Pts',(0.0925496126076039,0.123580705843213,
0.291212831168599));
#13170=CARTESIAN_POINT('Ctrl Pts',(0.0465981836912963,0.138986860871753,
0.29386022054286));
#13171=CARTESIAN_POINT('Ctrl Pts',(0.000646754774988913,0.154393015900293,
0.296507609917119));
#13172=CARTESIAN_POINT('Ctrl Pts',(-0.0537015242821025,0.144754163809898,
0.29915499929138));
#13173=CARTESIAN_POINT('Ctrl Pts',(-0.0915523499663989,0.114485393976436,
0.30180238866564));
#13174=CARTESIAN_POINT('Ctrl Pts',(-0.125542580994678,0.0873038870745135,
0.30417975758233));
#13175=CARTESIAN_POINT('Ctrl Pts',(-0.146229051243382,0.0434861464246214,
0.30655712649902));
#13176=CARTESIAN_POINT('Ctrl Pts',(-0.146528765763263,-8.45393868379275E-5,
0.30893449541571));
#13177=CARTESIAN_POINT('Origin',(0.,0.,0.));
#13178=CARTESIAN_POINT('',(-0.146416087288192,0.000126442170093593,0.366065504584291));
#13179=CARTESIAN_POINT('',(-0.146408012399712,0.000128195943346294,0.358934495415711));
#13180=CARTESIAN_POINT('',(-0.14635,-1.79227059055215E-17,0.));
#13181=CARTESIAN_POINT('Ctrl Pts',(-0.146416087288192,0.000126442170093593,
0.366065504584291));
#13182=CARTESIAN_POINT('Ctrl Pts',(-0.146499294961499,0.00925816812376314,
0.365568242605721));
#13183=CARTESIAN_POINT('Ctrl Pts',(-0.145718277739785,0.0183757049974218,
0.365070980627151));
#13184=CARTESIAN_POINT('Ctrl Pts',(-0.144021710151773,0.0273195705351122,
0.364573718648581));
#13185=CARTESIAN_POINT('Ctrl Pts',(-0.134992913071845,0.0749170536065741,
0.361927388769479));
#13186=CARTESIAN_POINT('Ctrl Pts',(-0.100034284522917,0.117595890322328,
0.359281058890377));
#13187=CARTESIAN_POINT('Ctrl Pts',(-0.0551469387876206,0.135821305661589,
0.356634729011275));
#13188=CARTESIAN_POINT('Ctrl Pts',(-0.0102595930523245,0.15404672100085,
0.353988399132173));
#13189=CARTESIAN_POINT('Ctrl Pts',(0.0445564698693406,0.147818714963618,
0.351342069253072));
#13190=CARTESIAN_POINT('Ctrl Pts',(0.0842110755700531,0.119987943896873,
0.34869573937397));
#13191=CARTESIAN_POINT('Ctrl Pts',(0.123865681270766,0.0921571728301272,
0.346049409494868));
#13192=CARTESIAN_POINT('Ctrl Pts',(0.148358829750526,0.0427236367338667,
0.343403079615766));
#13193=CARTESIAN_POINT('Ctrl Pts',(0.146479621605269,-0.00568615719458776,
0.340756749736664));
#13194=CARTESIAN_POINT('Ctrl Pts',(0.144600413460012,-0.0540959511230416,
0.338110419857562));
#13195=CARTESIAN_POINT('Ctrl Pts',(0.116348848689739,-0.101482002883689,
0.33546408997846));
#13196=CARTESIAN_POINT('Ctrl Pts',(0.0746561129649502,-0.126154971072205,
0.332817760099358));
#13197=CARTESIAN_POINT('Ctrl Pts',(0.0329633772401616,-0.150827939260721,
0.330171430220256));
#13198=CARTESIAN_POINT('Ctrl Pts',(-0.0221705294391424,-0.152787823877104,
0.327525100341154));
#13199=CARTESIAN_POINT('Ctrl Pts',(-0.0655099505772086,-0.131137554898038,
0.324878770462052));
#13200=CARTESIAN_POINT('Ctrl Pts',(-0.108849371715275,-0.109487285918972,
0.322232440582951));
#13201=CARTESIAN_POINT('Ctrl Pts',(-0.140394307312104,-0.0642268633444555,
0.319586110703849));
#13202=CARTESIAN_POINT('Ctrl Pts',(-0.14570614405606,-0.0160726946583056,
0.316939780824747));
#13203=CARTESIAN_POINT('Ctrl Pts',(-0.146291106736525,-0.0107697471190636,
0.316648355411261));
#13204=CARTESIAN_POINT('Ctrl Pts',(-0.146557930734812,-0.0054317060295066,
0.316356929997776));
#13205=CARTESIAN_POINT('Ctrl Pts',(-0.146519404976022,-8.97763884284003E-5,
0.316065504584291));
#13206=CARTESIAN_POINT('Ctrl Pts',(-0.146528765763263,-8.45393868379275E-5,
0.30893449541571));
#13207=CARTESIAN_POINT('Ctrl Pts',(-0.146562807199252,-0.00503327764821679,
0.30920451587328));
#13208=CARTESIAN_POINT('Ctrl Pts',(-0.14633385314783,-0.00997882882536714,
0.30947453633085));
#13209=CARTESIAN_POINT('Ctrl Pts',(-0.145831525524598,-0.0148964553326841,
0.309744556788419));
#13210=CARTESIAN_POINT('Ctrl Pts',(-0.140906503086998,-0.0631108472318147,
0.312391946162679));
#13211=CARTESIAN_POINT('Ctrl Pts',(-0.109703085900295,-0.108640943453547,
0.31503933553694));
#13212=CARTESIAN_POINT('Ctrl Pts',(-0.0665140418604196,-0.13063162118607,
0.3176867249112));
#13213=CARTESIAN_POINT('Ctrl Pts',(-0.0233249978205455,-0.152622298918592,
0.32033411428546));
#13214=CARTESIAN_POINT('Ctrl Pts',(0.0318496730725009,-0.151073558161906,
0.322981503659719));
#13215=CARTESIAN_POINT('Ctrl Pts',(0.0737371373950496,-0.126694801736668,
0.325628893033979));
#13216=CARTESIAN_POINT('Ctrl Pts',(0.115624601717599,-0.10231604531143,
0.328276282408239));
#13217=CARTESIAN_POINT('Ctrl Pts',(0.144224859469651,-0.0551072732176397,
0.3309236717825));
#13218=CARTESIAN_POINT('Ctrl Pts',(0.146437523492708,-0.0066925280449658,
0.33357106115676));
#13219=CARTESIAN_POINT('Ctrl Pts',(0.148650187515766,0.0417222171277085,
0.33621845053102));
#13220=CARTESIAN_POINT('Ctrl Pts',(0.124475257809829,0.0913429353792657,
0.33886583990528));
#13221=CARTESIAN_POINT('Ctrl Pts',(0.0849860939726622,0.119440788885456,
0.34151322927954));
#13222=CARTESIAN_POINT('Ctrl Pts',(0.0454969301354961,0.147538642391646,
0.344160618653799));
#13223=CARTESIAN_POINT('Ctrl Pts',(-0.00930646783289898,0.154113631152469,
0.346808008028059));
#13224=CARTESIAN_POINT('Ctrl Pts',(-0.0543213285795041,0.136154072578339,
0.349455397402319));
#13225=CARTESIAN_POINT('Ctrl Pts',(-0.0993361893261098,0.11819451400421,
0.352102786776579));
#13226=CARTESIAN_POINT('Ctrl Pts',(-0.134562512850926,0.0757004080951257,
0.35475017615084));
#13227=CARTESIAN_POINT('Ctrl Pts',(-0.143864833510727,0.0281362381501331,
0.3573975655251));
#13228=CARTESIAN_POINT('Ctrl Pts',(-0.145664973529558,0.0189318504589563,
0.357909875488637));
#13229=CARTESIAN_POINT('Ctrl Pts',(-0.146494308508217,0.00953759842677947,
0.358422185452174));
#13230=CARTESIAN_POINT('Ctrl Pts',(-0.146408012399712,0.000128195943346294,
0.358934495415711));
#13231=CARTESIAN_POINT('Origin',(0.,0.,0.));
#13232=CARTESIAN_POINT('',(-0.146110491840834,1.12683595067248E-5,0.416065504584291));
#13233=CARTESIAN_POINT('',(-0.146109756335714,8.81622270207575E-6,0.40893449541571));
#13234=CARTESIAN_POINT('',(-0.14635,-1.79227059055215E-17,0.));
#13235=CARTESIAN_POINT('Ctrl Pts',(-0.146110491840834,1.12683595067248E-5,
0.416065504584291));
#13236=CARTESIAN_POINT('Ctrl Pts',(-0.146126798292857,0.0237518011834032,
0.414779555213666));
#13237=CARTESIAN_POINT('Ctrl Pts',(-0.140669750958991,0.0474852665485293,
0.413493605843041));
#13238=CARTESIAN_POINT('Ctrl Pts',(-0.129698698951591,0.0683144158983218,
0.412207656472415));
#13239=CARTESIAN_POINT('Ctrl Pts',(-0.107121587134001,0.111178312051432,
0.409561326593314));
#13240=CARTESIAN_POINT('Ctrl Pts',(-0.0611933749717542,0.141742803557285,
0.406914996714211));
#13241=CARTESIAN_POINT('Ctrl Pts',(-0.0129361277491455,0.146018041789781,
0.40426866683511));
#13242=CARTESIAN_POINT('Ctrl Pts',(0.0353211194734639,0.150293280022276,
0.401622336956008));
#13243=CARTESIAN_POINT('Ctrl Pts',(0.0859074017564354,0.128279264981412,
0.398976007076906));
#13244=CARTESIAN_POINT('Ctrl Pts',(0.115668581836909,0.0900521576926538,
0.396329677197804));
#13245=CARTESIAN_POINT('Ctrl Pts',(0.145429761917382,0.0518250504038959,
0.393683347318702));
#13246=CARTESIAN_POINT('Ctrl Pts',(0.154365839795359,-0.0026151491327561,
0.3910370174396));
#13247=CARTESIAN_POINT('Ctrl Pts',(0.138386632036901,-0.0483503050946702,
0.388390687560498));
#13248=CARTESIAN_POINT('Ctrl Pts',(0.122407424278443,-0.094085461056585,
0.385744357681396));
#13249=CARTESIAN_POINT('Ctrl Pts',(0.0815129308835505,-0.131115573443762,
0.383098027802294));
#13250=CARTESIAN_POINT('Ctrl Pts',(0.0344212048624006,-0.142491377230642,
0.380451697923192));
#13251=CARTESIAN_POINT('Ctrl Pts',(-0.0126705211587486,-0.153867181017521,
0.37780536804409));
#13252=CARTESIAN_POINT('Ctrl Pts',(-0.0659594798061549,-0.139588676204105,
0.375159038164988));
#13253=CARTESIAN_POINT('Ctrl Pts',(-0.101054476324393,-0.106191359083811,
0.372512708285887));
#13254=CARTESIAN_POINT('Ctrl Pts',(-0.129554902927378,-0.0790696072742943,
0.370363640385355));
#13255=CARTESIAN_POINT('Ctrl Pts',(-0.146056480184715,-0.0393390709180539,
0.368214572484823));
#13256=CARTESIAN_POINT('Ctrl Pts',(-0.146416087288192,0.000126442170093593,
0.366065504584291));
#13257=CARTESIAN_POINT('Ctrl Pts',(-0.146408012399712,0.000128195943346294,
0.358934495415711));
#13258=CARTESIAN_POINT('Ctrl Pts',(-0.146048368712081,-0.0390859965171687,
0.361069574826434));
#13259=CARTESIAN_POINT('Ctrl Pts',(-0.1297855810823,-0.0785633296797545,
0.363204654237157));
#13260=CARTESIAN_POINT('Ctrl Pts',(-0.101613371150224,-0.105657280969165,
0.36533973364788));
#13261=CARTESIAN_POINT('Ctrl Pts',(-0.066681270335132,-0.139252396162569,
0.36798712302214));
#13262=CARTESIAN_POINT('Ctrl Pts',(-0.0134387509101597,-0.153808392568477,
0.370634512396399));
#13263=CARTESIAN_POINT('Ctrl Pts',(0.0337263783221333,-0.142657876135818,
0.373281901770659));
#13264=CARTESIAN_POINT('Ctrl Pts',(0.0808915075544263,-0.13150735970316,
0.375929291144919));
#13265=CARTESIAN_POINT('Ctrl Pts',(0.12197924659404,-0.0946503304319347,
0.378576680519179));
#13266=CARTESIAN_POINT('Ctrl Pts',(0.138169300408926,-0.0489692009616054,
0.38122406989344));
#13267=CARTESIAN_POINT('Ctrl Pts',(0.154359354223812,-0.00328807149127619,
0.3838714592677));
#13268=CARTESIAN_POINT('Ctrl Pts',(0.14565172281397,0.0512171581781573,
0.38651884864196));
#13269=CARTESIAN_POINT('Ctrl Pts',(0.11603494864959,0.0895802930905963,
0.38916623801622));
#13270=CARTESIAN_POINT('Ctrl Pts',(0.0864181744852101,0.127943428003035,
0.39181362739048));
#13271=CARTESIAN_POINT('Ctrl Pts',(0.0358922575662923,0.15016446815848,
0.394461016764739));
#13272=CARTESIAN_POINT('Ctrl Pts',(-0.0123993367959677,0.146065035738641,
0.397108406138999));
#13273=CARTESIAN_POINT('Ctrl Pts',(-0.0606909311582276,0.141965603318802,
0.399755795513259));
#13274=CARTESIAN_POINT('Ctrl Pts',(-0.106748202963829,0.111545698323679,
0.40240318488752));
#13275=CARTESIAN_POINT('Ctrl Pts',(-0.129474555904152,0.0687391998188283,
0.40505057426178));
#13276=CARTESIAN_POINT('Ctrl Pts',(-0.140588317483115,0.0478057390183907,
0.406345214646423));
#13277=CARTESIAN_POINT('Ctrl Pts',(-0.146122589096428,0.0239100770892618,
0.407639855031067));
#13278=CARTESIAN_POINT('Ctrl Pts',(-0.146109756335714,8.81622270207575E-6,
0.40893449541571));
#13279=CARTESIAN_POINT('Origin',(0.,0.,0.));
#13280=CARTESIAN_POINT('',(-0.146374718215768,-0.000132229735885947,0.466065504584291));
#13281=CARTESIAN_POINT('',(-0.146375609273197,-0.000132432188538665,0.458934495415711));
#13282=CARTESIAN_POINT('',(-0.14635,-1.79227059055215E-17,0.));
#13283=CARTESIAN_POINT('Ctrl Pts',(-0.146374718215768,-0.000132229735885947,
0.466065504584291));
#13284=CARTESIAN_POINT('Ctrl Pts',(-0.146022504084922,0.0379941335185874,
0.46399086782161));
#13285=CARTESIAN_POINT('Ctrl Pts',(-0.130761950520226,0.0763703265456945,
0.46191623105893));
#13286=CARTESIAN_POINT('Ctrl Pts',(-0.103994021541854,0.103314352404769,
0.45984159429625));
#13287=CARTESIAN_POINT('Ctrl Pts',(-0.0698498419286355,0.137683154682254,
0.457195264417148));
#13288=CARTESIAN_POINT('Ctrl Pts',(-0.0169824611430249,0.153451124186949,
0.454548934538046));
#13289=CARTESIAN_POINT('Ctrl Pts',(0.030409888879481,0.143401013202843,
0.451902604658944));
#13290=CARTESIAN_POINT('Ctrl Pts',(0.0778022389019875,0.133350902218736,
0.449256274779842));
#13291=CARTESIAN_POINT('Ctrl Pts',(0.119719558161389,0.0974827107458278,
0.44660994490074));
#13292=CARTESIAN_POINT('Ctrl Pts',(0.136975630157447,0.0522138743269898,
0.443963615021638));
#13293=CARTESIAN_POINT('Ctrl Pts',(0.154231702153504,0.00694503790815254,
0.441317285142536));
#13294=CARTESIAN_POINT('Ctrl Pts',(0.146826526886218,-0.0477244434566137,
0.438670955263434));
#13295=CARTESIAN_POINT('Ctrl Pts',(0.118149569579287,-0.0867714880447125,
0.436024625384332));
#13296=CARTESIAN_POINT('Ctrl Pts',(0.0894726122723542,-0.125818532632812,
0.43337829550523));
#13297=CARTESIAN_POINT('Ctrl Pts',(0.0395238729257754,-0.149243140444243,
0.430731965626129));
#13298=CARTESIAN_POINT('Ctrl Pts',(-0.00883432462988853,-0.146323499949933,
0.428085635747027));
#13299=CARTESIAN_POINT('Ctrl Pts',(-0.0571925221855517,-0.143403859455623,
0.425439305867925));
#13300=CARTESIAN_POINT('Ctrl Pts',(-0.1039601779503,-0.114139970655572,
0.422792975988823));
#13301=CARTESIAN_POINT('Ctrl Pts',(-0.127731000096207,-0.0719263758553634,
0.420146646109721));
#13302=CARTESIAN_POINT('Ctrl Pts',(-0.139950702323481,-0.0502259249733931,
0.418786265601244));
#13303=CARTESIAN_POINT('Ctrl Pts',(-0.146093241566443,-0.0251033736724598,
0.417425885092767));
#13304=CARTESIAN_POINT('Ctrl Pts',(-0.146110491840834,1.12683595067248E-5,
0.416065504584291));
#13305=CARTESIAN_POINT('Ctrl Pts',(-0.146109756335714,8.81622270207575E-6,
0.40893449541571));
#13306=CARTESIAN_POINT('Ctrl Pts',(-0.146096347589706,-0.0249652282079418,
0.410287244405327));
#13307=CARTESIAN_POINT('Ctrl Pts',(-0.140026707259891,-0.049945385460595,
0.411639993394943));
#13308=CARTESIAN_POINT('Ctrl Pts',(-0.127937780377622,-0.0715588049813403,
0.412992742384559));
#13309=CARTESIAN_POINT('Ctrl Pts',(-0.104279217835726,-0.113857219262079,
0.415640131758819));
#13310=CARTESIAN_POINT('Ctrl Pts',(-0.0575666586768896,-0.14326095580898,
0.41828752113308));
#13311=CARTESIAN_POINT('Ctrl Pts',(-0.00919685447762893,-0.146301592903247,
0.42093491050734));
#13312=CARTESIAN_POINT('Ctrl Pts',(0.039172949721632,-0.149342229997515,
0.4235822998816));
#13313=CARTESIAN_POINT('Ctrl Pts',(0.089199998961318,-0.126019767639148,
0.426229689255859));
#13314=CARTESIAN_POINT('Ctrl Pts',(0.117969334952632,-0.0870170915920772,
0.428877078630119));
#13315=CARTESIAN_POINT('Ctrl Pts',(0.146738670943946,-0.0480144155450057,
0.431524468004379));
#13316=CARTESIAN_POINT('Ctrl Pts',(0.154250293686888,0.00666847419077017,
0.43417185737864));
#13317=CARTESIAN_POINT('Ctrl Pts',(0.137063494116028,0.051984005222912,
0.4368192467529));
#13318=CARTESIAN_POINT('Ctrl Pts',(0.119876694545168,0.0972995362550541,
0.43946663612716));
#13319=CARTESIAN_POINT('Ctrl Pts',(0.0779914726605056,0.133247708583562,
0.442114025501419));
#13320=CARTESIAN_POINT('Ctrl Pts',(0.0305934116013849,0.143362412733947,
0.444761414875679));
#13321=CARTESIAN_POINT('Ctrl Pts',(-0.0168046494577345,0.153477116884331,
0.447408804249939));
#13322=CARTESIAN_POINT('Ctrl Pts',(-0.0697155496913122,0.137758352856595,
0.4500561936242));
#13323=CARTESIAN_POINT('Ctrl Pts',(-0.103903378920715,0.103406122000434,
0.45270358299846));
#13324=CARTESIAN_POINT('Ctrl Pts',(-0.130724942802416,0.0764555792150183,
0.45478055380421));
#13325=CARTESIAN_POINT('Ctrl Pts',(-0.146022533856355,0.0380362146017157,
0.45685752460996));
#13326=CARTESIAN_POINT('Ctrl Pts',(-0.146375609273197,-0.000132432188538665,
0.458934495415711));
#13327=CARTESIAN_POINT('Origin',(0.,0.,0.));
#13328=CARTESIAN_POINT('',(-0.146548608312775,6.99729089778146E-5,0.516065504584291));
#13329=CARTESIAN_POINT('',(-0.146550766805835,6.86360251013434E-5,0.508934495415711));
#13330=CARTESIAN_POINT('',(-0.14635,-1.79227059055215E-17,0.));
#13331=CARTESIAN_POINT('Ctrl Pts',(-0.146548608312775,6.99729089778146E-5,
0.516065504584291));
#13332=CARTESIAN_POINT('Ctrl Pts',(-0.146572081366671,0.00404546554386884,
0.515848510308657));
#13333=CARTESIAN_POINT('Ctrl Pts',(-0.146424333269732,0.00801918670503405,
0.515631516033023));
#13334=CARTESIAN_POINT('Ctrl Pts',(-0.146099725131082,0.0119784074854107,
0.51541452175739));
#13335=CARTESIAN_POINT('Ctrl Pts',(-0.142141002193345,0.06026265009261,
0.512768191878288));
#13336=CARTESIAN_POINT('Ctrl Pts',(-0.111878319621163,0.106390286678145,
0.510121861999186));
#13337=CARTESIAN_POINT('Ctrl Pts',(-0.069163383343408,0.129247972261684,
0.507475532120084));
#13338=CARTESIAN_POINT('Ctrl Pts',(-0.0264484470656534,0.152105657845224,
0.504829202240982));
#13339=CARTESIAN_POINT('Ctrl Pts',(0.0287187429176733,0.151693392426768,
0.50218287236188));
#13340=CARTESIAN_POINT('Ctrl Pts',(0.07108729581893,0.128199876374419,0.499536542482778));
#13341=CARTESIAN_POINT('Ctrl Pts',(0.113455848720186,0.10470636032207,0.496890212603677));
#13342=CARTESIAN_POINT('Ctrl Pts',(0.143025764539373,0.0581315936358261,
0.494243882724575));
#13343=CARTESIAN_POINT('Ctrl Pts',(0.146262427589597,0.00979357977770552,
0.491597552845473));
#13344=CARTESIAN_POINT('Ctrl Pts',(0.149499090639821,-0.0385444340804161,
0.488951222966371));
#13345=CARTESIAN_POINT('Ctrl Pts',(0.126402500921083,-0.0886456951104151,
0.486304893087269));
#13346=CARTESIAN_POINT('Ctrl Pts',(0.087544330920799,-0.117578067907642,
0.483658563208167));
#13347=CARTESIAN_POINT('Ctrl Pts',(0.0486861609205161,-0.146510440704867,
0.481012233329065));
#13348=CARTESIAN_POINT('Ctrl Pts',(-0.00593358936131212,-0.154273925269321,
0.478365903449963));
#13349=CARTESIAN_POINT('Ctrl Pts',(-0.0513146009011563,-0.137315052574797,
0.475719573570861));
#13350=CARTESIAN_POINT('Ctrl Pts',(-0.0966956124410008,-0.120356179880273,
0.473073243691759));
#13351=CARTESIAN_POINT('Ctrl Pts',(-0.132837885238862,-0.078674949926771,
0.470426913812657));
#13352=CARTESIAN_POINT('Ctrl Pts',(-0.14319853241738,-0.0313495174248821,
0.467780583933555));
#13353=CARTESIAN_POINT('Ctrl Pts',(-0.145436768368387,-0.0211256884885646,
0.467208890817134));
#13354=CARTESIAN_POINT('Ctrl Pts',(-0.146471775395962,-0.0106384445195334,
0.466637197700712));
#13355=CARTESIAN_POINT('Ctrl Pts',(-0.146374718215768,-0.000132229735885947,
0.466065504584291));
#13356=CARTESIAN_POINT('Ctrl Pts',(-0.146375609273197,-0.000132432188538665,
0.458934495415711));
#13357=CARTESIAN_POINT('Ctrl Pts',(-0.146472577787773,-0.0106150565970108,
0.45950491398422));
#13358=CARTESIAN_POINT('Ctrl Pts',(-0.145442327125792,-0.021078770125739,
0.46007533255273));
#13359=CARTESIAN_POINT('Ctrl Pts',(-0.143213999951756,-0.0312807998000163,
0.460645751121239));
#13360=CARTESIAN_POINT('Ctrl Pts',(-0.132872033528166,-0.0786297930597184,
0.463293140495499));
#13361=CARTESIAN_POINT('Ctrl Pts',(-0.0967233424557573,-0.120342081894533,
0.465940529869759));
#13362=CARTESIAN_POINT('Ctrl Pts',(-0.0513258840937604,-0.13731129538499,
0.46858791924402));
#13363=CARTESIAN_POINT('Ctrl Pts',(-0.00592842573176499,-0.154280508875447,
0.47123530861828));
#13364=CARTESIAN_POINT('Ctrl Pts',(0.0487177999198187,-0.146506647021548,
0.47388269799254));
#13365=CARTESIAN_POINT('Ctrl Pts',(0.0875820145025328,-0.117550537871965,
0.476530087366799));
#13366=CARTESIAN_POINT('Ctrl Pts',(0.126446229085248,-0.0885944287223814,
0.47917747674106));
#13367=CARTESIAN_POINT('Ctrl Pts',(0.149528432599094,-0.0384560722771122,
0.481824866115319));
#13368=CARTESIAN_POINT('Ctrl Pts',(0.146255790172295,0.0098985887573764,
0.484472255489579));
#13369=CARTESIAN_POINT('Ctrl Pts',(0.142983147745498,0.0582532497918637,
0.487119644863839));
#13370=CARTESIAN_POINT('Ctrl Pts',(0.113355659378058,0.10482421541557,0.4897670342381));
#13371=CARTESIAN_POINT('Ctrl Pts',(0.0709442366160257,0.128279591164298,
0.49241442361236));
#13372=CARTESIAN_POINT('Ctrl Pts',(0.0285328138539934,0.151734966913027,
0.49506181298662));
#13373=CARTESIAN_POINT('Ctrl Pts',(-0.0266625433026316,0.152074752786777,
0.497709202360879));
#13374=CARTESIAN_POINT('Ctrl Pts',(-0.0693595260588707,0.129143309401606,
0.500356591735139));
#13375=CARTESIAN_POINT('Ctrl Pts',(-0.11205650881511,0.106211866016435,
0.503003981109399));
#13376=CARTESIAN_POINT('Ctrl Pts',(-0.142255117170964,0.060009193372344,
0.505651370483659));
#13377=CARTESIAN_POINT('Ctrl Pts',(-0.146122837288996,0.0116984888307781,
0.50829875985792));
#13378=CARTESIAN_POINT('Ctrl Pts',(-0.146432431239741,0.00783142983325791,
0.508510671710517));
#13379=CARTESIAN_POINT('Ctrl Pts',(-0.14657331536999,0.00395086404934249,
0.508722583563114));
#13380=CARTESIAN_POINT('Ctrl Pts',(-0.146550766805835,6.86360251013434E-5,
0.508934495415711));
#13381=CARTESIAN_POINT('Origin',(0.,0.,0.));
#13382=CARTESIAN_POINT('',(-0.146165204287215,8.83645032875094E-5,0.566065504584291));
#13383=CARTESIAN_POINT('',(-0.146168951232552,9.12430751481418E-5,0.558934495415711));
#13384=CARTESIAN_POINT('',(-0.14635,-1.79227059055215E-17,0.));
#13385=CARTESIAN_POINT('Ctrl Pts',(-0.146165204287215,8.83645032875094E-5,
0.566065504584291));
#13386=CARTESIAN_POINT('Ctrl Pts',(-0.146267412293664,0.0186373661349918,
0.565059822916602));
#13387=CARTESIAN_POINT('Ctrl Pts',(-0.142994166834961,0.0371516370495788,
0.564054141248913));
#13388=CARTESIAN_POINT('Ctrl Pts',(-0.136179985035193,0.0542551712289143,
0.563048459581224));
#13389=CARTESIAN_POINT('Ctrl Pts',(-0.118249288396568,0.0992610562830057,
0.560402129702122));
#13390=CARTESIAN_POINT('Ctrl Pts',(-0.0758005933416487,0.134498778989873,
0.55775579982302));
#13391=CARTESIAN_POINT('Ctrl Pts',(-0.0282633354322908,0.143839479279877,
0.555109469943918));
#13392=CARTESIAN_POINT('Ctrl Pts',(0.0192739224770691,0.153180179569881,
0.552463140064816));
#13393=CARTESIAN_POINT('Ctrl Pts',(0.0718997432408687,0.136623857443018,
0.549816810185715));
#13394=CARTESIAN_POINT('Ctrl Pts',(0.105526460745998,0.101748602013432,
0.547170480306613));
#13395=CARTESIAN_POINT('Ctrl Pts',(0.139153178251127,0.0668733465838454,
0.544524150427511));
#13396=CARTESIAN_POINT('Ctrl Pts',(0.153780792497586,0.0136791578515372,
0.541877820548409));
#13397=CARTESIAN_POINT('Ctrl Pts',(0.142714014311998,-0.0334861471092027,
0.539231490669307));
#13398=CARTESIAN_POINT('Ctrl Pts',(0.13164723612641,-0.0806514520699426,
0.536585160790205));
#13399=CARTESIAN_POINT('Ctrl Pts',(0.0948860655087725,-0.121787873259113,
0.533938830911103));
#13400=CARTESIAN_POINT('Ctrl Pts',(0.0492566686055307,-0.138066623508903,
0.531292501032001));
#13401=CARTESIAN_POINT('Ctrl Pts',(0.00362727170228945,-0.154345373758693,
0.528646171152899));
#13402=CARTESIAN_POINT('Ctrl Pts',(-0.050870351486557,-0.145766453069103,
0.525999841273797));
#13403=CARTESIAN_POINT('Ctrl Pts',(-0.089291781429334,-0.116256568409877,
0.523353511394695));
#13404=CARTESIAN_POINT('Ctrl Pts',(-0.124562723435938,-0.0891664410515947,
0.520924175791227));
#13405=CARTESIAN_POINT('Ctrl Pts',(-0.146285818313441,-0.0444372186796531,
0.518494840187759));
#13406=CARTESIAN_POINT('Ctrl Pts',(-0.146548608312775,6.99729089778146E-5,
0.516065504584291));
#13407=CARTESIAN_POINT('Ctrl Pts',(-0.146550766805835,6.86360251013434E-5,
0.508934495415711));
#13408=CARTESIAN_POINT('Ctrl Pts',(-0.146291618860727,-0.0445493453248537,
0.511369972937373));
#13409=CARTESIAN_POINT('Ctrl Pts',(-0.124445252016267,-0.0893868858389474,
0.513805450459036));
#13410=CARTESIAN_POINT('Ctrl Pts',(-0.0890226177929609,-0.116463349340462,
0.516240927980699));
#13411=CARTESIAN_POINT('Ctrl Pts',(-0.0505178462986829,-0.145895746531099,
0.518888317354959));
#13412=CARTESIAN_POINT('Ctrl Pts',(0.00402852857008221,-0.154341804473332,
0.52153570672922));
#13413=CARTESIAN_POINT('Ctrl Pts',(0.0496314652424392,-0.137932794781367,
0.52418309610348));
#13414=CARTESIAN_POINT('Ctrl Pts',(0.0952344019147948,-0.121523785089403,
0.52683048547774));
#13415=CARTESIAN_POINT('Ctrl Pts',(0.131893900390741,-0.0802597077632436,
0.529477874851999));
#13416=CARTESIAN_POINT('Ctrl Pts',(0.14281802728161,-0.0330416298281342,
0.532125264226259));
#13417=CARTESIAN_POINT('Ctrl Pts',(0.153742154172479,0.0141764481069759,
0.53477265360052));
#13418=CARTESIAN_POINT('Ctrl Pts',(0.138930909478268,0.0673485266510362,
0.53742004297478));
#13419=CARTESIAN_POINT('Ctrl Pts',(0.105168604077417,0.102119062543277,
0.54006743234904));
#13420=CARTESIAN_POINT('Ctrl Pts',(0.0714062986765666,0.136889598435517,
0.5427148217233));
#13421=CARTESIAN_POINT('Ctrl Pts',(0.018692932569077,0.153258591675938,
0.545362211097559));
#13422=CARTESIAN_POINT('Ctrl Pts',(-0.0288260648428939,0.143728202535144,
0.548009600471819));
#13423=CARTESIAN_POINT('Ctrl Pts',(-0.0763450622548654,0.13419781339435,
0.550656989846079));
#13424=CARTESIAN_POINT('Ctrl Pts',(-0.118669690971318,0.0987680418723385,
0.55330437922034));
#13425=CARTESIAN_POINT('Ctrl Pts',(-0.136413096952957,0.0536675432455532,
0.5559517685946));
#13426=CARTESIAN_POINT('Ctrl Pts',(-0.143076734904351,0.036729792140314,
0.556946010868304));
#13427=CARTESIAN_POINT('Ctrl Pts',(-0.146273385252938,0.0184280612467595,
0.557940253142007));
#13428=CARTESIAN_POINT('Ctrl Pts',(-0.146168951232552,9.12430751481418E-5,
0.558934495415711));
#13429=CARTESIAN_POINT('Origin',(0.,0.,0.));
#13430=CARTESIAN_POINT('',(-0.146227179098081,-0.000117664897458569,0.616065504584291));
#13431=CARTESIAN_POINT('',(-0.146218520919543,-0.000115076211918358,0.608934495415711));
#13432=CARTESIAN_POINT('',(-0.14635,-1.79227059055215E-17,0.));
#13433=CARTESIAN_POINT('Ctrl Pts',(-0.146227179098081,-0.000117664897458569,
0.616065504584291));
#13434=CARTESIAN_POINT('Ctrl Pts',(-0.145977603365176,0.0329427899635141,
0.614271135524546));
#13435=CARTESIAN_POINT('Ctrl Pts',(-0.134874795495675,0.0661550248562671,
0.612476766464802));
#13436=CARTESIAN_POINT('Ctrl Pts',(-0.114309815624116,0.091770790457776,
0.610682397405058));
#13437=CARTESIAN_POINT('Ctrl Pts',(-0.0839806476072558,0.129548841477563,
0.608036067525956));
#13438=CARTESIAN_POINT('Ctrl Pts',(-0.0330710111925292,0.150804375664025,
0.605389737646855));
#13439=CARTESIAN_POINT('Ctrl Pts',(0.0151169520838501,0.145808400611758,
0.602743407767753));
#13440=CARTESIAN_POINT('Ctrl Pts',(0.0633049153602295,0.140812425559491,
0.600097077888651));
#13441=CARTESIAN_POINT('Ctrl Pts',(0.108771205498262,0.109564941268491,
0.597450748009549));
#13442=CARTESIAN_POINT('Ctrl Pts',(0.130705186191441,0.0663684129079872,
0.594804418130447));
#13443=CARTESIAN_POINT('Ctrl Pts',(0.152639166884621,0.023171884547483,
0.592158088251345));
#13444=CARTESIAN_POINT('Ctrl Pts',(0.151040838132949,-0.0319736878825246,
0.589511758372243));
#13445=CARTESIAN_POINT('Ctrl Pts',(0.126641780152193,-0.0738273082886534,
0.586865428493141));
#13446=CARTESIAN_POINT('Ctrl Pts',(0.102242722171437,-0.115680928694782,
0.584219098614039));
#13447=CARTESIAN_POINT('Ctrl Pts',(0.0550429349615966,-0.14424259707703,
0.581572768734937));
#13448=CARTESIAN_POINT('Ctrl Pts',(0.00664650371163741,-0.14643918846291,
0.578926438855836));
#13449=CARTESIAN_POINT('Ctrl Pts',(-0.0417499275383225,-0.148635779848789,
0.576280108976733));
#13450=CARTESIAN_POINT('Ctrl Pts',(-0.0913430028284016,-0.1244672942383,
0.573633779097631));
#13451=CARTESIAN_POINT('Ctrl Pts',(-0.119433191362276,-0.0849960277323969,
0.570987449218529));
#13452=CARTESIAN_POINT('Ctrl Pts',(-0.136848298201485,-0.0605249807527623,
0.569346801007117));
#13453=CARTESIAN_POINT('Ctrl Pts',(-0.145998464265635,-0.0301720919893573,
0.567706152795704));
#13454=CARTESIAN_POINT('Ctrl Pts',(-0.146165204287215,8.83645032875094E-5,
0.566065504584291));
#13455=CARTESIAN_POINT('Ctrl Pts',(-0.146168951232552,9.12430751481418E-5,
0.558934495415711));
#13456=CARTESIAN_POINT('Ctrl Pts',(-0.145995306636495,-0.0303977620653178,
0.560587642516267));
#13457=CARTESIAN_POINT('Ctrl Pts',(-0.136695352934655,-0.0609837708898569,
0.562240789616823));
#13458=CARTESIAN_POINT('Ctrl Pts',(-0.119031718004195,-0.0855580991331628,
0.563893936717379));
#13459=CARTESIAN_POINT('Ctrl Pts',(-0.090744749826965,-0.124912017153538,
0.566541326091639));
#13460=CARTESIAN_POINT('Ctrl Pts',(-0.0410086302256792,-0.148848627462727,
0.5691887154659));
#13461=CARTESIAN_POINT('Ctrl Pts',(0.00739494322942312,-0.146403732988417,
0.57183610484016));
#13462=CARTESIAN_POINT('Ctrl Pts',(0.0557985166845234,-0.143958838514108,
0.57448349421442));
#13463=CARTESIAN_POINT('Ctrl Pts',(0.10286954399344,-0.1151324392563,0.57713088358868));
#13464=CARTESIAN_POINT('Ctrl Pts',(0.127047076753504,-0.0731285067993286,
0.579778272962939));
#13465=CARTESIAN_POINT('Ctrl Pts',(0.151224609513568,-0.031124574342357,
0.5824256623372));
#13466=CARTESIAN_POINT('Ctrl Pts',(0.15250864772478,0.0240568913137802,
0.58507305171146));
#13467=CARTESIAN_POINT('Ctrl Pts',(0.130311035929276,0.0671399443948921,
0.58772044108572));
#13468=CARTESIAN_POINT('Ctrl Pts',(0.108113424133771,0.110222997476006,
0.59036783045998));
#13469=CARTESIAN_POINT('Ctrl Pts',(0.0624341623315493,0.141207637982093,
0.593015219834239));
#13470=CARTESIAN_POINT('Ctrl Pts',(0.0141966988324609,0.145901308974836,
0.595662609208499));
#13471=CARTESIAN_POINT('Ctrl Pts',(-0.0340407646666261,0.150594979967579,
0.598309998582759));
#13472=CARTESIAN_POINT('Ctrl Pts',(-0.0848364298625779,0.128997681446978,
0.60095738795702));
#13473=CARTESIAN_POINT('Ctrl Pts',(-0.114923272877171,0.091002085522857,
0.60360477733128));
#13474=CARTESIAN_POINT('Ctrl Pts',(-0.135113526827902,0.0655045372973676,
0.60538135002609));
#13475=CARTESIAN_POINT('Ctrl Pts',(-0.14597798884013,0.0326223532682757,
0.6071579227209));
#13476=CARTESIAN_POINT('Ctrl Pts',(-0.146218520919543,-0.000115076211918358,
0.608934495415711));
#13477=CARTESIAN_POINT('Origin',(0.,0.,0.));
#13478=CARTESIAN_POINT('',(-0.146586033401767,-2.15382961294558E-5,0.66606550458429));
#13479=CARTESIAN_POINT('',(-0.146582846697157,-3.00215943766004E-5,0.65893449541571));
#13480=CARTESIAN_POINT('',(-0.14635,-1.79227059055215E-17,0.));
#13481=CARTESIAN_POINT('Ctrl Pts',(-0.146586033401767,-2.15382961294558E-5,
0.66606550458429));
#13482=CARTESIAN_POINT('Ctrl Pts',(-0.146488810225965,0.0472697707580183,
0.663482448132491));
#13483=CARTESIAN_POINT('Ctrl Pts',(-0.121516563758978,0.0946492637554097,
0.660899391680692));
#13484=CARTESIAN_POINT('Ctrl Pts',(-0.0824084263440199,0.121233094478226,
0.658316335228893));
#13485=CARTESIAN_POINT('Ctrl Pts',(-0.0423423130056393,0.148468111155377,
0.655670005349791));
#13486=CARTESIAN_POINT('Ctrl Pts',(0.0125607065496858,0.153876184485078,
0.653023675470689));
#13487=CARTESIAN_POINT('Ctrl Pts',(0.0571706564953393,0.134981954220393,
0.650377345591587));
#13488=CARTESIAN_POINT('Ctrl Pts',(0.101780606440992,0.116087723955709,
0.647731015712485));
#13489=CARTESIAN_POINT('Ctrl Pts',(0.136097486776972,0.0728911900966409,
0.645084685833384));
#13490=CARTESIAN_POINT('Ctrl Pts',(0.144413921474191,0.0251640857912735,
0.642438355954282));
#13491=CARTESIAN_POINT('Ctrl Pts',(0.152730356171409,-0.0225630185140953,
0.63979202607518));
#13492=CARTESIAN_POINT('Ctrl Pts',(0.135046345229863,-0.0748206932657649,
0.637145696196077));
#13493=CARTESIAN_POINT('Ctrl Pts',(0.0994561386758346,-0.10768977857233,
0.634499366316975));
#13494=CARTESIAN_POINT('Ctrl Pts',(0.0638659321218069,-0.140558863878895,
0.631853036437873));
#13495=CARTESIAN_POINT('Ctrl Pts',(0.0103695299552984,-0.154039359740357,
0.629206706558772));
#13496=CARTESIAN_POINT('Ctrl Pts',(-0.0365469229059137,-0.141961031115491,
0.62656037667967));
#13497=CARTESIAN_POINT('Ctrl Pts',(-0.0834633757671259,-0.129882702490626,
0.623914046800568));
#13498=CARTESIAN_POINT('Ctrl Pts',(-0.123799879323041,-0.0922455493794331,
0.621267716921466));
#13499=CARTESIAN_POINT('Ctrl Pts',(-0.139093781291504,-0.0462766888972804,
0.618621387042364));
#13500=CARTESIAN_POINT('Ctrl Pts',(-0.14401750805555,-0.0314774500153124,
0.617769426223006));
#13501=CARTESIAN_POINT('Ctrl Pts',(-0.14634567687575,-0.0158146654998378,
0.616917465403648));
#13502=CARTESIAN_POINT('Ctrl Pts',(-0.146227179098081,-0.000117664897458569,
0.616065504584291));
#13503=CARTESIAN_POINT('Ctrl Pts',(-0.146218520919543,-0.000115076211918358,
0.608934495415711));
#13504=CARTESIAN_POINT('Ctrl Pts',(-0.1463364217222,-0.0161618722236638,
0.60980531209516));
#13505=CARTESIAN_POINT('Ctrl Pts',(-0.143901781624712,-0.032173889023867,
0.61067612877461));
#13506=CARTESIAN_POINT('Ctrl Pts',(-0.138761720114909,-0.0472643972675185,
0.611546945454059));
#13507=CARTESIAN_POINT('Ctrl Pts',(-0.123135303504819,-0.0931413908061287,
0.614194334828319));
#13508=CARTESIAN_POINT('Ctrl Pts',(-0.0825044494514074,-0.130501484555709,
0.616841724202579));
#13509=CARTESIAN_POINT('Ctrl Pts',(-0.0354801761942514,-0.142231836504824,
0.619489113576839));
#13510=CARTESIAN_POINT('Ctrl Pts',(0.0115440970629072,-0.15396218845394,
0.6221365029511));
#13511=CARTESIAN_POINT('Ctrl Pts',(0.0649617895238099,-0.140062798602586,
0.624783892325359));
#13512=CARTESIAN_POINT('Ctrl Pts',(0.100304854137336,-0.106900301471969,
0.627431281699619));
#13513=CARTESIAN_POINT('Ctrl Pts',(0.135647918750861,-0.0737378043413545,
0.630078671073879));
#13514=CARTESIAN_POINT('Ctrl Pts',(0.15291635551701,-0.0213121999314781,
0.63272606044814));
#13515=CARTESIAN_POINT('Ctrl Pts',(0.144200333369931,0.026362891994447,
0.6353734498224));
#13516=CARTESIAN_POINT('Ctrl Pts',(0.135484311222852,0.0740379839203748,
0.63802083919666));
#13517=CARTESIAN_POINT('Ctrl Pts',(0.100783830162543,0.11696256336235,0.640668228570919));
#13518=CARTESIAN_POINT('Ctrl Pts',(0.055993492972559,0.135474968031154,
0.643315617945179));
#13519=CARTESIAN_POINT('Ctrl Pts',(0.0112031557825773,0.153987372699956,
0.64596300731944));
#13520=CARTESIAN_POINT('Ctrl Pts',(-0.04367703753708,0.148087602595587,
0.6486103966937));
#13521=CARTESIAN_POINT('Ctrl Pts',(-0.0835091394177698,0.120478055479053,
0.65125778606796));
#13522=CARTESIAN_POINT('Ctrl Pts',(-0.122009894390588,0.0937913289882395,
0.653816689183877));
#13523=CARTESIAN_POINT('Ctrl Pts',(-0.146451680634158,0.0468218259492564,
0.656375592299793));
#13524=CARTESIAN_POINT('Ctrl Pts',(-0.146582846697157,-3.00215943766004E-5,
0.65893449541571));
#13525=CARTESIAN_POINT('Origin',(0.,0.,0.));
#13526=CARTESIAN_POINT('',(-0.146290249280603,0.000131112932912382,0.716065504584291));
#13527=CARTESIAN_POINT('',(-0.146307221518699,0.000133045872591754,0.708934495415711));
#13528=CARTESIAN_POINT('',(-0.14635,-1.79227059055215E-17,0.));
#13529=CARTESIAN_POINT('Ctrl Pts',(-0.146290249280603,0.000131112932912382,
0.716065504584291));
#13530=CARTESIAN_POINT('Ctrl Pts',(-0.146406294125046,0.0134819654399978,
0.715340090619538));
#13531=CARTESIAN_POINT('Ctrl Pts',(-0.144729088574721,0.0268041890186768,
0.714614676654786));
#13532=CARTESIAN_POINT('Ctrl Pts',(-0.141142411757643,0.0395908011096033,
0.713889262690033));
#13533=CARTESIAN_POINT('Ctrl Pts',(-0.128058117149462,0.0862367098911347,
0.711242932810931));
#13534=CARTESIAN_POINT('Ctrl Pts',(-0.0895623832093418,0.125754646095387,
0.708596602931829));
#13535=CARTESIAN_POINT('Ctrl Pts',(-0.0432753130058998,0.140056628595385,
0.705950273052727));
#13536=CARTESIAN_POINT('Ctrl Pts',(0.00301175719754219,0.154358611095384,
0.703303943173625));
#13537=CARTESIAN_POINT('Ctrl Pts',(0.0570901636643063,0.143444639891129,
0.700657613294523));
#13538=CARTESIAN_POINT('Ctrl Pts',(0.0942073689518517,0.11231021130972,
0.698011283415421));
#13539=CARTESIAN_POINT('Ctrl Pts',(0.131324574239397,0.0811757827283121,
0.695364953536319));
#13540=CARTESIAN_POINT('Ctrl Pts',(0.151480578347723,0.0298208967697505,
0.692718623657217));
#13541=CARTESIAN_POINT('Ctrl Pts',(0.145449661086834,-0.0182485073085286,
0.690072293778115));
#13542=CARTESIAN_POINT('Ctrl Pts',(0.139418743825945,-0.0663179113868083,
0.687425963899014));
#13543=CARTESIAN_POINT('Ctrl Pts',(0.107200905195838,-0.111101833584806,
0.684779634019911));
#13544=CARTESIAN_POINT('Ctrl Pts',(0.0635427568131047,-0.132101968137704,
0.68213330414081));
#13545=CARTESIAN_POINT('Ctrl Pts',(0.0198846084303716,-0.153102102690602,
0.679486974261708));
#13546=CARTESIAN_POINT('Ctrl Pts',(-0.0352138497049885,-0.150318449598402,
0.676840644382606));
#13547=CARTESIAN_POINT('Ctrl Pts',(-0.0765331864534889,-0.125025130675956,
0.674194314503504));
#13548=CARTESIAN_POINT('Ctrl Pts',(-0.117852523201989,-0.0997318117535095,
0.671547984624402));
#13549=CARTESIAN_POINT('Ctrl Pts',(-0.14539273856363,-0.0519288270008166,
0.6689016547453));
#13550=CARTESIAN_POINT('Ctrl Pts',(-0.146548242683733,-0.00349635461217019,
0.666255324866198));
#13551=CARTESIAN_POINT('Ctrl Pts',(-0.146575870647472,-0.00233834005587287,
0.666192051438896));
#13552=CARTESIAN_POINT('Ctrl Pts',(-0.146588414938392,-0.00117996563262623,
0.666128778011593));
#13553=CARTESIAN_POINT('Ctrl Pts',(-0.146586033401767,-2.15382961294558E-5,
0.66606550458429));
#13554=CARTESIAN_POINT('Ctrl Pts',(-0.146582846697157,-3.00215943766004E-5,
0.65893449541571));
#13555=CARTESIAN_POINT('Ctrl Pts',(-0.146587382388275,-0.00165014728799839,
0.659022981674053));
#13556=CARTESIAN_POINT('Ctrl Pts',(-0.146562848415234,-0.00327013229389975,
0.659111467932396));
#13557=CARTESIAN_POINT('Ctrl Pts',(-0.146508820881567,-0.00488913307276392,
0.659199954190739));
#13558=CARTESIAN_POINT('Ctrl Pts',(-0.144892390022949,-0.0533274503793473,
0.661847343564999));
#13559=CARTESIAN_POINT('Ctrl Pts',(-0.116875517863988,-0.100884760863813,
0.66449473293926));
#13560=CARTESIAN_POINT('Ctrl Pts',(-0.0752913709948059,-0.125777373450206,
0.66714212231352));
#13561=CARTESIAN_POINT('Ctrl Pts',(-0.0337072241256252,-0.150669986036599,
0.66978951168778));
#13562=CARTESIAN_POINT('Ctrl Pts',(0.021444197453776,-0.15289790072492,
0.672436901062039));
#13563=CARTESIAN_POINT('Ctrl Pts',(0.0649007096996251,-0.131440618146733,
0.675084290436299));
#13564=CARTESIAN_POINT('Ctrl Pts',(0.108357221945475,-0.109983335568545,
0.677731679810559));
#13565=CARTESIAN_POINT('Ctrl Pts',(0.140118824857774,-0.0648408557238465,
0.68037906918482));
#13566=CARTESIAN_POINT('Ctrl Pts',(0.145637072805965,-0.0166907532130915,
0.68302645855908));
#13567=CARTESIAN_POINT('Ctrl Pts',(0.151155320754156,0.031459349297663,
0.68567384793334));
#13568=CARTESIAN_POINT('Ctrl Pts',(0.130430213738242,0.0826170744744734,
0.688321237307599));
#13569=CARTESIAN_POINT('Ctrl Pts',(0.0929549153570804,0.113349556369966,
0.690968626681859));
#13570=CARTESIAN_POINT('Ctrl Pts',(0.0554796169759186,0.14408203826546,
0.693616016056119));
#13571=CARTESIAN_POINT('Ctrl Pts',(0.00125412722950909,0.154389276879634,
0.69626340543038));
#13572=CARTESIAN_POINT('Ctrl Pts',(-0.0448834941801804,0.139550027475769,
0.69891079480464));
#13573=CARTESIAN_POINT('Ctrl Pts',(-0.0910211155898686,0.124710778071904,
0.7015581841789));
#13574=CARTESIAN_POINT('Ctrl Pts',(-0.129070868662838,0.0847250406500019,
0.704205573553159));
#13575=CARTESIAN_POINT('Ctrl Pts',(-0.141604011991841,0.0379083368947344,
0.706852962927419));
#13576=CARTESIAN_POINT('Ctrl Pts',(-0.144888775625201,0.0256383259412015,
0.707546807090183));
#13577=CARTESIAN_POINT('Ctrl Pts',(-0.146420824649375,0.0128991016161637,
0.708240651252947));
#13578=CARTESIAN_POINT('Ctrl Pts',(-0.146307221518699,0.000133045872591754,
0.708934495415711));
#13579=CARTESIAN_POINT('Origin',(0.,0.,0.));
#13580=CARTESIAN_POINT('',(-0.1461301977291,-5.61458017395017E-5,0.766065504584291));
#13581=CARTESIAN_POINT('',(-0.14612241379348,-4.54149644099216E-5,0.758934495415711));
#13582=CARTESIAN_POINT('',(-0.14635,-1.79227059055215E-17,0.));
#13583=CARTESIAN_POINT('Ctrl Pts',(-0.1461301977291,-5.61458017395017E-5,
0.766065504584291));
#13584=CARTESIAN_POINT('Ctrl Pts',(-0.14603380141711,0.0278870014676159,
0.764551403227483));
#13585=CARTESIAN_POINT('Ctrl Pts',(-0.138327245009168,0.0558793842949389,
0.763037301870675));
#13586=CARTESIAN_POINT('Ctrl Pts',(-0.123350675409043,0.079203679241543,
0.761523200513867));
#13587=CARTESIAN_POINT('Ctrl Pts',(-0.0971747899961838,0.119969628197767,
0.758876870634766));
#13588=CARTESIAN_POINT('Ctrl Pts',(-0.048790709571801,0.146475657227381,
0.756230540755664));
#13589=CARTESIAN_POINT('Ctrl Pts',(-0.000344588961360588,0.146589539830481,
0.753584210876561));
#13590=CARTESIAN_POINT('Ctrl Pts',(0.0481015316490792,0.14670342243358,
0.750937880997459));
#13591=CARTESIAN_POINT('Ctrl Pts',(0.0966096924455767,0.120425158610167,
0.748291551118357));
#13592=CARTESIAN_POINT('Ctrl Pts',(0.122976945064223,0.0797827231418903,
0.745645221239255));
#13593=CARTESIAN_POINT('Ctrl Pts',(0.149344197682869,0.0391402876736125,
0.742998891360154));
#13594=CARTESIAN_POINT('Ctrl Pts',(0.153570542123663,-0.01586631943953,
0.740352561481052));
#13595=CARTESIAN_POINT('Ctrl Pts',(0.133721514043982,-0.0600597087159893,
0.73770623160195));
#13596=CARTESIAN_POINT('Ctrl Pts',(0.113872485964301,-0.104253097992448,
0.735059901722848));
#13597=CARTESIAN_POINT('Ctrl Pts',(0.0699480853641458,-0.137633269432224,
0.732413571843746));
#13598=CARTESIAN_POINT('Ctrl Pts',(0.0220532014503509,-0.144921593405036,
0.729767241964644));
#13599=CARTESIAN_POINT('Ctrl Pts',(-0.0258416824634434,-0.152209917377848,
0.727120912085542));
#13600=CARTESIAN_POINT('Ctrl Pts',(-0.0777070496908773,-0.133406393883698,
0.724474582206441));
#13601=CARTESIAN_POINT('Ctrl Pts',(-0.109803305666473,-0.0971176914572187,
0.721828252327339));
#13602=CARTESIAN_POINT('Ctrl Pts',(-0.133101311474982,-0.0707764758164216,
0.71990733641299));
#13603=CARTESIAN_POINT('Ctrl Pts',(-0.14598295937539,-0.0352223077304616,
0.71798642049864));
#13604=CARTESIAN_POINT('Ctrl Pts',(-0.146290249280603,0.000131112932912382,
0.716065504584291));
#13605=CARTESIAN_POINT('Ctrl Pts',(-0.146307221518699,0.000133045872591754,
0.708934495415711));
#13606=CARTESIAN_POINT('Ctrl Pts',(-0.145987367488279,-0.0358102803178394,
0.710888040627207));
#13607=CARTESIAN_POINT('Ctrl Pts',(-0.132622002370819,-0.0719663061161047,
0.712841585838703));
#13608=CARTESIAN_POINT('Ctrl Pts',(-0.1086007072861,-0.0984612847532928,
0.7147951310502));
#13609=CARTESIAN_POINT('Ctrl Pts',(-0.0760477256663158,-0.134366532557423,
0.71744252042446));
#13610=CARTESIAN_POINT('Ctrl Pts',(-0.0239252288417074,-0.152529358077047,
0.720089909798719));
#13611=CARTESIAN_POINT('Ctrl Pts',(0.0238920022682765,-0.144630254255197,
0.722737299172979));
#13612=CARTESIAN_POINT('Ctrl Pts',(0.071709233378259,-0.136731150433346,
0.725384688547239));
#13613=CARTESIAN_POINT('Ctrl Pts',(0.115221198773618,-0.102770117270024,
0.7280320779215));
#13614=CARTESIAN_POINT('Ctrl Pts',(0.134497183226257,-0.058303052428779,
0.730679467295759));
#13615=CARTESIAN_POINT('Ctrl Pts',(0.153773167678896,-0.0138359875875333,
0.733326856670019));
#13616=CARTESIAN_POINT('Ctrl Pts',(0.148813171188813,0.0411371089316358,
0.735974246044279));
#13617=CARTESIAN_POINT('Ctrl Pts',(0.121889126928366,0.0814357351225549,
0.738621635418539));
#13618=CARTESIAN_POINT('Ctrl Pts',(0.0949650826679194,0.121734361313473,
0.741269024792799));
#13619=CARTESIAN_POINT('Ctrl Pts',(0.0460769906371109,0.147358517176143,
0.74391641416706));
#13620=CARTESIAN_POINT('Ctrl Pts',(-0.00238189178169058,0.146571023090686,
0.74656380354132));
#13621=CARTESIAN_POINT('Ctrl Pts',(-0.0508407742004934,0.14578352900523,
0.74921119291558));
#13622=CARTESIAN_POINT('Ctrl Pts',(-0.0988704470072894,0.118584384971644,
0.751858582289839));
#13623=CARTESIAN_POINT('Ctrl Pts',(-0.124470852918682,0.0774321960944291,
0.754505971664099));
#13624=CARTESIAN_POINT('Ctrl Pts',(-0.138745545153454,0.0544858868428234,
0.75598214624797));
#13625=CARTESIAN_POINT('Ctrl Pts',(-0.146046671909043,0.027201385339783,
0.757458320831841));
#13626=CARTESIAN_POINT('Ctrl Pts',(-0.14612241379348,-4.54149644099216E-5,
0.758934495415711));
#13627=CARTESIAN_POINT('Origin',(0.,0.,0.));
#13628=CARTESIAN_POINT('',(-0.146495788566881,-0.000101744904923998,0.816065504584291));
#13629=CARTESIAN_POINT('',(-0.146473871348434,-0.000110945968026819,0.808934495415711));
#13630=CARTESIAN_POINT('',(-0.14635,-1.79227059055215E-17,0.));
#13631=CARTESIAN_POINT('Ctrl Pts',(-0.146495788566881,-0.000101744904923998,
0.816065504584291));
#13632=CARTESIAN_POINT('Ctrl Pts',(-0.14616118452328,0.0421270051992108,
0.813762715835428));
#13633=CARTESIAN_POINT('Ctrl Pts',(-0.126905337350145,0.0846218946815527,
0.811459927086565));
#13634=CARTESIAN_POINT('Ctrl Pts',(-0.0947343415465314,0.111866064832055,
0.809157138337701));
#13635=CARTESIAN_POINT('Ctrl Pts',(-0.0577639214515077,0.143174651664521,
0.806510808458599));
#13636=CARTESIAN_POINT('Ctrl Pts',(-0.00373742343573488,0.154342745753647,
0.803864478579497));
#13637=CARTESIAN_POINT('Ctrl Pts',(0.0426163743729279,0.140258534729872,
0.801218148700395));
#13638=CARTESIAN_POINT('Ctrl Pts',(0.0889701721815907,0.126174323706097,
0.798571818821294));
#13639=CARTESIAN_POINT('Ctrl Pts',(0.127651269783143,0.0868378075694234,
0.795925488942192));
#13640=CARTESIAN_POINT('Ctrl Pts',(0.140954720244851,0.040253928627653,
0.79327915906309));
#13641=CARTESIAN_POINT('Ctrl Pts',(0.154258170706558,-0.00632995031411615,
0.790632829183988));
#13642=CARTESIAN_POINT('Ctrl Pts',(0.14218397402842,-0.060161192060982,
0.787986499304886));
#13643=CARTESIAN_POINT('Ctrl Pts',(0.110258679990485,-0.0966003903512828,
0.785340169425784));
#13644=CARTESIAN_POINT('Ctrl Pts',(0.0783333859525485,-0.133039588641585,
0.782693839546682));
#13645=CARTESIAN_POINT('Ctrl Pts',(0.0265569945548152,-0.152086743475322,
0.780047509667581));
#13646=CARTESIAN_POINT('Ctrl Pts',(-0.021371625274328,-0.14502367242074,
0.777401179788479));
#13647=CARTESIAN_POINT('Ctrl Pts',(-0.0693002451034712,-0.137960601366157,
0.774754849909377));
#13648=CARTESIAN_POINT('Ctrl Pts',(-0.113381093364023,-0.104787304423254,
0.772108520030274));
#13649=CARTESIAN_POINT('Ctrl Pts',(-0.133437672293631,-0.0606877215103841,
0.769462190151172));
#13650=CARTESIAN_POINT('Ctrl Pts',(-0.1420188514214,-0.0418197768941368,
0.768329961628878));
#13651=CARTESIAN_POINT('Ctrl Pts',(-0.146202281842484,-0.0209517273285418,
0.767197733106584));
#13652=CARTESIAN_POINT('Ctrl Pts',(-0.1461301977291,-5.61458017395017E-5,
0.766065504584291));
#13653=CARTESIAN_POINT('Ctrl Pts',(-0.14612241379348,-4.54149644099216E-5,
0.758934495415711));
#13654=CARTESIAN_POINT('Ctrl Pts',(-0.146182508321779,-0.0216633562673834,
0.760105710206101));
#13655=CARTESIAN_POINT('Ctrl Pts',(-0.141694203021096,-0.0432575645610501,
0.76127692499649));
#13656=CARTESIAN_POINT('Ctrl Pts',(-0.132531725405586,-0.0626424774360703,
0.76244813978688));
#13657=CARTESIAN_POINT('Ctrl Pts',(-0.111821052965107,-0.106459728368519,
0.76509552916114));
#13658=CARTESIAN_POINT('Ctrl Pts',(-0.067228569068158,-0.138988996512573,
0.767742918535399));
#13659=CARTESIAN_POINT('Ctrl Pts',(-0.0191799219195066,-0.145330206128911,
0.770390307909659));
#13660=CARTESIAN_POINT('Ctrl Pts',(0.0288687252291434,-0.151671415745249,
0.773037697283919));
#13661=CARTESIAN_POINT('Ctrl Pts',(0.080373535629496,-0.131824566833873,
0.77568508665818));
#13662=CARTESIAN_POINT('Ctrl Pts',(0.111742660473083,-0.0948805356683208,
0.77833247603244));
#13663=CARTESIAN_POINT('Ctrl Pts',(0.14311178531667,-0.0579365045027684,
0.7809798654067));
#13664=CARTESIAN_POINT('Ctrl Pts',(0.154345224603492,-0.00389529108304171,
0.783627254780959));
#13665=CARTESIAN_POINT('Ctrl Pts',(0.140297486112651,0.0424894529122293,
0.786274644155219));
#13666=CARTESIAN_POINT('Ctrl Pts',(0.126249747621811,0.0888741969075009,
0.788922033529479));
#13667=CARTESIAN_POINT('Ctrl Pts',(0.0869208313533056,0.127602471478316,
0.79156942290374));
#13668=CARTESIAN_POINT('Ctrl Pts',(0.0403254011646538,0.140934737517831,
0.794216812278));
#13669=CARTESIAN_POINT('Ctrl Pts',(-0.00627002902399674,0.154267003557346,
0.79686420165226));
#13670=CARTESIAN_POINT('Ctrl Pts',(-0.0601319731327944,0.142203261065564,
0.799511591026519));
#13671=CARTESIAN_POINT('Ctrl Pts',(-0.0965888940360299,0.110269323781398,
0.802158980400779));
#13672=CARTESIAN_POINT('Ctrl Pts',(-0.127690529151203,0.0830262752573849,
0.804417485405756));
#13673=CARTESIAN_POINT('Ctrl Pts',(-0.146124951115714,0.0413218847513699,
0.806675990410734));
#13674=CARTESIAN_POINT('Ctrl Pts',(-0.146473871348434,-0.000110945968026819,
0.808934495415711));
#13675=CARTESIAN_POINT('Origin',(0.,0.,0.));
#13676=CARTESIAN_POINT('',(-0.146444331750498,0.000119944961782359,0.866065504584291));
#13677=CARTESIAN_POINT('',(-0.146471560192382,0.00011177640072981,0.858934495415711));
#13678=CARTESIAN_POINT('',(-0.14635,-1.79227059055215E-17,0.));
#13679=CARTESIAN_POINT('Ctrl Pts',(-0.146444331750498,0.000119944961782359,
0.866065504584291));
#13680=CARTESIAN_POINT('Ctrl Pts',(-0.146516681599632,0.00829054204730037,
0.865620358322474));
#13681=CARTESIAN_POINT('Ctrl Pts',(-0.145891801779796,0.0164500693154795,
0.865175212060658));
#13682=CARTESIAN_POINT('Ctrl Pts',(-0.14453063157077,0.0244848619971339,
0.864730065798841));
#13683=CARTESIAN_POINT('Ctrl Pts',(-0.136438672357208,0.0722505376181754,
0.862083735919739));
#13684=CARTESIAN_POINT('Ctrl Pts',(-0.102325254887189,0.115607931012472,
0.859437406040638));
#13685=CARTESIAN_POINT('Ctrl Pts',(-0.0578046270350215,0.134711681091902,
0.856791076161536));
#13686=CARTESIAN_POINT('Ctrl Pts',(-0.0132839991828526,0.153815431171333,
0.854144746282434));
#13687=CARTESIAN_POINT('Ctrl Pts',(0.0416438390514653,0.148665537935894,
0.851498416403331));
#13688=CARTESIAN_POINT('Ctrl Pts',(0.081837551941475,0.121619188541491,
0.848852086524229));
#13689=CARTESIAN_POINT('Ctrl Pts',(0.122031264831484,0.0945728391470885,
0.846205756645128));
#13690=CARTESIAN_POINT('Ctrl Pts',(0.147490852377186,0.0456300335937214,
0.843559426766026));
#13691=CARTESIAN_POINT('Ctrl Pts',(0.146563060809277,-0.0028073360113171,
0.840913096886925));
#13692=CARTESIAN_POINT('Ctrl Pts',(0.145635269241369,-0.0512447056163556,
0.838266767007823));
#13693=CARTESIAN_POINT('Ctrl Pts',(0.118320098559852,-0.0991766392730661,
0.835620437128721));
#13694=CARTESIAN_POINT('Ctrl Pts',(0.0771201321287374,-0.124663936845065,
0.832974107249619));
#13695=CARTESIAN_POINT('Ctrl Pts',(0.035920165697623,-0.150151234417064,
0.830327777370517));
#13696=CARTESIAN_POINT('Ctrl Pts',(-0.0191645964830881,-0.153193895904352,
0.827681447491415));
#13697=CARTESIAN_POINT('Ctrl Pts',(-0.0629209921278279,-0.132399247274726,
0.825035117612313));
#13698=CARTESIAN_POINT('Ctrl Pts',(-0.106677387772568,-0.111604598645101,
0.822388787733211));
#13699=CARTESIAN_POINT('Ctrl Pts',(-0.139105416881337,-0.0669726398985626,
0.819742457854109));
#13700=CARTESIAN_POINT('Ctrl Pts',(-0.145362260348583,-0.0189321207373897,
0.817096127975007));
#13701=CARTESIAN_POINT('Ctrl Pts',(-0.146174510965348,-0.0126955988357878,
0.816752586844768));
#13702=CARTESIAN_POINT('Ctrl Pts',(-0.146545706411658,-0.00640163348415362,
0.81640904571453));
#13703=CARTESIAN_POINT('Ctrl Pts',(-0.146495788566881,-0.000101744904923998,
0.816065504584291));
#13704=CARTESIAN_POINT('Ctrl Pts',(-0.146473871348434,-0.000110945968026819,
0.808934495415711));
#13705=CARTESIAN_POINT('Ctrl Pts',(-0.146533950748007,-0.00724512552769256,
0.809323379784994));
#13706=CARTESIAN_POINT('Ctrl Pts',(-0.146057826922151,-0.0143712538186879,
0.809712264154277));
#13707=CARTESIAN_POINT('Ctrl Pts',(-0.145017839345608,-0.0214141189368497,
0.81010114852356));
#13708=CARTESIAN_POINT('Ctrl Pts',(-0.137937966054276,-0.0693594922943736,
0.81274853789782));
#13709=CARTESIAN_POINT('Ctrl Pts',(-0.104726321773939,-0.113446106932874,
0.81539592727208));
#13710=CARTESIAN_POINT('Ctrl Pts',(-0.0605955455659204,-0.133480028752914,
0.818043316646339));
#13711=CARTESIAN_POINT('Ctrl Pts',(-0.0164647693578984,-0.153513950572954,
0.820690706020599));
#13712=CARTESIAN_POINT('Ctrl Pts',(0.0385851387778066,-0.149495179574532,
0.823338095394859));
#13713=CARTESIAN_POINT('Ctrl Pts',(0.0793384931690736,-0.12326451930694,
0.825985484769119));
#13714=CARTESIAN_POINT('Ctrl Pts',(0.120091847560339,-0.0970338590393495,
0.828632874143379));
#13715=CARTESIAN_POINT('Ctrl Pts',(0.146548648207165,-0.0485913095025905,
0.83128026351764));
#13716=CARTESIAN_POINT('Ctrl Pts',(0.146590321408106,-0.000126046730599388,
0.833927652891899));
#13717=CARTESIAN_POINT('Ctrl Pts',(0.146631994609047,0.0483392160413931,
0.836575042266159));
#13718=CARTESIAN_POINT('Ctrl Pts',(0.120258540364101,0.0968271920486179,
0.839222431640419));
#13719=CARTESIAN_POINT('Ctrl Pts',(0.0795503554414038,0.123127897600245,
0.841869821014679));
#13720=CARTESIAN_POINT('Ctrl Pts',(0.0388421705187073,0.149428603151872,
0.844517210388939));
#13721=CARTESIAN_POINT('Ctrl Pts',(-0.0162007450817403,0.153542038247903,
0.8471645997632));
#13722=CARTESIAN_POINT('Ctrl Pts',(-0.0603659086281491,0.133584038319734,
0.84981198913746));
#13723=CARTESIAN_POINT('Ctrl Pts',(-0.104531072174558,0.113626038391565,
0.85245937851172));
#13724=CARTESIAN_POINT('Ctrl Pts',(-0.137818483666928,0.0695966034391962,
0.855106767885979));
#13725=CARTESIAN_POINT('Ctrl Pts',(-0.144980798768897,0.0216634763286692,
0.857754157260239));
#13726=CARTESIAN_POINT('Ctrl Pts',(-0.146045237806912,0.0145398171508471,
0.858147603312063));
#13727=CARTESIAN_POINT('Ctrl Pts',(-0.146532654486068,0.00732993751956911,
0.858541049363887));
#13728=CARTESIAN_POINT('Ctrl Pts',(-0.146471560192382,0.00011177640072981,
0.858934495415711));
#13729=CARTESIAN_POINT('Origin',(0.,0.,0.));
#13730=CARTESIAN_POINT('',(-0.146114231148477,2.69008449349656E-5,0.916065504584291));
#13731=CARTESIAN_POINT('',(-0.146121644853617,4.41067432152685E-5,0.908934495415711));
#13732=CARTESIAN_POINT('',(-0.14635,-1.79227059055215E-17,0.));
#13733=CARTESIAN_POINT('Ctrl Pts',(-0.146114231148477,2.69008449349656E-5,
0.916065504584291));
#13734=CARTESIAN_POINT('Ctrl Pts',(-0.146151635159142,0.0228038459942234,
0.914831670930419));
#13735=CARTESIAN_POINT('Ctrl Pts',(-0.141147538069067,0.0455652341090756,
0.913597837276548));
#13736=CARTESIAN_POINT('Ctrl Pts',(-0.131015765267123,0.0657531838068269,
0.912364003622676));
#13737=CARTESIAN_POINT('Ctrl Pts',(-0.109285110563454,0.109052354902802,
0.909717673743574));
#13738=CARTESIAN_POINT('Ctrl Pts',(-0.0639662294071284,0.140513248471977,
0.907071343864472));
#13739=CARTESIAN_POINT('Ctrl Pts',(-0.015802286694576,0.145735718560985,
0.90442501398537));
#13740=CARTESIAN_POINT('Ctrl Pts',(0.0323616560179757,0.150958188649994,
0.901778684106268));
#13741=CARTESIAN_POINT('Ctrl Pts',(0.0833706602867547,0.129942235258839,
0.899132354227166));
#13742=CARTESIAN_POINT('Ctrl Pts',(0.113877102345416,0.0923071908936453,
0.896486024348064));
#13743=CARTESIAN_POINT('Ctrl Pts',(0.144383544404078,0.0546721465284523,
0.893839694468962));
#13744=CARTESIAN_POINT('Ctrl Pts',(0.15438742425262,0.000418011189221586,
0.891193364589861));
#13745=CARTESIAN_POINT('Ctrl Pts',(0.139309808695705,-0.0456222438118789,
0.888547034710759));
#13746=CARTESIAN_POINT('Ctrl Pts',(0.124232193138789,-0.0916624988129813,
0.885900704831657));
#13747=CARTESIAN_POINT('Ctrl Pts',(0.0840730821764119,-0.129488873475953,
0.883254374952555));
#13748=CARTESIAN_POINT('Ctrl Pts',(0.0372139327097935,-0.141787641004198,
0.880608045073453));
#13749=CARTESIAN_POINT('Ctrl Pts',(-0.00964521675682358,-0.154086408532443,
0.877961715194351));
#13750=CARTESIAN_POINT('Ctrl Pts',(-0.0632044047276821,-0.140857568925962,
0.875315385315249));
#13751=CARTESIAN_POINT('Ctrl Pts',(-0.0989487482345592,-0.108156170198829,
0.872669055436147));
#13752=CARTESIAN_POINT('Ctrl Pts',(-0.128680439645858,-0.0809555616469925,
0.870467871818862));
#13753=CARTESIAN_POINT('Ctrl Pts',(-0.146086572253705,-0.0402824710322022,
0.868266688201576));
#13754=CARTESIAN_POINT('Ctrl Pts',(-0.146444331750498,0.000119944961782359,
0.866065504584291));
#13755=CARTESIAN_POINT('Ctrl Pts',(-0.146471560192382,0.00011177640072981,
0.858934495415711));
#13756=CARTESIAN_POINT('Ctrl Pts',(-0.146121567926216,-0.0412390669452651,
0.861188438738147));
#13757=CARTESIAN_POINT('Ctrl Pts',(-0.127770397964496,-0.0828616943330661,
0.863442382060584));
#13758=CARTESIAN_POINT('Ctrl Pts',(-0.096778382793969,-0.110103055552942,
0.86569632538302));
#13759=CARTESIAN_POINT('Ctrl Pts',(-0.0603764330055066,-0.142099641055337,
0.86834371475728));
#13760=CARTESIAN_POINT('Ctrl Pts',(-0.00653531471701479,-0.154255992791443,
0.870991104131539));
#13761=CARTESIAN_POINT('Ctrl Pts',(0.040082974241256,-0.14100387723139,
0.873638493505799));
#13762=CARTESIAN_POINT('Ctrl Pts',(0.0867012631995282,-0.127751761671338,
0.876285882880059));
#13763=CARTESIAN_POINT('Ctrl Pts',(0.12609672282758,-0.0890911788151255,
0.878933272254319));
#13764=CARTESIAN_POINT('Ctrl Pts',(0.140224208991091,-0.042730661487191,
0.88158066162858));
#13765=CARTESIAN_POINT('Ctrl Pts',(0.154351695154603,0.00362985584074295,
0.88422805100284));
#13766=CARTESIAN_POINT('Ctrl Pts',(0.143211207853577,0.057690307640398,
0.886875440377099));
#13767=CARTESIAN_POINT('Ctrl Pts',(0.111905662524754,0.09468823006692,0.889522829751359));
#13768=CARTESIAN_POINT('Ctrl Pts',(0.0806001171959318,0.131686152493442,
0.892170219125619));
#13769=CARTESIAN_POINT('Ctrl Pts',(0.0291295138393125,0.15162154554683,
0.894817608499879));
#13770=CARTESIAN_POINT('Ctrl Pts',(-0.0189299673197759,0.145362975188259,
0.897464997874139));
#13771=CARTESIAN_POINT('Ctrl Pts',(-0.0669894484788628,0.139104404829688,
0.9001123872484));
#13772=CARTESIAN_POINT('Ctrl Pts',(-0.11163780744042,0.10665187105916,0.902759776622659));
#13773=CARTESIAN_POINT('Ctrl Pts',(-0.132423802349956,0.0628703013313112,
0.905407165996919));
#13774=CARTESIAN_POINT('Ctrl Pts',(-0.141655418982822,0.043425734493323,
0.90658294246985));
#13775=CARTESIAN_POINT('Ctrl Pts',(-0.146180218154578,0.0217465313827003,
0.907758718942781));
#13776=CARTESIAN_POINT('Ctrl Pts',(-0.146121644853617,4.41067432152685E-5,
0.908934495415711));
#13777=CARTESIAN_POINT('Origin',(0.,0.,0.));
#13778=CARTESIAN_POINT('',(-0.146345621585321,-0.000133809880645736,0.966065504584291));
#13779=CARTESIAN_POINT('',(-0.146309694201085,-0.000133223314395004,0.958934495415711));
#13780=CARTESIAN_POINT('',(-0.14635,-1.79227059055215E-17,0.));
#13781=CARTESIAN_POINT('Ctrl Pts',(-0.146345621585321,-0.000133809880645736,
0.966065504584291));
#13782=CARTESIAN_POINT('Ctrl Pts',(-0.146004672532387,0.0370537288701324,
0.964042983538364));
#13783=CARTESIAN_POINT('Ctrl Pts',(-0.131578083002406,0.0744765756810296,
0.962020462492437));
#13784=CARTESIAN_POINT('Ctrl Pts',(-0.106003654037246,0.101251356830495,
0.959997941446511));
#13785=CARTESIAN_POINT('Ctrl Pts',(-0.0725412702228666,0.136284319036219,
0.957351611567409));
#13786=CARTESIAN_POINT('Ctrl Pts',(-0.0199938687303381,0.153087872523943,
0.954705281688306));
#13787=CARTESIAN_POINT('Ctrl Pts',(0.0275867780614433,0.143970766496025,
0.952058951809204));
#13788=CARTESIAN_POINT('Ctrl Pts',(0.0751674248532248,0.134853660468108,
0.949412621930102));
#13789=CARTESIAN_POINT('Ctrl Pts',(0.11778131694426,0.0998158949245492,
0.946766292051));
#13790=CARTESIAN_POINT('Ctrl Pts',(0.135923405490256,0.0548948063954655,
0.944119962171899));
#13791=CARTESIAN_POINT('Ctrl Pts',(0.154065494036253,0.0099737178663825,
0.941473632292797));
#13792=CARTESIAN_POINT('Ctrl Pts',(0.147735779037212,-0.0448306936482241,
0.938827302413695));
#13793=CARTESIAN_POINT('Ctrl Pts',(0.119831470632095,-0.0844335867733556,
0.936180972534593));
#13794=CARTESIAN_POINT('Ctrl Pts',(0.0919271622269763,-0.124036479898489,
0.933534642655491));
#13795=CARTESIAN_POINT('Ctrl Pts',(0.0424482604157787,-0.148437854634144,
0.93088831277639));
#13796=CARTESIAN_POINT('Ctrl Pts',(-0.00595796300272124,-0.146468817862788,
0.928241982897288));
#13797=CARTESIAN_POINT('Ctrl Pts',(-0.0543641864212212,-0.144499781091432,
0.925595653018186));
#13798=CARTESIAN_POINT('Ctrl Pts',(-0.101697731447024,-0.116160332813065,
0.922949323139084));
#13799=CARTESIAN_POINT('Ctrl Pts',(-0.126293289834417,-0.0744218843624929,
0.920302993259982));
#13800=CARTESIAN_POINT('Ctrl Pts',(-0.139421333187579,-0.052143709087005,
0.918890497034752));
#13801=CARTESIAN_POINT('Ctrl Pts',(-0.146071410932229,-0.0260482098028304,
0.917478000809521));
#13802=CARTESIAN_POINT('Ctrl Pts',(-0.146114231148477,2.69008449349656E-5,
0.916065504584291));
#13803=CARTESIAN_POINT('Ctrl Pts',(-0.146121644853617,4.41067432152685E-5,
0.908934495415711));
#13804=CARTESIAN_POINT('Ctrl Pts',(-0.146048333958771,-0.027118852224649,
0.910406108317041));
#13805=CARTESIAN_POINT('Ctrl Pts',(-0.138795050353101,-0.0543181883240968,
0.91187772121837));
#13806=CARTESIAN_POINT('Ctrl Pts',(-0.124603830013468,-0.0772180274565794,
0.9133493341197));
#13807=CARTESIAN_POINT('Ctrl Pts',(-0.0990742319099257,-0.118414180831446,
0.91599672349396));
#13808=CARTESIAN_POINT('Ctrl Pts',(-0.0510914048453256,-0.145695881896007,
0.91864411286822));
#13809=CARTESIAN_POINT('Ctrl Pts',(-0.00263394834681351,-0.146566710184873,
0.92129150224248));
#13810=CARTESIAN_POINT('Ctrl Pts',(0.0458235081516972,-0.147437538473739,
0.92393889161674));
#13811=CARTESIAN_POINT('Ctrl Pts',(0.0947555940841207,-0.121897493986912,
0.926586280990999));
#13812=CARTESIAN_POINT('Ctrl Pts',(0.121748900601314,-0.0816452290135895,
0.929233670365259));
#13813=CARTESIAN_POINT('Ctrl Pts',(0.148742207118509,-0.0413929640402651,
0.931881059739519));
#13814=CARTESIAN_POINT('Ctrl Pts',(0.153796734220472,0.0135715214195569,
0.93452844911378));
#13815=CARTESIAN_POINT('Ctrl Pts',(0.134597248858856,0.0580716696672091,
0.93717583848804));
#13816=CARTESIAN_POINT('Ctrl Pts',(0.115397763497239,0.102571817914861,
0.9398232278623));
#13817=CARTESIAN_POINT('Ctrl Pts',(0.0719442656720451,0.136607628950342,
0.942470617236559));
#13818=CARTESIAN_POINT('Ctrl Pts',(0.0241406894609324,0.144588953003544,
0.945118006610819));
#13819=CARTESIAN_POINT('Ctrl Pts',(-0.023662886750181,0.152570277056746,
0.947765395985079));
#13820=CARTESIAN_POINT('Ctrl Pts',(-0.0758165413472122,0.134497114127667,
0.950412785359339));
#13821=CARTESIAN_POINT('Ctrl Pts',(-0.108431221550465,0.0986479012011113,
0.953060174733599));
#13822=CARTESIAN_POINT('Ctrl Pts',(-0.132554242808212,0.0721325001574252,
0.955018281627637));
#13823=CARTESIAN_POINT('Ctrl Pts',(-0.145988218858404,0.0358924841874147,
0.956976388521674));
#13824=CARTESIAN_POINT('Ctrl Pts',(-0.146309694201085,-0.000133223314395004,
0.958934495415711));
#13825=CARTESIAN_POINT('Origin',(0.,0.,0.));
#13826=CARTESIAN_POINT('',(-0.146565171121453,5.44893591410845E-5,1.01606550458429));
#13827=CARTESIAN_POINT('',(-0.146582076026177,3.15354312248815E-5,1.00893449541571));
#13828=CARTESIAN_POINT('',(-0.14635,-1.79227059055215E-17,0.));
#13829=CARTESIAN_POINT('Ctrl Pts',(-0.146565171121453,5.44893591410845E-5,
1.01606550458429));
#13830=CARTESIAN_POINT('Ctrl Pts',(-0.146579596851449,0.00307427920823236,
1.01590062602541));
#13831=CARTESIAN_POINT('Ctrl Pts',(-0.146494352296349,0.00609323927190738,
1.01573574746653));
#13832=CARTESIAN_POINT('Ctrl Pts',(-0.146306854564556,0.00910583530985269,
1.01557086890765));
#13833=CARTESIAN_POINT('Ctrl Pts',(-0.143297482980539,0.0574585317612167,
1.01292453902855));
#13834=CARTESIAN_POINT('Ctrl Pts',(-0.11394685994478,0.104171803331984,
1.01027820914945));
#13835=CARTESIAN_POINT('Ctrl Pts',(-0.0716892273871119,0.127864250695428,
1.00763187927034));
#13836=CARTESIAN_POINT('Ctrl Pts',(-0.0294315948294418,0.151556698058874,
1.00498554939124));
#13837=CARTESIAN_POINT('Ctrl Pts',(0.0257330472501378,0.152228321214993,
1.00233921951214));
#13838=CARTESIAN_POINT('Ctrl Pts',(0.0685549742796134,0.129571707678744,
0.999692889633039));
#13839=CARTESIAN_POINT('Ctrl Pts',(0.111376901309088,0.106915094142495,
0.997046559753937));
#13840=CARTESIAN_POINT('Ctrl Pts',(0.141856113288459,0.0609302439138786,
0.994400229874835));
#13841=CARTESIAN_POINT('Ctrl Pts',(0.146041795372579,0.0126651464112397,
0.991753899995733));
#13842=CARTESIAN_POINT('Ctrl Pts',(0.150227477456699,-0.0355999510913994,
0.989107570116631));
#13843=CARTESIAN_POINT('Ctrl Pts',(0.128119629645567,-0.0861452958680607,
0.986461240237529));
#13844=CARTESIAN_POINT('Ctrl Pts',(0.0898373616998479,-0.115835488396583,
0.983814910358427));
#13845=CARTESIAN_POINT('Ctrl Pts',(0.051555093754129,-0.145525680925106,
0.981168580479325));
#13846=CARTESIAN_POINT('Ctrl Pts',(-0.00290159432617693,-0.154360721205491,
0.978522250600224));
#13847=CARTESIAN_POINT('Ctrl Pts',(-0.0486070196525971,-0.138296672301818,
0.975875920721122));
#13848=CARTESIAN_POINT('Ctrl Pts',(-0.0943124449790173,-0.122232623398145,
0.97322959084202));
#13849=CARTESIAN_POINT('Ctrl Pts',(-0.131266607551552,-0.081269485310415,
0.970583260962917));
#13850=CARTESIAN_POINT('Ctrl Pts',(-0.142555005769704,-0.0341567308046872,
0.967936931083816));
#13851=CARTESIAN_POINT('Ctrl Pts',(-0.145215975052668,-0.0230510282813687,
0.967313122250641));
#13852=CARTESIAN_POINT('Ctrl Pts',(-0.146450780951306,-0.0116036114945705,
0.966689313417466));
#13853=CARTESIAN_POINT('Ctrl Pts',(-0.146345621585321,-0.000133809880645736,
0.966065504584291));
#13854=CARTESIAN_POINT('Ctrl Pts',(-0.146309694201085,-0.000133223314395004,
0.958934495415711));
#13855=CARTESIAN_POINT('Ctrl Pts',(-0.146422858258782,-0.0128148032088542,
0.959623777895933));
#13856=CARTESIAN_POINT('Ctrl Pts',(-0.14491119500038,-0.0254698272036438,
0.960313060376156));
#13857=CARTESIAN_POINT('Ctrl Pts',(-0.141668994059001,-0.037664762585484,
0.961002342856379));
#13858=CARTESIAN_POINT('Ctrl Pts',(-0.129216380554811,-0.0845029505214961,
0.963649732230639));
#13859=CARTESIAN_POINT('Ctrl Pts',(-0.0912354477369537,-0.12455406346949,
0.966297121604899));
#13860=CARTESIAN_POINT('Ctrl Pts',(-0.0451234138007503,-0.1394726343957,
0.968944510979159));
#13861=CARTESIAN_POINT('Ctrl Pts',(0.00098862013545236,-0.154391205321909,
0.97159190035342));
#13862=CARTESIAN_POINT('Ctrl Pts',(0.055231755190001,-0.144177234226336,
0.974239289727679));
#13863=CARTESIAN_POINT('Ctrl Pts',(0.0927598492034174,-0.113509244531313,
0.976886679101939));
#13864=CARTESIAN_POINT('Ctrl Pts',(0.130287943216833,-0.0828412548362905,
0.979534068476199));
#13865=CARTESIAN_POINT('Ctrl Pts',(0.151100996189117,-0.0317192465418168,
0.982181457850459));
#13866=CARTESIAN_POINT('Ctrl Pts',(0.145665560755875,0.0164402745715088,
0.984828847224719));
#13867=CARTESIAN_POINT('Ctrl Pts',(0.140230125322634,0.0645997956848379,
0.987476236598979));
#13868=CARTESIAN_POINT('Ctrl Pts',(0.108546201483865,0.109796829617019,
0.990123625973239));
#13869=CARTESIAN_POINT('Ctrl Pts',(0.0651266538643092,0.131328813193254,
0.992771015347499));
#13870=CARTESIAN_POINT('Ctrl Pts',(0.0217071062447581,0.152860796769488,
0.995418404721759));
#13871=CARTESIAN_POINT('Ctrl Pts',(-0.0334480651555777,0.15072772998978,
0.998065794096019));
#13872=CARTESIAN_POINT('Ctrl Pts',(-0.0750749586823209,0.125906667008376,
1.00071318347028));
#13873=CARTESIAN_POINT('Ctrl Pts',(-0.116701852209067,0.101085604026969,
1.00336057284454));
#13874=CARTESIAN_POINT('Ctrl Pts',(-0.144800467862219,0.053576544843864,
1.0060079622188));
#13875=CARTESIAN_POINT('Ctrl Pts',(-0.146500196332402,0.00514107896046776,
1.00865535159306));
#13876=CARTESIAN_POINT('Ctrl Pts',(-0.146559936783033,0.00343871495990628,
1.00874839953394));
#13877=CARTESIAN_POINT('Ctrl Pts',(-0.146587066279139,0.00173520655478852,
1.00884144747483));
#13878=CARTESIAN_POINT('Ctrl Pts',(-0.146582076026177,3.15354312248815E-5,
1.00893449541571));
#13879=CARTESIAN_POINT('Origin',(0.,0.,0.));
#13880=CARTESIAN_POINT('',(-0.146184049129756,9.96948043307314E-5,1.06606550458429));
#13881=CARTESIAN_POINT('',(-0.146216477546812,0.000114345603752017,1.05893449541571));
#13882=CARTESIAN_POINT('',(-0.14635,-1.79227059055215E-17,0.));
#13883=CARTESIAN_POINT('Ctrl Pts',(-0.146184049129756,9.96948043307314E-5,
1.06606550458429));
#13884=CARTESIAN_POINT('Ctrl Pts',(-0.146294264763128,0.0176817746259609,
1.06511193863336));
#13885=CARTESIAN_POINT('Ctrl Pts',(-0.143360807533043,0.0352283113603788,
1.06415837268242));
#13886=CARTESIAN_POINT('Ctrl Pts',(-0.13721959397524,0.0515693218739058,
1.06320480673148));
#13887=CARTESIAN_POINT('Ctrl Pts',(-0.120176538991979,0.0969187854681546,
1.06055847685238));
#13888=CARTESIAN_POINT('Ctrl Pts',(-0.0784283132238915,0.132983650068601,
1.05791214697328));
#13889=CARTESIAN_POINT('Ctrl Pts',(-0.0310837364199337,0.143256459747686,
1.05526581709418));
#13890=CARTESIAN_POINT('Ctrl Pts',(0.0162608403840241,0.153529269426771,
1.05261948721508));
#13891=CARTESIAN_POINT('Ctrl Pts',(0.0692017682238519,0.138010024184496,
1.04997315733597));
#13892=CARTESIAN_POINT('Ctrl Pts',(0.103507151520239,0.103802126728842,
1.04732682745687));
#13893=CARTESIAN_POINT('Ctrl Pts',(0.137812534816628,0.0695942292731864,
1.04468049757777));
#13894=CARTESIAN_POINT('Ctrl Pts',(0.153482373569574,0.01669767960415,1.04203416769867));
#13895=CARTESIAN_POINT('Ctrl Pts',(0.143344336052008,-0.0306759392859165,
1.03938783781957));
#13896=CARTESIAN_POINT('Ctrl Pts',(0.133206298534443,-0.0780495581759789,
1.03674150794047));
#13897=CARTESIAN_POINT('Ctrl Pts',(0.0972603847463712,-0.119900246287072,
1.03409517806136));
#13898=CARTESIAN_POINT('Ctrl Pts',(0.0519596049571008,-0.137072285243832,
1.03144884818226));
#13899=CARTESIAN_POINT('Ctrl Pts',(0.00665882516783032,-0.154244324200591,
1.02880251830316));
#13900=CARTESIAN_POINT('Ctrl Pts',(-0.0479968206226384,-0.146737714003016,
1.02615618842406));
#13901=CARTESIAN_POINT('Ctrl Pts',(-0.0869905834517384,-0.11798834823825,
1.02350985854496));
#13902=CARTESIAN_POINT('Ctrl Pts',(-0.123554854979944,-0.0910302005802824,
1.02102840722473));
#13903=CARTESIAN_POINT('Ctrl Pts',(-0.146348061346918,-0.0453938791777224,
1.01854695590451));
#13904=CARTESIAN_POINT('Ctrl Pts',(-0.146565171121453,5.44893591410845E-5,
1.01606550458429));
#13905=CARTESIAN_POINT('Ctrl Pts',(-0.146582076026177,3.15354312248815E-5,
1.00893449541571));
#13906=CARTESIAN_POINT('Ctrl Pts',(-0.146445084172466,-0.0467374494427972,
1.01148883684909));
#13907=CARTESIAN_POINT('Ctrl Pts',(-0.122102455869861,-0.0936290599181376,
1.01404317828246));
#13908=CARTESIAN_POINT('Ctrl Pts',(-0.0837162036049941,-0.120334265578335,
1.01659751971584));
#13909=CARTESIAN_POINT('Ctrl Pts',(-0.0439316411201867,-0.14801227165006,
1.0192449090901));
#13910=CARTESIAN_POINT('Ctrl Pts',(0.0109383251366414,-0.154006411209824,
1.02189229846436));
#13911=CARTESIAN_POINT('Ctrl Pts',(0.0557604321169594,-0.135571060438576,
1.02453968783862));
#13912=CARTESIAN_POINT('Ctrl Pts',(0.100582539097277,-0.11713570966733,
1.02718707721288));
#13913=CARTESIAN_POINT('Ctrl Pts',(0.135356786801084,-0.0742708685650716,
1.02983446658714));
#13914=CARTESIAN_POINT('Ctrl Pts',(0.144154783532934,-0.0266108361928598,
1.0324818559614));
#13915=CARTESIAN_POINT('Ctrl Pts',(0.152952780264784,0.0210491961793507,
1.03512924533566));
#13916=CARTESIAN_POINT('Ctrl Pts',(0.135774526024679,0.0735044198215165,
1.03777663470992));
#13917=CARTESIAN_POINT('Ctrl Pts',(0.100488543649143,0.106727647840587,
1.04042402408418));
#13918=CARTESIAN_POINT('Ctrl Pts',(0.0652025612736062,0.139950875859659,
1.04307141345844));
#13919=CARTESIAN_POINT('Ctrl Pts',(0.0118088507626404,0.153942108255635,
1.0457188028327));
#13920=CARTESIAN_POINT('Ctrl Pts',(-0.0352355257975899,0.142292641904202,
1.04836619220696));
#13921=CARTESIAN_POINT('Ctrl Pts',(-0.0822799023578202,0.130643175552769,
1.05101358158122));
#13922=CARTESIAN_POINT('Ctrl Pts',(-0.122974944967313,0.0933530104539243,
1.05366097095548));
#13923=CARTESIAN_POINT('Ctrl Pts',(-0.138680233730631,0.0475029577050484,
1.05630836032974));
#13924=CARTESIAN_POINT('Ctrl Pts',(-0.143873300563147,0.0323423075707214,
1.05718373869173));
#13925=CARTESIAN_POINT('Ctrl Pts',(-0.146334133026589,0.0162457690968458,
1.05805911705372));
#13926=CARTESIAN_POINT('Ctrl Pts',(-0.146216477546812,0.000114345603752017,
1.05893449541571));
#13927=CARTESIAN_POINT('Origin',(0.,0.,0.));
#13928=CARTESIAN_POINT('',(-0.146204073634541,-0.000109175101205505,1.11606550458429));
#13929=CARTESIAN_POINT('',(-0.146170555016798,-9.22629125885076E-5,1.10893449541571));
#13930=CARTESIAN_POINT('',(-0.14635,-1.79227059055215E-17,0.));
#13931=CARTESIAN_POINT('Ctrl Pts',(-0.146204073634541,-0.000109175101205505,
1.11606550458429));
#13932=CARTESIAN_POINT('Ctrl Pts',(-0.145981599624502,0.032003853555373,
1.1143232512413));
#13933=CARTESIAN_POINT('Ctrl Pts',(-0.135565881201595,0.0642480963468658,
1.11258099789831));
#13934=CARTESIAN_POINT('Ctrl Pts',(-0.11609067353381,0.0895073597405865,
1.11083874455532));
#13935=CARTESIAN_POINT('Ctrl Pts',(-0.0865095427755784,0.127873963375947,
1.10819241467622));
#13936=CARTESIAN_POINT('Ctrl Pts',(-0.0360273159486943,0.150125560802435,
1.10554608479712));
#13937=CARTESIAN_POINT('Ctrl Pts',(0.0122494975033169,0.14607724579886,
1.10289975491801));
#13938=CARTESIAN_POINT('Ctrl Pts',(0.0605263109553308,0.142028930795284,
1.10025342503891));
#13939=CARTESIAN_POINT('Ctrl Pts',(0.10659771103247,0.111680703361642,1.09760709515981));
#13940=CARTESIAN_POINT('Ctrl Pts',(0.129376093089052,0.0689234246557527,
1.09496076528071));
#13941=CARTESIAN_POINT('Ctrl Pts',(0.152154475145634,0.0261661459498645,
1.09231443540161));
#13942=CARTESIAN_POINT('Ctrl Pts',(0.151639839181659,-0.0290001840282729,
1.0896681055225));
#13943=CARTESIAN_POINT('Ctrl Pts',(0.128067742174483,-0.0713250681289163,
1.0870217756434));
#13944=CARTESIAN_POINT('Ctrl Pts',(0.104495645167307,-0.11364995222956,
1.0843754457643));
#13945=CARTESIAN_POINT('Ctrl Pts',(0.0578660871169326,-0.143133390452712,
1.0817291158852));
#13946=CARTESIAN_POINT('Ctrl Pts',(0.00952215035475689,-0.146280349267719,
1.0790827860061));
#13947=CARTESIAN_POINT('Ctrl Pts',(-0.0388217864074202,-0.149427308082725,
1.07643645612699));
#13948=CARTESIAN_POINT('Ctrl Pts',(-0.0888801018813974,-0.126237787489585,
1.07379012624789));
#13949=CARTESIAN_POINT('Ctrl Pts',(-0.117740317519168,-0.0873259958989869,
1.07114379636879));
#13950=CARTESIAN_POINT('Ctrl Pts',(-0.136201180005177,-0.0624354946409797,
1.06945103244062));
#13951=CARTESIAN_POINT('Ctrl Pts',(-0.145988395071105,-0.0311118962502767,
1.06775826851246));
#13952=CARTESIAN_POINT('Ctrl Pts',(-0.146184049129756,9.96948043307314E-5,
1.06606550458429));
#13953=CARTESIAN_POINT('Ctrl Pts',(-0.146216477546812,0.000114345603752017,
1.05893449541571));
#13954=CARTESIAN_POINT('Ctrl Pts',(-0.145978309898544,-0.0325401742182177,
1.06070650642798));
#13955=CARTESIAN_POINT('Ctrl Pts',(-0.135174246449945,-0.06533764273189,
1.06247851744025));
#13956=CARTESIAN_POINT('Ctrl Pts',(-0.115079600404687,-0.0908043159161929,
1.06425052845252));
#13957=CARTESIAN_POINT('Ctrl Pts',(-0.0850581433982766,-0.128851596389654,
1.06689791782678));
#13958=CARTESIAN_POINT('Ctrl Pts',(-0.0342996944683099,-0.150536216937668,
1.06954530720104));
#13959=CARTESIAN_POINT('Ctrl Pts',(0.0139457694684962,-0.145925507476389,
1.0721926965753));
#13960=CARTESIAN_POINT('Ctrl Pts',(0.0621912334052997,-0.14131479801511,
1.07484008594956));
#13961=CARTESIAN_POINT('Ctrl Pts',(0.107923712348941,-0.110408758544542,
1.07748747532382));
#13962=CARTESIAN_POINT('Ctrl Pts',(0.1301953818052,-0.0673639426912374,
1.08013486469808));
#13963=CARTESIAN_POINT('Ctrl Pts',(0.15246705126146,-0.024319126837932,
1.08278225407234));
#13964=CARTESIAN_POINT('Ctrl Pts',(0.151277911230334,0.0308644653981125,
1.0854296434466));
#13965=CARTESIAN_POINT('Ctrl Pts',(0.127172648928576,0.0729099141598672,
1.08807703282086));
#13966=CARTESIAN_POINT('Ctrl Pts',(0.103067386626818,0.114955362921624,
1.09072442219512));
#13967=CARTESIAN_POINT('Ctrl Pts',(0.0560460020544268,0.143862668209093,
1.09337181156938));
#13968=CARTESIAN_POINT('Ctrl Pts',(0.00764670469074742,0.146390799320458,
1.09601920094364));
#13969=CARTESIAN_POINT('Ctrl Pts',(-0.0407525926729279,0.148918930431823,
1.0986665903179));
#13970=CARTESIAN_POINT('Ctrl Pts',(-0.0905298028278899,0.125067887367091,
1.10131397969216));
#13971=CARTESIAN_POINT('Ctrl Pts',(-0.11888440661962,0.0857626730052823,
1.10396136906642));
#13972=CARTESIAN_POINT('Ctrl Pts',(-0.136639133674055,0.0611510311732957,
1.10561907784952));
#13973=CARTESIAN_POINT('Ctrl Pts',(-0.145994366384503,0.0304800321277272,
1.10727678663261));
#13974=CARTESIAN_POINT('Ctrl Pts',(-0.146170555016798,-9.22629125885076E-5,
1.10893449541571));
#13975=CARTESIAN_POINT('Origin',(0.,0.,0.));
#13976=CARTESIAN_POINT('',(-0.146577386142569,-3.88073511912723E-5,1.16606550458429));
#13977=CARTESIAN_POINT('',(-0.146552328192774,-6.73160170860698E-5,1.15893449541571));
#13978=CARTESIAN_POINT('',(-0.14635,-1.79227059055215E-17,0.));
#13979=CARTESIAN_POINT('Ctrl Pts',(-0.146577386142569,-3.88073511912723E-5,
1.16606550458429));
#13980=CARTESIAN_POINT('Ctrl Pts',(-0.146413350709018,0.0463056768050285,
1.16353456384924));
#13981=CARTESIAN_POINT('Ctrl Pts',(-0.122574225104448,0.0927954474992645,
1.1610036231142));
#13982=CARTESIAN_POINT('Ctrl Pts',(-0.0847742546295189,0.119590709008994,
1.15847268237915));
#13983=CARTESIAN_POINT('Ctrl Pts',(-0.0452509303920754,0.147607604138013,
1.15582635250005));
#13984=CARTESIAN_POINT('Ctrl Pts',(0.00953524646069181,0.154093252855687,
1.15318002262095));
#13985=CARTESIAN_POINT('Ctrl Pts',(0.0545077808453859,0.136079071706768,
1.15053369274185));
#13986=CARTESIAN_POINT('Ctrl Pts',(0.0994803152300801,0.118064890557849,
1.14788736286275));
#13987=CARTESIAN_POINT('Ctrl Pts',(0.134639207146701,0.0755508795423365,
1.14524103298364));
#13988=CARTESIAN_POINT('Ctrl Pts',(0.14389167861853,0.027996370364851,1.14259470310454));
#13989=CARTESIAN_POINT('Ctrl Pts',(0.15314415009036,-0.0195581388126345,
1.13994837322544));
#13990=CARTESIAN_POINT('Ctrl Pts',(0.136490201117397,-0.0721531461520931,
1.13730204334634));
#13991=CARTESIAN_POINT('Ctrl Pts',(0.101552606157185,-0.105715089329518,
1.13465571346724));
#13992=CARTESIAN_POINT('Ctrl Pts',(0.0666150111969725,-0.139277032506943,
1.13200938358813));
#13993=CARTESIAN_POINT('Ctrl Pts',(0.0133937702495101,-0.153805911522335,
1.12936305370903));
#13994=CARTESIAN_POINT('Ctrl Pts',(-0.033750917386428,-0.142651629870951,
1.12671672382993));
#13995=CARTESIAN_POINT('Ctrl Pts',(-0.0808956050223675,-0.131497348219567,
1.12407039395083));
#13996=CARTESIAN_POINT('Ctrl Pts',(-0.121963739346782,-0.094659905901407,
1.12142406407173));
#13997=CARTESIAN_POINT('Ctrl Pts',(-0.1381577891642,-0.0490003798202082,
1.11877773419262));
#13998=CARTESIAN_POINT('Ctrl Pts',(-0.143690228857438,-0.0334015285560649,
1.11787365765651));
#13999=CARTESIAN_POINT('Ctrl Pts',(-0.146319518115206,-0.0167730178360648,
1.1169695811204));
#14000=CARTESIAN_POINT('Ctrl Pts',(-0.146204073634541,-0.000109175101205505,
1.11606550458429));
#14001=CARTESIAN_POINT('Ctrl Pts',(-0.146170555016798,-9.22629125885076E-5,
1.10893449541571));
#14002=CARTESIAN_POINT('Ctrl Pts',(-0.146275742653821,-0.0183444476975235,
1.10992417600687));
#14003=CARTESIAN_POINT('Ctrl Pts',(-0.143109248288425,-0.0365614514641733,
1.11091385659804));
#14004=CARTESIAN_POINT('Ctrl Pts',(-0.136505188007283,-0.0534328725168923,
1.1119035371892));
#14005=CARTESIAN_POINT('Ctrl Pts',(-0.118839368174718,-0.0985638180183679,
1.11455092656346));
#14006=CARTESIAN_POINT('Ctrl Pts',(-0.0765757310810901,-0.134066323362434,
1.11719831593772));
#14007=CARTESIAN_POINT('Ctrl Pts',(-0.0290731934694857,-0.143678417446031,
1.11984570531198));
#14008=CARTESIAN_POINT('Ctrl Pts',(0.01842934414212,-0.153290511529629,
1.12249309468624));
#14009=CARTESIAN_POINT('Ctrl Pts',(0.071170782271703,-0.137012194352758,
1.1251404840605));
#14010=CARTESIAN_POINT('Ctrl Pts',(0.10499283308901,-0.102299771349957,
1.12778787343476));
#14011=CARTESIAN_POINT('Ctrl Pts',(0.138814883906317,-0.0675873483471558,
1.13043526280902));
#14012=CARTESIAN_POINT('Ctrl Pts',(0.153717547411349,-0.0144408195184256,
1.13308265218328));
#14013=CARTESIAN_POINT('Ctrl Pts',(0.142874638214406,0.0327959749574983,
1.13573004155754));
#14014=CARTESIAN_POINT('Ctrl Pts',(0.132031729017462,0.0800327694334235,
1.1383774309318));
#14015=CARTESIAN_POINT('Ctrl Pts',(0.0954432471185425,0.121359829556542,
1.14102482030606));
#14016=CARTESIAN_POINT('Ctrl Pts',(0.0498685966661331,0.137847238945365,
1.14367220968032));
#14017=CARTESIAN_POINT('Ctrl Pts',(0.00429394621372511,0.154334648334189,
1.14631959905458));
#14018=CARTESIAN_POINT('Ctrl Pts',(-0.0502668727921719,0.145982406988718,
1.14896698842884));
#14019=CARTESIAN_POINT('Ctrl Pts',(-0.0888222026239048,0.116616270474356,
1.1516143778031));
#14020=CARTESIAN_POINT('Ctrl Pts',(-0.124357782404925,0.0895501633622979,
1.1540544170073));
#14021=CARTESIAN_POINT('Ctrl Pts',(-0.146296868742479,0.0446329749882746,
1.15649445621151));
#14022=CARTESIAN_POINT('Ctrl Pts',(-0.146552328192774,-6.73160170860698E-5,
1.15893449541571));
#14023=CARTESIAN_POINT('Origin',(0.,0.,0.));
#14024=CARTESIAN_POINT('',(-0.146318311025392,0.000133437649768732,1.21606550458429));
#14025=CARTESIAN_POINT('',(-0.146373054956946,0.000132657382717961,1.20893449541571));
#14026=CARTESIAN_POINT('',(-0.14635,-1.79227059055215E-17,0.));
#14027=CARTESIAN_POINT('Ctrl Pts',(-0.146318311025392,0.000133437649768732,
1.21606550458429));
#14028=CARTESIAN_POINT('Ctrl Pts',(-0.146429658069886,0.0125190846592594,
1.21539220633629));
#14029=CARTESIAN_POINT('Ctrl Pts',(-0.144988168643405,0.0248791929292086,
1.21471890808829));
#14030=CARTESIAN_POINT('Ctrl Pts',(-0.141892968227885,0.0368102906365087,
1.21404560984029));
#14031=CARTESIAN_POINT('Ctrl Pts',(-0.129727599662405,0.083704249513052,
1.21139927996119));
#14032=CARTESIAN_POINT('Ctrl Pts',(-0.0920156607298113,0.123970842060419,
1.20875295008209));
#14033=CARTESIAN_POINT('Ctrl Pts',(-0.0460184991925076,0.139179415364965,
1.20610662020299));
#14034=CARTESIAN_POINT('Ctrl Pts',(-2.13376552038805E-5,0.15438798866951,
1.20346029032389));
#14035=CARTESIAN_POINT('Ctrl Pts',(0.0542610464868107,0.144538542731236,
1.20081396044478));
#14036=CARTESIAN_POINT('Ctrl Pts',(0.091982751999895,0.114139323915075,
1.19816763056568));
#14037=CARTESIAN_POINT('Ctrl Pts',(0.129704457512977,0.0837401050989159,
1.19552130068658));
#14038=CARTESIAN_POINT('Ctrl Pts',(0.150865484397133,0.0327911134048729,
1.19287497080748));
#14039=CARTESIAN_POINT('Ctrl Pts',(0.145780097726084,-0.0153874961003253,
1.19022864092838));
#14040=CARTESIAN_POINT('Ctrl Pts',(0.140694711055036,-0.063566105605525,
1.18758231104927));
#14041=CARTESIAN_POINT('Ctrl Pts',(0.109362910828785,-0.108974332921877,
1.18493598117017));
#14042=CARTESIAN_POINT('Ctrl Pts',(0.0661257549466402,-0.130828118009858,
1.18228965129107));
#14043=CARTESIAN_POINT('Ctrl Pts',(0.0228885990644955,-0.152681903097838,
1.17964332141197));
#14044=CARTESIAN_POINT('Ctrl Pts',(-0.0322539124735426,-0.150981245957443,
1.17699699153287));
#14045=CARTESIAN_POINT('Ctrl Pts',(-0.0740621845924981,-0.126504564117865,
1.17435066165376));
#14046=CARTESIAN_POINT('Ctrl Pts',(-0.115870456711455,-0.102027882278287,
1.17170433177466));
#14047=CARTESIAN_POINT('Ctrl Pts',(-0.144344489411329,-0.0547751757395235,
1.16905800189556));
#14048=CARTESIAN_POINT('Ctrl Pts',(-0.146451269950206,-0.00637475169995868,
1.16641167201646));
#14049=CARTESIAN_POINT('Ctrl Pts',(-0.146543132875163,-0.00426432565444621,
1.1662962828724));
#14050=CARTESIAN_POINT('Ctrl Pts',(-0.146584864748453,-0.00215171749738942,
1.16618089372835));
#14051=CARTESIAN_POINT('Ctrl Pts',(-0.146577386142569,-3.88073511912723E-5,
1.16606550458429));
#14052=CARTESIAN_POINT('Ctrl Pts',(-0.146552328192774,-6.73160170860698E-5,
1.15893449541571));
#14053=CARTESIAN_POINT('Ctrl Pts',(-0.146574036680232,-0.00386586684592084,
1.15914184558577));
#14054=CARTESIAN_POINT('Ctrl Pts',(-0.1464391612665,-0.00766285139452399,
1.15934919575582));
#14055=CARTESIAN_POINT('Ctrl Pts',(-0.146142739258869,-0.0114471821958193,
1.15955654592588));
#14056=CARTESIAN_POINT('Ctrl Pts',(-0.142358105404532,-0.0597644666683822,
1.16220393530014));
#14057=CARTESIAN_POINT('Ctrl Pts',(-0.112238997038288,-0.106019003930254,
1.1648513246744));
#14058=CARTESIAN_POINT('Ctrl Pts',(-0.0695815129186611,-0.129023839960917,
1.16749871404866));
#14059=CARTESIAN_POINT('Ctrl Pts',(-0.026924028799035,-0.15202867599158,
1.17014610342292));
#14060=CARTESIAN_POINT('Ctrl Pts',(0.0282718310739737,-0.151783810791035,
1.17279349279718));
#14061=CARTESIAN_POINT('Ctrl Pts',(0.0707235276354612,-0.128401405199111,
1.17544088217144));
#14062=CARTESIAN_POINT('Ctrl Pts',(0.11317522419695,-0.105018999607187,
1.1780882715457));
#14063=CARTESIAN_POINT('Ctrl Pts',(0.142882757446916,-0.0584990536238821,
1.18073566091996));
#14064=CARTESIAN_POINT('Ctrl Pts',(0.146238551171451,-0.0101500920973681,
1.18338305029422));
#14065=CARTESIAN_POINT('Ctrl Pts',(0.149594344895986,0.0381988694291446,
1.18603043966848));
#14066=CARTESIAN_POINT('Ctrl Pts',(0.12659839909509,0.0883768464988665,
1.18867782904274));
#14067=CARTESIAN_POINT('Ctrl Pts',(0.0877840381772113,0.117399748124142,
1.191325218417));
#14068=CARTESIAN_POINT('Ctrl Pts',(0.0489696772593311,0.146422649749419,
1.19397260779126));
#14069=CARTESIAN_POINT('Ctrl Pts',(-0.00566309877553352,0.154290475930249,
1.19661999716552));
#14070=CARTESIAN_POINT('Ctrl Pts',(-0.0510896721842483,0.137399358129564,
1.19926738653978));
#14071=CARTESIAN_POINT('Ctrl Pts',(-0.0965162455929618,0.12050824032888,
1.20191477591404));
#14072=CARTESIAN_POINT('Ctrl Pts',(-0.132736616375526,0.0788581785466829,
1.2045621652883));
#14073=CARTESIAN_POINT('Ctrl Pts',(-0.143159994183491,0.0315270405159292,
1.20720955466256));
#14074=CARTESIAN_POINT('Ctrl Pts',(-0.145423823013163,0.021247302336111,
1.20778453491361));
#14075=CARTESIAN_POINT('Ctrl Pts',(-0.146470795531708,0.0106995851133921,
1.20835951516466));
#14076=CARTESIAN_POINT('Ctrl Pts',(-0.146373054956946,0.000132657382717961,
1.20893449541571));
#14077=CARTESIAN_POINT('Origin',(0.,0.,0.));
#14078=CARTESIAN_POINT('',(-0.146120596765396,-4.14129048147555E-5,1.26606550458429));
#14079=CARTESIAN_POINT('',(-0.146109918970638,-1.0198006988139E-5,1.25893449541571));
#14080=CARTESIAN_POINT('',(-0.14635,-1.79227059055215E-17,0.));
#14081=CARTESIAN_POINT('Ctrl Pts',(-0.146120596765396,-4.14129048147555E-5,
1.26606550458429));
#14082=CARTESIAN_POINT('Ctrl Pts',(-0.14605219935785,0.0269443530192317,
1.26460351894424));
#14083=CARTESIAN_POINT('Ctrl Pts',(-0.138898723445843,0.053963836666407,
1.26314153330418));
#14084=CARTESIAN_POINT('Ctrl Pts',(-0.124882896249422,0.0767650581554474,
1.26167954766413));
#14085=CARTESIAN_POINT('Ctrl Pts',(-0.0995129464537159,0.118037388097231,
1.25903321778503));
#14086=CARTESIAN_POINT('Ctrl Pts',(-0.051658938874944,0.145488850208621,
1.25638688790592));
#14087=CARTESIAN_POINT('Ctrl Pts',(-0.00322440565727106,0.146554478394238,
1.25374055802682));
#14088=CARTESIAN_POINT('Ctrl Pts',(0.0452101275604033,0.147620106579856,
1.25109422814772));
#14089=CARTESIAN_POINT('Ctrl Pts',(0.0942251864169787,0.122299900839699,
1.24844789826862));
#14090=CARTESIAN_POINT('Ctrl Pts',(0.121385807331354,0.0821833176976391,
1.24580156838952));
#14091=CARTESIAN_POINT('Ctrl Pts',(0.148546428245729,0.0420667345555804,
1.24315523851041));
#14092=CARTESIAN_POINT('Ctrl Pts',(0.153852611217905,-0.0128462259883804,
1.24050890863131));
#14093=CARTESIAN_POINT('Ctrl Pts',(0.134875632820701,-0.0574210379606392,
1.23786257875221));
#14094=CARTESIAN_POINT('Ctrl Pts',(0.115898654423498,-0.101995849932898,
1.23521624887311));
#14095=CARTESIAN_POINT('Ctrl Pts',(0.0726385146569148,-0.136232513333455,
1.23256991899401));
#14096=CARTESIAN_POINT('Ctrl Pts',(0.0248960600935515,-0.144460368686643,
1.2299235891149));
#14097=CARTESIAN_POINT('Ctrl Pts',(-0.0228463944698117,-0.152688224039831,
1.2272772592358));
#14098=CARTESIAN_POINT('Ctrl Pts',(-0.0750711638299551,-0.134907271345651,
1.2246309293567));
#14099=CARTESIAN_POINT('Ctrl Pts',(-0.107874149410843,-0.0992561323957017,
1.2219845994776));
#14100=CARTESIAN_POINT('Ctrl Pts',(-0.132331163880887,-0.072675612185966,
1.2200115678465));
#14101=CARTESIAN_POINT('Ctrl Pts',(-0.145992019903337,-0.0361614337449312,
1.21803853621539));
#14102=CARTESIAN_POINT('Ctrl Pts',(-0.146318311025392,0.000133437649768732,
1.21606550458429));
#14103=CARTESIAN_POINT('Ctrl Pts',(-0.146373054956946,0.000132657382717961,
1.20893449541571));
#14104=CARTESIAN_POINT('Ctrl Pts',(-0.146020767276673,-0.0379538636644633,
1.21100690453892));
#14105=CARTESIAN_POINT('Ctrl Pts',(-0.130797424420382,-0.0762899498869128,
1.21307931366213));
#14106=CARTESIAN_POINT('Ctrl Pts',(-0.104081054125652,-0.103227285106232,
1.21515172278534));
#14107=CARTESIAN_POINT('Ctrl Pts',(-0.0699523514264828,-0.137638258418326,
1.2177991121596));
#14108=CARTESIAN_POINT('Ctrl Pts',(-0.0170685611947798,-0.153447990763203,
1.22044650153386));
#14109=CARTESIAN_POINT('Ctrl Pts',(0.0303468241642401,-0.143414812629152,
1.22309389090812));
#14110=CARTESIAN_POINT('Ctrl Pts',(0.0777622095232573,-0.133381634495101,
1.22574128028238));
#14111=CARTESIAN_POINT('Ctrl Pts',(0.119709190009594,-0.0975055458821257,
1.22838866965664));
#14112=CARTESIAN_POINT('Ctrl Pts',(0.136973893871985,-0.052219638220276,
1.2310360590309));
#14113=CARTESIAN_POINT('Ctrl Pts',(0.154238597734379,-0.00693373055842239,
1.23368344840516));
#14114=CARTESIAN_POINT('Ctrl Pts',(0.146821024972825,0.0477619961523044,
1.23633083777942));
#14115=CARTESIAN_POINT('Ctrl Pts',(0.118118804930222,0.0868140895256425,
1.23897822715368));
#14116=CARTESIAN_POINT('Ctrl Pts',(0.0894165848876198,0.125866182898978,
1.24162561652794));
#14117=CARTESIAN_POINT('Ctrl Pts',(0.0394297175639698,0.149274642934924,
1.2442730059022));
#14118=CARTESIAN_POINT('Ctrl Pts',(-0.00894524413350711,0.146317192515786,
1.24692039527646));
#14119=CARTESIAN_POINT('Ctrl Pts',(-0.0573202058309854,0.143359742096648,
1.24956778465072));
#14120=CARTESIAN_POINT('Ctrl Pts',(-0.104083261902292,0.114036381222425,
1.25221517402498));
#14121=CARTESIAN_POINT('Ctrl Pts',(-0.127814530591109,0.0717787154251623,
1.25486256339924));
#14122=CARTESIAN_POINT('Ctrl Pts',(-0.139981499518435,0.0501133037087236,
1.2562198740714));
#14123=CARTESIAN_POINT('Ctrl Pts',(-0.146094355379323,0.0250479932723348,
1.25757718474355));
#14124=CARTESIAN_POINT('Ctrl Pts',(-0.146109918970638,-1.0198006988139E-5,
1.25893449541571));
#14125=CARTESIAN_POINT('Origin',(0.,0.,0.));
#14126=CARTESIAN_POINT('',(-0.146470135615938,-0.000111966546850736,1.31606550458429));
#14127=CARTESIAN_POINT('',(-0.146410535958061,-0.000127756381200432,1.30893449541571));
#14128=CARTESIAN_POINT('',(-0.14635,-1.79227059055215E-17,0.));
#14129=CARTESIAN_POINT('Ctrl Pts',(-0.146470135615938,-0.000111966546850736,
1.31606550458429));
#14130=CARTESIAN_POINT('Ctrl Pts',(-0.146120207411574,0.0411799307449602,
1.31381483155218));
#14131=CARTESIAN_POINT('Ctrl Pts',(-0.127827491572984,0.0827431563937987,
1.31156415852007));
#14132=CARTESIAN_POINT('Ctrl Pts',(-0.0969137672218927,0.10998333351997,
1.30931348548796));
#14133=CARTESIAN_POINT('Ctrl Pts',(-0.0605655677022408,0.142012194937238,
1.30666715560886));
#14134=CARTESIAN_POINT('Ctrl Pts',(-0.00676890401288169,0.154239532672684,
1.30402082572976));
#14135=CARTESIAN_POINT('Ctrl Pts',(0.0398526445220406,0.14106870189023,
1.30137449585066));
#14136=CARTESIAN_POINT('Ctrl Pts',(0.0864741930569617,0.127897871107775,
1.29872816597155));
#14137=CARTESIAN_POINT('Ctrl Pts',(0.125920626437448,0.0893288718074177,
1.29608183609245));
#14138=CARTESIAN_POINT('Ctrl Pts',(0.14013669149516,0.0430153417578024,
1.29343550621335));
#14139=CARTESIAN_POINT('Ctrl Pts',(0.154352756552873,-0.00329818829181684,
1.29078917633425));
#14140=CARTESIAN_POINT('Ctrl Pts',(0.143338453287813,-0.0573562490906975,
1.28814284645515));
#14141=CARTESIAN_POINT('Ctrl Pts',(0.112135201594409,-0.0944156157243562,
1.28549651657604));
#14142=CARTESIAN_POINT('Ctrl Pts',(0.0809319499010078,-0.131474982358013,
1.28285018669694));
#14143=CARTESIAN_POINT('Ctrl Pts',(0.0295397497792676,-0.151535654826449,
1.28020385681784));
#14144=CARTESIAN_POINT('Ctrl Pts',(-0.0185183802362589,-0.1454155477333,
1.27755752693874));
#14145=CARTESIAN_POINT('Ctrl Pts',(-0.066576510251784,-0.139295440640151,
1.27491119705964));
#14146=CARTESIAN_POINT('Ctrl Pts',(-0.111300570161094,-0.106994553985419,
1.27226486718053));
#14147=CARTESIAN_POINT('Ctrl Pts',(-0.13221965410943,-0.0632975117719662,
1.26961853730143));
#14148=CARTESIAN_POINT('Ctrl Pts',(-0.141581826511298,-0.0437412423069929,
1.26843419306239));
#14149=CARTESIAN_POINT('Ctrl Pts',(-0.146176005022067,-0.0219023912433209,
1.26724984882334));
#14150=CARTESIAN_POINT('Ctrl Pts',(-0.146120596765396,-4.14129048147555E-5,
1.26606550458429));
#14151=CARTESIAN_POINT('Ctrl Pts',(-0.146109918970638,-1.0198006988139E-5,
1.25893449541571));
#14152=CARTESIAN_POINT('Ctrl Pts',(-0.146124711647138,-0.0238271763493914,
1.26022457411781));
#14153=CARTESIAN_POINT('Ctrl Pts',(-0.140631289159497,-0.0476377233371588,
1.26151465281992));
#14154=CARTESIAN_POINT('Ctrl Pts',(-0.129592576141605,-0.0685164391025303,
1.26280473152202));
#14155=CARTESIAN_POINT('Ctrl Pts',(-0.106939871696956,-0.111361957112663,
1.26545212089628));
#14156=CARTESIAN_POINT('Ctrl Pts',(-0.0609349815013302,-0.141861022412626,
1.26809951027054));
#14157=CARTESIAN_POINT('Ctrl Pts',(-0.0126505083952331,-0.146043496451057,
1.2707468996448));
#14158=CARTESIAN_POINT('Ctrl Pts',(0.0356339647108625,-0.150225970489488,
1.27339428901906));
#14159=CARTESIAN_POINT('Ctrl Pts',(0.0861980207274291,-0.128091853266388,
1.27604167839332));
#14160=CARTESIAN_POINT('Ctrl Pts',(0.11588072467734,-0.0897797074320025,
1.27868906776758));
#14161=CARTESIAN_POINT('Ctrl Pts',(0.145563428627253,-0.0514675615976161,
1.28133645714184));
#14162=CARTESIAN_POINT('Ctrl Pts',(0.154364780510509,0.00302261284805656,
1.2839838465161));
#14163=CARTESIAN_POINT('Ctrl Pts',(0.138253309066183,0.0487315170146188,
1.28663123589036));
#14164=CARTESIAN_POINT('Ctrl Pts',(0.122141837621857,0.0944404211811797,
1.28927862526462));
#14165=CARTESIAN_POINT('Ctrl Pts',(0.0811175428499519,0.131368055068631,
1.29192601463888));
#14166=CARTESIAN_POINT('Ctrl Pts',(0.0339716590485425,0.142599665496764,
1.29457340401314));
#14167=CARTESIAN_POINT('Ctrl Pts',(-0.013174224752867,0.153831275924897,
1.2972207933874));
#14168=CARTESIAN_POINT('Ctrl Pts',(-0.0664416975837803,0.139366862893713,
1.29986818276166));
#14169=CARTESIAN_POINT('Ctrl Pts',(-0.101431520699135,0.105831870563862,
1.30251557213592));
#14170=CARTESIAN_POINT('Ctrl Pts',(-0.129710573305276,0.0787286237393239,
1.30465521322918));
#14171=CARTESIAN_POINT('Ctrl Pts',(-0.146050663974784,0.0391684733249047,
1.30679485432245));
#14172=CARTESIAN_POINT('Ctrl Pts',(-0.146410535958061,-0.000127756381200432,
1.30893449541571));
#14173=CARTESIAN_POINT('Origin',(0.,0.,0.));
#14174=CARTESIAN_POINT('',(-0.146471469669193,0.000111495080380188,1.36606550458429));
#14175=CARTESIAN_POINT('',(-0.146526884620975,8.5711493927648E-5,1.35893449541571));
#14176=CARTESIAN_POINT('',(-0.14635,-1.79227059055215E-17,0.));
#14177=CARTESIAN_POINT('Ctrl Pts',(-0.146471469669193,0.000111495080380188,
1.36606550458429));
#14178=CARTESIAN_POINT('Ctrl Pts',(-0.146532402405025,0.0073220458586883,
1.36567247403923));
#14179=CARTESIAN_POINT('Ctrl Pts',(-0.146045973070864,0.0145243451116175,
1.36527944349416));
#14180=CARTESIAN_POINT('Ctrl Pts',(-0.144983764805735,0.0216407019395156,
1.3648864129491));
#14181=CARTESIAN_POINT('Ctrl Pts',(-0.137831767320671,0.0695561322809842,
1.36224008307));
#14182=CARTESIAN_POINT('Ctrl Pts',(-0.104576727819841,0.113575347233418,
1.3595937531909));
#14183=CARTESIAN_POINT('Ctrl Pts',(-0.060440002550743,0.133550058215342,
1.3569474233118));
#14184=CARTESIAN_POINT('Ctrl Pts',(-0.0163032772816473,0.153524769197265,
1.35430109343269));
#14185=CARTESIAN_POINT('Ctrl Pts',(0.0387151337557165,0.149454976208681,
1.35165476355359));
#14186=CARTESIAN_POINT('Ctrl Pts',(0.0794324390145508,0.123203488242689,
1.34900843367449));
#14187=CARTESIAN_POINT('Ctrl Pts',(0.120149744273387,0.0969520002766962,
1.34636210379539));
#14188=CARTESIAN_POINT('Ctrl Pts',(0.146565943753694,0.048518817333291,
1.34371577391629));
#14189=CARTESIAN_POINT('Ctrl Pts',(0.14658992694451,7.25688577880009E-5,
1.34106944403718));
#14190=CARTESIAN_POINT('Ctrl Pts',(0.146613910135327,-0.0483736796177136,
1.33842311415808));
#14191=CARTESIAN_POINT('Ctrl Pts',(0.120245677036657,-0.0968329936253116,
1.33577678427898));
#14192=CARTESIAN_POINT('Ctrl Pts',(0.0795543829983497,-0.123124782547022,
1.33313045439988));
#14193=CARTESIAN_POINT('Ctrl Pts',(0.0388630889600415,-0.149416571468734,
1.33048412452078));
#14194=CARTESIAN_POINT('Ctrl Pts',(-0.0161512660179049,-0.153540835304554,
1.32783779464168));
#14195=CARTESIAN_POINT('Ctrl Pts',(-0.0603077462478081,-0.133609833714981,
1.32519146476257));
#14196=CARTESIAN_POINT('Ctrl Pts',(-0.10446422647771,-0.113678832125408,
1.32254513488347));
#14197=CARTESIAN_POINT('Ctrl Pts',(-0.137762831959571,-0.0696925651104417,
1.31989880500437));
#14198=CARTESIAN_POINT('Ctrl Pts',(-0.144962267025529,-0.0217842390534145,
1.31725247512527));
#14199=CARTESIAN_POINT('Ctrl Pts',(-0.146038665626028,-0.0146213916011371,
1.31685681827827));
#14200=CARTESIAN_POINT('Ctrl Pts',(-0.146531651210624,-0.00737087161912708,
1.31646116143128));
#14201=CARTESIAN_POINT('Ctrl Pts',(-0.146470135615938,-0.000111966546850736,
1.31606550458429));
#14202=CARTESIAN_POINT('Ctrl Pts',(-0.146410535958061,-0.000127756381200432,
1.30893449541571));
#14203=CARTESIAN_POINT('Ctrl Pts',(-0.146495935505426,-0.00945296197092968,
1.30944224369671));
#14204=CARTESIAN_POINT('Ctrl Pts',(-0.145681427739287,-0.018763305174839,
1.3099499919777));
#14205=CARTESIAN_POINT('Ctrl Pts',(-0.143913007029536,-0.0278887903271487,
1.3104577402587));
#14206=CARTESIAN_POINT('Ctrl Pts',(-0.134692496844786,-0.0754688872597875,
1.31310512963296));
#14207=CARTESIAN_POINT('Ctrl Pts',(-0.0995393030754929,-0.118023509496548,
1.31575251900722));
#14208=CARTESIAN_POINT('Ctrl Pts',(-0.0545553941775042,-0.136060454153345,
1.31839990838148));
#14209=CARTESIAN_POINT('Ctrl Pts',(-0.00957148527951295,-0.154097398810142,
1.32104729775574));
#14210=CARTESIAN_POINT('Ctrl Pts',(0.0452431387471776,-0.14761666588697,
1.32369468713));
#14211=CARTESIAN_POINT('Ctrl Pts',(0.0847805644327026,-0.119586763955155,
1.32634207650426));
#14212=CARTESIAN_POINT('Ctrl Pts',(0.124317990118227,-0.09155686202334,
1.32898946587852));
#14213=CARTESIAN_POINT('Ctrl Pts',(0.148578217462589,-0.041977791082884,
1.33163685525278));
#14214=CARTESIAN_POINT('Ctrl Pts',(0.146448816178573,0.00644068764408242,
1.33428424462704));
#14215=CARTESIAN_POINT('Ctrl Pts',(0.144319414894557,0.0548591663710502,
1.3369316340013));
#14216=CARTESIAN_POINT('Ctrl Pts',(0.115800384982161,0.102117052884526,
1.33957902337556));
#14217=CARTESIAN_POINT('Ctrl Pts',(0.0739549070570988,0.126567807678519,
1.34222641274982));
#14218=CARTESIAN_POINT('Ctrl Pts',(0.0321094291320376,0.151018562472512,
1.34487380212408));
#14219=CARTESIAN_POINT('Ctrl Pts',(-0.0230624968056921,0.152662185547021,
1.34752119149834));
#14220=CARTESIAN_POINT('Ctrl Pts',(-0.0662892946253695,0.1307458130856,
1.3501685808726));
#14221=CARTESIAN_POINT('Ctrl Pts',(-0.109516092445046,0.10882944062418,
1.35281597024686));
#14222=CARTESIAN_POINT('Ctrl Pts',(-0.140797762146673,0.0633530726268328,
1.35546335962112));
#14223=CARTESIAN_POINT('Ctrl Pts',(-0.145805692234247,0.0151472216574969,
1.35811074899538));
#14224=CARTESIAN_POINT('Ctrl Pts',(-0.146325105122407,0.0101474034011793,
1.35838533113549));
#14225=CARTESIAN_POINT('Ctrl Pts',(-0.146561879835735,0.00511822289583405,
1.3586599132756));
#14226=CARTESIAN_POINT('Ctrl Pts',(-0.146526884620975,8.5711493927648E-5,
1.35893449541571));
#14227=CARTESIAN_POINT('Origin',(0.,0.,0.));
#14228=CARTESIAN_POINT('',(-0.146120987371435,4.2191387702159E-5,1.41606550458429));
#14229=CARTESIAN_POINT('',(-0.146148882937928,7.6306569664006E-5,1.40893449541571));
#14230=CARTESIAN_POINT('',(-0.14635,-1.79227059055215E-17,0.));
#14231=CARTESIAN_POINT('Ctrl Pts',(-0.146120987371435,4.2191387702159E-5,
1.41606550458429));
#14232=CARTESIAN_POINT('Ctrl Pts',(-0.146177309023295,0.021854523983563,
1.41488378664717));
#14233=CARTESIAN_POINT('Ctrl Pts',(-0.141604359564088,0.0436444172696427,
1.41370206871005));
#14234=CARTESIAN_POINT('Ctrl Pts',(-0.132282279973341,0.0631665524487371,
1.41252035077294));
#14235=CARTESIAN_POINT('Ctrl Pts',(-0.1114064880593,0.106884268839086,1.40987402089383));
#14236=CARTESIAN_POINT('Ctrl Pts',(-0.0667143915920224,0.139229456738304,
1.40722769101473));
#14237=CARTESIAN_POINT('Ctrl Pts',(-0.0186623352932378,0.145397151366753,
1.40458136113563));
#14238=CARTESIAN_POINT('Ctrl Pts',(0.0293897210055454,0.151564845995202,
1.40193503125653));
#14239=CARTESIAN_POINT('Ctrl Pts',(0.0808017371358351,0.131555047352884,
1.39928870137743));
#14240=CARTESIAN_POINT('Ctrl Pts',(0.112041660826149,0.0945265884816804,
1.39664237149832));
#14241=CARTESIAN_POINT('Ctrl Pts',(0.143281584516463,0.0574981296104763,
1.39399604161922));
#14242=CARTESIAN_POINT('Ctrl Pts',(0.154349415766802,0.00345101051038574,
1.39134971174012));
#14243=CARTESIAN_POINT('Ctrl Pts',(0.140179214932283,-0.0428765696854336,
1.38870338186102));
#14244=CARTESIAN_POINT('Ctrl Pts',(0.126009014097764,-0.089204149881253,
1.38605705198192));
#14245=CARTESIAN_POINT('Ctrl Pts',(0.0866007811783877,-0.127812191172801,
1.38341072210282));
#14246=CARTESIAN_POINT('Ctrl Pts',(0.0399922944706322,-0.14102917638501,
1.38076439222371));
#14247=CARTESIAN_POINT('Ctrl Pts',(-0.00661619223712474,-0.15424616159722,
1.37811806234461));
#14248=CARTESIAN_POINT('Ctrl Pts',(-0.060424932733261,-0.142072090730089,
1.37547173246551));
#14249=CARTESIAN_POINT('Ctrl Pts',(-0.0968048252466797,-0.110079232431271,
1.37282540258641));
#14250=CARTESIAN_POINT('Ctrl Pts',(-0.127781608685608,-0.08283792481198,
1.37057210325237));
#14251=CARTESIAN_POINT('Ctrl Pts',(-0.146122133733866,-0.0412276055847571,
1.36831880391833));
#14252=CARTESIAN_POINT('Ctrl Pts',(-0.146471469669193,0.000111495080380188,
1.36606550458429));
#14253=CARTESIAN_POINT('Ctrl Pts',(-0.146526884620975,8.5711493927648E-5,
1.35893449541571));
#14254=CARTESIAN_POINT('Ctrl Pts',(-0.146224472749943,-0.0434028397118431,
1.36130730264986));
#14255=CARTESIAN_POINT('Ctrl Pts',(-0.125627402569456,-0.0871401285467012,
1.36368010988401));
#14256=CARTESIAN_POINT('Ctrl Pts',(-0.0917490966422633,-0.114327780902106,
1.36605291711816));
#14257=CARTESIAN_POINT('Ctrl Pts',(-0.0539503804891888,-0.144661598551044,
1.36870030649242));
#14258=CARTESIAN_POINT('Ctrl Pts',(0.00038124229047478,-0.154393899907594,
1.37134769586668));
#14259=CARTESIAN_POINT('Ctrl Pts',(0.0463590973565905,-0.139066790892088,
1.37399508524094));
#14260=CARTESIAN_POINT('Ctrl Pts',(0.0923369524227062,-0.123739681876581,
1.3766424746152));
#14261=CARTESIAN_POINT('Ctrl Pts',(0.129961039775272,-0.083353162489017,
1.37928986398946));
#14262=CARTESIAN_POINT('Ctrl Pts',(0.141997595260484,-0.0364063334065561,
1.38193725336372));
#14263=CARTESIAN_POINT('Ctrl Pts',(0.154034150745695,0.0105404956759021,
1.38458464273798));
#14264=CARTESIAN_POINT('Ctrl Pts',(0.140483174363557,0.0640476344532581,
1.38723203211224));
#14265=CARTESIAN_POINT('Ctrl Pts',(0.10755170844225,0.0996060653705087,
1.3898794214865));
#14266=CARTESIAN_POINT('Ctrl Pts',(0.0746202425209409,0.135164496287762,
1.39252681086076));
#14267=CARTESIAN_POINT('Ctrl Pts',(0.0223082870604623,0.152774219344908,
1.39517420023502));
#14268=CARTESIAN_POINT('Ctrl Pts',(-0.025422593472234,0.144369075867769,
1.39782158960928));
#14269=CARTESIAN_POINT('Ctrl Pts',(-0.073153474004929,0.135963932390631,
1.40046897898354));
#14270=CARTESIAN_POINT('Ctrl Pts',(-0.11630327960984,0.101543922379208,
1.4031163683578));
#14271=CARTESIAN_POINT('Ctrl Pts',(-0.135107186188192,0.0568751802851974,
1.40576375773206));
#14272=CARTESIAN_POINT('Ctrl Pts',(-0.142614236437708,0.0390421576584788,
1.40682067029328));
#14273=CARTESIAN_POINT('Ctrl Pts',(-0.14624095998336,0.0195756595648056,
1.40787758285449));
#14274=CARTESIAN_POINT('Ctrl Pts',(-0.146148882937928,7.6306569664006E-5,
1.40893449541571));
#14275=CARTESIAN_POINT('Origin',(0.,0.,0.));
#14276=CARTESIAN_POINT('',(-0.14631473222987,-0.000131398079681141,1.46606550458429));
#14277=CARTESIAN_POINT('',(-0.146248097568756,-0.000123763188177425,1.45893449541571));
#14278=CARTESIAN_POINT('',(-0.14635,-1.79227059055215E-17,0.));
#14279=CARTESIAN_POINT('Ctrl Pts',(-0.14631473222987,-0.000131398079681141,
1.46606550458429));
#14280=CARTESIAN_POINT('Ctrl Pts',(-0.145989697979493,0.0361157155227289,
1.46409509925512));
#14281=CARTESIAN_POINT('Ctrl Pts',(-0.132370868650209,0.0725796635271419,
1.46212469392594));
#14282=CARTESIAN_POINT('Ctrl Pts',(-0.107973319296019,0.0991484059484618,
1.46015428859677));
#14283=CARTESIAN_POINT('Ctrl Pts',(-0.0752064754000165,0.134831245351468,
1.45750795871767));
#14284=CARTESIAN_POINT('Ctrl Pts',(-0.0229974942306327,0.152665588379184,
1.45486162883857));
#14285=CARTESIAN_POINT('Ctrl Pts',(0.0247535192036911,0.144485406820094,
1.45221529895946));
#14286=CARTESIAN_POINT('Ctrl Pts',(0.0725045326380122,0.136305225261004,
1.44956896908036));
#14287=CARTESIAN_POINT('Ctrl Pts',(0.115797578337275,0.102110519115111,
1.44692263920126));
#14288=CARTESIAN_POINT('Ctrl Pts',(0.134818450998255,0.0575543070937695,
1.44427630932216));
#14289=CARTESIAN_POINT('Ctrl Pts',(0.153839323659235,0.0129980950724284,
1.44162997944306));
#14290=CARTESIAN_POINT('Ctrl Pts',(0.148588023281934,-0.0419196228243577,
1.43898364956396));
#14291=CARTESIAN_POINT('Ctrl Pts',(0.121467255745355,-0.082062966762292,
1.43633731968485));
#14292=CARTESIAN_POINT('Ctrl Pts',(0.0943464882087764,-0.122206310700226,
1.43369098980575));
#14293=CARTESIAN_POINT('Ctrl Pts',(0.0453562535129183,-0.147575280679306,
1.43104465992665));
#14294=CARTESIAN_POINT('Ctrl Pts',(-0.00307937473935208,-0.146557666176543,
1.42839833004755));
#14295=CARTESIAN_POINT('Ctrl Pts',(-0.0515150029916225,-0.14554005167378,
1.42575200016845));
#14296=CARTESIAN_POINT('Ctrl Pts',(-0.0993960248003067,-0.118135852689175,
1.42310567028934));
#14297=CARTESIAN_POINT('Ctrl Pts',(-0.124806792024246,-0.0768886307561326,
1.42045934041024));
#14298=CARTESIAN_POINT('Ctrl Pts',(-0.138870387581649,-0.0540603453281256,
1.41899472846826));
#14299=CARTESIAN_POINT('Ctrl Pts',(-0.146051182757901,-0.0269918425378075,
1.41753011652627));
#14300=CARTESIAN_POINT('Ctrl Pts',(-0.146120987371435,4.2191387702159E-5,
1.41606550458429));
#14301=CARTESIAN_POINT('Ctrl Pts',(-0.146148882937928,7.6306569664006E-5,
1.40893449541571));
#14302=CARTESIAN_POINT('Ctrl Pts',(-0.146010322369016,-0.0292669616874671,
1.41052497222875));
#14303=CARTESIAN_POINT('Ctrl Pts',(-0.137450455640384,-0.0586846305953837,
1.4121154490418));
#14304=CARTESIAN_POINT('Ctrl Pts',(-0.121019719714466,-0.0827222215753489,
1.41370592585484));
#14305=CARTESIAN_POINT('Ctrl Pts',(-0.0936703391105966,-0.122733407165291,
1.4163533152291));
#14306=CARTESIAN_POINT('Ctrl Pts',(-0.0445135703510636,-0.147838304168576,
1.41900070460336));
#14307=CARTESIAN_POINT('Ctrl Pts',(0.00393424939099551,-0.146537573651384,
1.42164809397762));
#14308=CARTESIAN_POINT('Ctrl Pts',(0.0523820691330518,-0.145236843134192,
1.42429548335188));
#14309=CARTESIAN_POINT('Ctrl Pts',(0.100120939857634,-0.117530485096527,
1.42694287272614));
#14310=CARTESIAN_POINT('Ctrl Pts',(0.125284029446909,-0.0761094471358441,
1.4295902621004));
#14311=CARTESIAN_POINT('Ctrl Pts',(0.150447119036187,-0.0346884091751576,
1.43223765147466));
#14312=CARTESIAN_POINT('Ctrl Pts',(0.153034427490153,0.020447308708549,
1.43488504084892));
#14313=CARTESIAN_POINT('Ctrl Pts',(0.13186079120536,0.0640427391611241,
1.43753243022318));
#14314=CARTESIAN_POINT('Ctrl Pts',(0.110687154920568,0.107638169613697,
1.44017981959744));
#14315=CARTESIAN_POINT('Ctrl Pts',(0.0657525738970213,0.139693312635139,
1.4428272089717));
#14316=CARTESIAN_POINT('Ctrl Pts',(0.0176394768514684,0.145525221357757,
1.44547459834596));
#14317=CARTESIAN_POINT('Ctrl Pts',(-0.0304736201940859,0.151357130080375,
1.44812198772022));
#14318=CARTESIAN_POINT('Ctrl Pts',(-0.0817652332616461,0.130965804504167,
1.45076937709448));
#14319=CARTESIAN_POINT('Ctrl Pts',(-0.112741325423428,0.0936916042199666,
1.45341676646874));
#14320=CARTESIAN_POINT('Ctrl Pts',(-0.134261605244105,0.0677957870194472,
1.45525600945106));
#14321=CARTESIAN_POINT('Ctrl Pts',(-0.145976367207401,0.0337512577971725,
1.45709525243339));
#14322=CARTESIAN_POINT('Ctrl Pts',(-0.146248097568756,-0.000123763188177425,
1.45893449541571));
#14323=CARTESIAN_POINT('Origin',(0.,0.,-0.0924367114736175));
#14324=CARTESIAN_POINT('',(-0.117746618301147,-0.000105742458702955,1.48256328852638));
#14325=CARTESIAN_POINT('',(-0.117971241274414,-5.28325160115065E-6,1.49243671147361));
#14326=CARTESIAN_POINT('',(-0.117775,2.85464118895969E-14,-0.0924367114736175));
#14327=CARTESIAN_POINT('',(-0.117668597464313,0.00500517689812599,1.532225));
#14328=CARTESIAN_POINT('Ctrl Pts',(-0.117746618301147,-0.000105742458702949,
1.48256328852638));
#14329=CARTESIAN_POINT('Ctrl Pts',(-0.117836347163251,-0.0101121102621826,
1.48323921307631));
#14330=CARTESIAN_POINT('Ctrl Pts',(-0.112089674709738,-0.0591937430214443,
1.48656146750534));
#14331=CARTESIAN_POINT('Ctrl Pts',(-0.0435804807853106,-0.132222740314769,
1.49253005181348));
#14332=CARTESIAN_POINT('Ctrl Pts',(0.0874774386997331,-0.108286040948335,
1.50046904145078));
#14333=CARTESIAN_POINT('Ctrl Pts',(0.138385550162814,0.0147146982980264,
1.50840803108809));
#14334=CARTESIAN_POINT('Ctrl Pts',(0.0627460642121078,0.124368470664037,
1.51634702072539));
#14335=CARTESIAN_POINT('Ctrl Pts',(-0.0706026869052757,0.119928391791904,
1.5242860103627));
#14336=CARTESIAN_POINT('Ctrl Pts',(-0.116004137797729,0.0441355889673283,
1.5295786701209));
#14337=CARTESIAN_POINT('Ctrl Pts',(-0.117668597464313,0.00500517689812487,
1.532225));
#14338=CARTESIAN_POINT('',(-0.0334019664627544,0.1129391839063,1.53222500000001));
#14339=CARTESIAN_POINT('Origin',(0.,0.,1.532225));
#14340=CARTESIAN_POINT('Ctrl Pts',(-0.117971276761593,-5.28420699491729E-6,
1.49243671147361));
#14341=CARTESIAN_POINT('Ctrl Pts',(-0.117971582784674,-0.000385634193345565,
1.49246252744444));
#14342=CARTESIAN_POINT('Ctrl Pts',(-0.117794795258817,-0.0397700451254522,
1.49513573278954));
#14343=CARTESIAN_POINT('Ctrl Pts',(-0.0742871760264013,-0.117748889605885,
1.50045632750888));
#14344=CARTESIAN_POINT('Ctrl Pts',(0.0586284551779338,-0.126233948370975,
1.50839849563167));
#14345=CARTESIAN_POINT('Ctrl Pts',(0.137995068118234,-0.019163470063063,
1.51634066375444));
#14346=CARTESIAN_POINT('Ctrl Pts',(0.0906261803825392,0.105639137646141,
1.52428283187723));
#14347=CARTESIAN_POINT('Ctrl Pts',(0.00417072711528833,0.124051375507138,
1.52957761062575));
#14348=CARTESIAN_POINT('Ctrl Pts',(-0.0334019664627544,0.1129391839063,
1.53222500000001));
#14349=CARTESIAN_POINT('Origin',(0.,0.,-0.0924367114736175));
#14350=CARTESIAN_POINT('',(-0.117590702341447,3.3953472435133E-5,1.43256328852638));
#14351=CARTESIAN_POINT('',(-0.117692994131604,-9.95982882293356E-5,1.44243671147361));
#14352=CARTESIAN_POINT('',(-0.117775,2.85464118895969E-14,-0.0924367114736175));
#14353=CARTESIAN_POINT('Ctrl Pts',(-0.117590702341447,3.39534724351446E-5,
1.43256328852638));
#14354=CARTESIAN_POINT('Ctrl Pts',(-0.117534527156218,-0.0217216553118358,
1.43402790046837));
#14355=CARTESIAN_POINT('Ctrl Pts',(-0.101314495966545,-0.0828641818343832,
1.43813884228945));
#14356=CARTESIAN_POINT('Ctrl Pts',(-0.00292444232197888,-0.139176693688359,
1.44489611398964));
#14357=CARTESIAN_POINT('Ctrl Pts',(0.115350068603298,-0.0779297424218237,
1.45283510362695));
#14358=CARTESIAN_POINT('Ctrl Pts',(0.128028003046829,0.0546551750765237,
1.46077409326425));
#14359=CARTESIAN_POINT('Ctrl Pts',(0.0235079116789307,0.137209630484779,
1.46871308290156));
#14360=CARTESIAN_POINT('Ctrl Pts',(-0.0918059616614023,0.0978189523496558,
1.47597614798894));
#14361=CARTESIAN_POINT('Ctrl Pts',(-0.117485047349053,0.0290640819657798,
1.48059288319721));
#14362=CARTESIAN_POINT('Ctrl Pts',(-0.117746618301147,-0.000105742458702949,
1.48256328852638));
#14363=CARTESIAN_POINT('Ctrl Pts',(-0.117692994131604,-9.9598288229346E-5,
1.44243671147361));
#14364=CARTESIAN_POINT('Ctrl Pts',(-0.117789077779518,-0.0120777797952868,
1.44324485786555));
#14365=CARTESIAN_POINT('Ctrl Pts',(-0.110597905189529,-0.0631824179582176,
1.44670039363175));
#14366=CARTESIAN_POINT('Ctrl Pts',(-0.0368790902657646,-0.134252921254984,
1.45280331877221));
#14367=CARTESIAN_POINT('Ctrl Pts',(0.0928396680879532,-0.103751556080299,
1.46074548689499));
#14368=CARTESIAN_POINT('Ctrl Pts',(0.137511141307062,0.0217950526079239,
1.46868765501776));
#14369=CARTESIAN_POINT('Ctrl Pts',(0.0562018483347667,0.127378648737854,
1.47662982314055));
#14370=CARTESIAN_POINT('Ctrl Pts',(-0.0761502833827582,0.1162998103107,
1.48454617529249));
#14371=CARTESIAN_POINT('Ctrl Pts',(-0.117940200573233,0.0386186906477724,
1.48981513807018));
#14372=CARTESIAN_POINT('Ctrl Pts',(-0.117971276761593,-5.28420699491729E-6,
1.49243671147361));
#14373=CARTESIAN_POINT('Origin',(0.,0.,-0.0924367114736175));
#14374=CARTESIAN_POINT('',(-0.117872752581409,8.97255421561373E-5,1.38256328852638));
#14375=CARTESIAN_POINT('',(-0.117613151267609,6.14076272390171E-5,1.39243671147361));
#14376=CARTESIAN_POINT('',(-0.117775,2.85464118895969E-14,-0.0924367114736175));
#14377=CARTESIAN_POINT('Ctrl Pts',(-0.117872752581409,8.97255421561322E-5,
1.38256328852638));
#14378=CARTESIAN_POINT('Ctrl Pts',(-0.117591624875346,-0.0331778698171688,
1.38481658786042));
#14379=CARTESIAN_POINT('Ctrl Pts',(-0.0854981695600773,-0.105990339321694,
1.38971621707357));
#14380=CARTESIAN_POINT('Ctrl Pts',(0.0379781508110965,-0.133926497290667,
1.39726217616581));
#14381=CARTESIAN_POINT('Ctrl Pts',(0.133119345865688,-0.0407171622080862,
1.40520116580311));
#14382=CARTESIAN_POINT('Ctrl Pts',(0.106398871137127,0.0897659150453452,
1.41314015544042));
#14383=CARTESIAN_POINT('Ctrl Pts',(-0.0177224175491345,0.138074504763813,
1.42107914507772));
#14384=CARTESIAN_POINT('Ctrl Pts',(-0.105714817800915,0.0743914165933911,
1.42755352277305));
#14385=CARTESIAN_POINT('Ctrl Pts',(-0.11763602712824,0.0175874039095825,
1.43138157058926));
#14386=CARTESIAN_POINT('Ctrl Pts',(-0.117590702341447,3.39534724351446E-5,
1.43256328852638));
#14387=CARTESIAN_POINT('Ctrl Pts',(-0.117613151267609,6.1407627239024E-5,
1.39243671147361));
#14388=CARTESIAN_POINT('Ctrl Pts',(-0.117501644803633,-0.0235525549213426,
1.39402718828666));
#14389=CARTESIAN_POINT('Ctrl Pts',(-0.0991469449676741,-0.0866320980727062,
1.39826505447396));
#14390=CARTESIAN_POINT('Ctrl Pts',(0.00373660876362508,-0.139175849115243,
1.40515031003553));
#14391=CARTESIAN_POINT('Ctrl Pts',(0.118990018389619,-0.0722858665142316,
1.41309247815831));
#14392=CARTESIAN_POINT('Ctrl Pts',(0.125236419206141,0.0608253567263532,
1.42103464628109));
#14393=CARTESIAN_POINT('Ctrl Pts',(0.0167532566496359,0.13821437898841,
1.42897681440387));
#14394=CARTESIAN_POINT('Ctrl Pts',(-0.0944771051913143,0.0939940009069027,
1.43611083613471));
#14395=CARTESIAN_POINT('Ctrl Pts',(-0.117474319425011,0.0271612872365273,
1.44059746849129));
#14396=CARTESIAN_POINT('Ctrl Pts',(-0.117692994131604,-9.9598288229346E-5,
1.44243671147361));
#14397=CARTESIAN_POINT('Origin',(0.,0.,-0.0924367114736175));
#14398=CARTESIAN_POINT('',(-0.117871679003533,-9.01049542302267E-5,1.33256328852638));
#14399=CARTESIAN_POINT('',(-0.117917347702326,6.89762296073142E-5,1.34243671147361));
#14400=CARTESIAN_POINT('',(-0.117775,2.85464118895969E-14,-0.0924367114736175));
#14401=CARTESIAN_POINT('Ctrl Pts',(-0.117871679003533,-9.01049542302501E-5,
1.33256328852638));
#14402=CARTESIAN_POINT('Ctrl Pts',(-0.117921183610054,-0.00593170075121234,
1.33295894537338));
#14403=CARTESIAN_POINT('Ctrl Pts',(-0.114870949065289,-0.0507926200311143,
1.33600093209947));
#14404=CARTESIAN_POINT('Ctrl Pts',(-0.0572704544775333,-0.126880813469472,
1.34168924870467));
#14405=CARTESIAN_POINT('Ctrl Pts',(0.0755477687720905,-0.116923823242002,
1.34962823834197));
#14406=CARTESIAN_POINT('Ctrl Pts',(0.13920718769651,6.89141801743488E-5,
1.35756722797928));
#14407=CARTESIAN_POINT('Ctrl Pts',(0.0754319660950179,0.116998564767658,
1.36550621761658));
#14408=CARTESIAN_POINT('Ctrl Pts',(-0.0573960494825499,0.126824048933643,
1.37344520725389));
#14409=CARTESIAN_POINT('Ctrl Pts',(-0.11489462347839,0.0507140179075799,
1.37913089755716));
#14410=CARTESIAN_POINT('Ctrl Pts',(-0.117921788132912,0.00589240827474643,
1.38217025798132));
#14411=CARTESIAN_POINT('Ctrl Pts',(-0.117872752581409,8.97255421561322E-5,
1.38256328852638));
#14412=CARTESIAN_POINT('Ctrl Pts',(-0.117917347702326,6.89762296073276E-5,
1.34243671147361));
#14413=CARTESIAN_POINT('Ctrl Pts',(-0.117673982084908,-0.0349283870656527,
1.34480951870776));
#14414=CARTESIAN_POINT('Ctrl Pts',(-0.0826049238592893,-0.109396528181867,
1.34982971531618));
#14415=CARTESIAN_POINT('Ctrl Pts',(0.0440301174146577,-0.132080378229483,
1.35749730129884));
#14416=CARTESIAN_POINT('Ctrl Pts',(0.13486394497766,-0.0345773583278084,
1.36543946942163));
#14417=CARTESIAN_POINT('Ctrl Pts',(0.102148545386143,0.0946020732301706,
1.3733816375444));
#14418=CARTESIAN_POINT('Ctrl Pts',(-0.0241454188302812,0.137116288461919,
1.38132380566719));
#14419=CARTESIAN_POINT('Ctrl Pts',(-0.107458038693719,0.07065895059964,
1.38767549697692));
#14420=CARTESIAN_POINT('Ctrl Pts',(-0.117687250167678,0.015753490298928,
1.3913797989124));
#14421=CARTESIAN_POINT('Ctrl Pts',(-0.117613151267609,6.1407627239024E-5,
1.39243671147361));
#14422=CARTESIAN_POINT('Origin',(0.,0.,-0.0924367114736175));
#14423=CARTESIAN_POINT('',(-0.117590388001671,-3.33269891443968E-5,1.28256328852638));
#14424=CARTESIAN_POINT('',(-0.117823716245033,-0.000102811805890834,1.29243671147362));
#14425=CARTESIAN_POINT('',(-0.117775,2.85464118895969E-14,-0.0924367114736175));
#14426=CARTESIAN_POINT('Ctrl Pts',(-0.117590388001671,-3.33269891444124E-5,
1.28256328852638));
#14427=CARTESIAN_POINT('Ctrl Pts',(-0.117634977734708,-0.017625925033684,
1.28374763276543));
#14428=CARTESIAN_POINT('Ctrl Pts',(-0.105676786131388,-0.0744702911817869,
1.28757830688358));
#14429=CARTESIAN_POINT('Ctrl Pts',(-0.0175857351491984,-0.138091953858251,
1.29405531088083));
#14430=CARTESIAN_POINT('Ctrl Pts',(0.106487712804436,-0.089660542174548,
1.30199430051814));
#14431=CARTESIAN_POINT('Ctrl Pts',(0.133078957772855,0.0408489510387311,
1.30993329015544));
#14432=CARTESIAN_POINT('Ctrl Pts',(0.0378455373822902,0.133964029124136,
1.31787227979275));
#14433=CARTESIAN_POINT('Ctrl Pts',(-0.0855601048685178,0.105915403748908,
1.32541561258306));
#14434=CARTESIAN_POINT('Ctrl Pts',(-0.117590074669608,0.0331395035428114,
1.33031261549427));
#14435=CARTESIAN_POINT('Ctrl Pts',(-0.117871679003533,-9.01049542302501E-5,
1.33256328852638));
#14436=CARTESIAN_POINT('Ctrl Pts',(-0.117823716245033,-0.000102811805890825,
1.29243671147362));
#14437=CARTESIAN_POINT('Ctrl Pts',(-0.117892441435953,-0.00760726064997237,
1.29294445975461));
#14438=CARTESIAN_POINT('Ctrl Pts',(-0.113819337750002,-0.0541654333254181,
1.29609959740987));
#14439=CARTESIAN_POINT('Ctrl Pts',(-0.0518146499729274,-0.129225073214149,
1.30190212443939));
#14440=CARTESIAN_POINT('Ctrl Pts',(0.0805213734929343,-0.11357898534207,
1.30984429256217));
#14441=CARTESIAN_POINT('Ctrl Pts',(0.1390915465469,0.0061171215252809,1.31778646068495));
#14442=CARTESIAN_POINT('Ctrl Pts',(0.0702395735793815,0.120209316621791,
1.32572862880773));
#14443=CARTESIAN_POINT('Ctrl Pts',(-0.0629590648350173,0.124177428154433,
1.33367079693051));
#14444=CARTESIAN_POINT('Ctrl Pts',(-0.115917830154768,0.0471875384414626,
1.33924015781913));
#14445=CARTESIAN_POINT('Ctrl Pts',(-0.117945510062545,0.00411888419242175,
1.3421621293335));
#14446=CARTESIAN_POINT('Ctrl Pts',(-0.117917347702326,6.89762296073276E-5,
1.34243671147361));
#14447=CARTESIAN_POINT('Origin',(0.,0.,-0.0924367114736175));
#14448=CARTESIAN_POINT('',(-0.11774949833287,0.000107383800510985,1.23256328852638));
#14449=CARTESIAN_POINT('',(-0.117581795058195,-8.20683476789735E-6,1.24243671147361));
#14450=CARTESIAN_POINT('',(-0.117775,2.85464118895969E-14,-0.0924367114736175));
#14451=CARTESIAN_POINT('Ctrl Pts',(-0.11774949833287,0.000107383800510997,
1.23256328852638));
#14452=CARTESIAN_POINT('Ctrl Pts',(-0.1174869159147,-0.0291008736543001,
1.23453632015749));
#14453=CARTESIAN_POINT('Ctrl Pts',(-0.0917482398636095,-0.0978979247776974,
1.23915568166769));
#14454=CARTESIAN_POINT('Ctrl Pts',(0.0236422145726536,-0.137184880695923,
1.246421373057));
#14455=CARTESIAN_POINT('Ctrl Pts',(0.128082862902196,-0.0545291301253663,
1.2543603626943));
#14456=CARTESIAN_POINT('Ctrl Pts',(0.115272428336817,0.0780443019497631,
1.26229935233161));
#14457=CARTESIAN_POINT('Ctrl Pts',(-0.00306201423577413,0.139173524314926,
1.27023834196891));
#14458=CARTESIAN_POINT('Ctrl Pts',(-0.101358337705897,0.08278581645186,
1.27699298736717));
#14459=CARTESIAN_POINT('Ctrl Pts',(-0.117535345263889,0.02168343817453,
1.28110130288633));
#14460=CARTESIAN_POINT('Ctrl Pts',(-0.117590388001671,-3.33269891444124E-5,
1.28256328852638));
#14461=CARTESIAN_POINT('Ctrl Pts',(-0.117581795058195,-8.20683476789562E-6,
1.24243671147361));
#14462=CARTESIAN_POINT('Ctrl Pts',(-0.117593699448189,-0.0191748937105988,
1.24372679017572));
#14463=CARTESIAN_POINT('Ctrl Pts',(-0.104100832827715,-0.0776580224685839,
1.24766425825208));
#14464=CARTESIAN_POINT('Ctrl Pts',(-0.0120149744006178,-0.138706589206355,
1.25424911570271));
#14465=CARTESIAN_POINT('Ctrl Pts',(0.110059129405696,-0.0852693704304675,
1.26219128382548));
#14466=CARTESIAN_POINT('Ctrl Pts',(0.13130776387206,0.0462833517151888,
1.27013345194827));
#14467=CARTESIAN_POINT('Ctrl Pts',(0.0322649968732001,0.135435768819968,
1.27807562007105));
#14468=CARTESIAN_POINT('Ctrl Pts',(-0.0881142830049797,0.102747609761224,
1.28551003991283));
#14469=CARTESIAN_POINT('Ctrl Pts',(-0.117534109666069,0.0315207854174475,
1.29029707038035));
#14470=CARTESIAN_POINT('Ctrl Pts',(-0.117823716245033,-0.000102811805890825,
1.29243671147362));
#14471=CARTESIAN_POINT('Origin',(0.,0.,-0.0924367114736175));
#14472=CARTESIAN_POINT('',(-0.117957988745754,-3.12301727557783E-5,1.18256328852638));
#14473=CARTESIAN_POINT('',(-0.117793553451004,0.000106755881474893,1.19243671147362));
#14474=CARTESIAN_POINT('',(-0.117775,2.85464118895969E-14,-0.0924367114736175));
#14475=CARTESIAN_POINT('Ctrl Pts',(-0.117957988745754,-3.12301727557569E-5,
1.18256328852638));
#14476=CARTESIAN_POINT('Ctrl Pts',(-0.117964007145535,-0.00173159226684161,
1.18267867767044));
#14477=CARTESIAN_POINT('Ctrl Pts',(-0.117160216762375,-0.0424221720604921,
1.1854403966936));
#14478=CARTESIAN_POINT('Ctrl Pts',(-0.0703321751825429,-0.12013338809653,
1.19084844559586));
#14479=CARTESIAN_POINT('Ctrl Pts',(0.0627954496153871,-0.124239193932754,
1.19878743523316));
#14480=CARTESIAN_POINT('Ctrl Pts',(0.138438143943654,-0.0146125323915816,
1.20672642487047));
#14481=CARTESIAN_POINT('Ctrl Pts',(0.0873502052771435,0.108390901091839,
1.21466541450777));
#14482=CARTESIAN_POINT('Ctrl Pts',(-0.043700859820065,0.132169893139269,
1.22260440414508));
#14483=CARTESIAN_POINT('Ctrl Pts',(-0.112119660921406,0.0591163174148552,
1.22857036215128));
#14484=CARTESIAN_POINT('Ctrl Pts',(-0.117839104743291,0.0100747194789664,
1.23188999027838));
#14485=CARTESIAN_POINT('Ctrl Pts',(-0.11774949833287,0.000107383800510997,
1.23256328852638));
#14486=CARTESIAN_POINT('Ctrl Pts',(-0.117793553451004,0.000106755881474891,
1.19243671147362));
#14487=CARTESIAN_POINT('Ctrl Pts',(-0.117510050331475,-0.0305433296418112,
1.19450912059683));
#14488=CARTESIAN_POINT('Ctrl Pts',(-0.0896091397727994,-0.100804620014092,
1.19922891909429));
#14489=CARTESIAN_POINT('Ctrl Pts',(0.0288222657999454,-0.136209964735594,
1.20659610696603));
#14490=CARTESIAN_POINT('Ctrl Pts',(0.130092623711363,-0.0495962373069701,
1.21453827508881));
#14491=CARTESIAN_POINT('Ctrl Pts',(0.112184773380136,0.082452738709893,
1.22248044321158));
#14492=CARTESIAN_POINT('Ctrl Pts',(-0.00849585454694533,0.138966535376798,
1.23042261133437));
#14493=CARTESIAN_POINT('Ctrl Pts',(-0.103054997843392,0.079672038485689,
1.23707470075504));
#14494=CARTESIAN_POINT('Ctrl Pts',(-0.11756927027536,0.0201573447738481,
1.24107940080146));
#14495=CARTESIAN_POINT('Ctrl Pts',(-0.117581795058195,-8.20683476789562E-6,
1.24243671147361));
#14496=CARTESIAN_POINT('Origin',(0.,0.,-0.0924367114736175));
#14497=CARTESIAN_POINT('',(-0.117657565919426,-8.78585414499747E-5,1.13256328852638));
#14498=CARTESIAN_POINT('',(-0.117937823388479,-5.4172489969917E-5,1.14243671147362));
#14499=CARTESIAN_POINT('',(-0.117775,2.85464118895969E-14,-0.0924367114736175));
#14500=CARTESIAN_POINT('Ctrl Pts',(-0.117657565919426,-8.78585414499974E-5,
1.13256328852638));
#14501=CARTESIAN_POINT('Ctrl Pts',(-0.11775046973706,-0.0134980674796043,
1.13346736506249));
#14502=CARTESIAN_POINT('Ctrl Pts',(-0.109441032251172,-0.0660497484721492,
1.13701777147771));
#14503=CARTESIAN_POINT('Ctrl Pts',(-0.0320511128216771,-0.13546723577438,
1.14321450777202));
#14504=CARTESIAN_POINT('Ctrl Pts',(0.0964380908528195,-0.100390938007982,
1.15115349740933));
#14505=CARTESIAN_POINT('Ctrl Pts',(0.136644831685568,0.0265863832644056,
1.15909248704664));
#14506=CARTESIAN_POINT('Ctrl Pts',(0.0517625939920979,0.129225692742072,
1.16703147668394));
#14507=CARTESIAN_POINT('Ctrl Pts',(-0.0785823129332351,0.113795317289389,
1.17485507717719));
#14508=CARTESIAN_POINT('Ctrl Pts',(-0.117825981412732,0.0372644419932696,
1.18003234779134));
#14509=CARTESIAN_POINT('Ctrl Pts',(-0.117957988745754,-3.12301727557569E-5,
1.18256328852638));
#14510=CARTESIAN_POINT('Ctrl Pts',(-0.117937823388479,-5.41724899699178E-5,
1.14243671147362));
#14511=CARTESIAN_POINT('Ctrl Pts',(-0.117955293269658,-0.0031110520517566,
1.14264406164367));
#14512=CARTESIAN_POINT('Ctrl Pts',(-0.116460933142332,-0.0451799670343263,
1.14549880118799));
#14513=CARTESIAN_POINT('Ctrl Pts',(-0.0660858892268601,-0.122541963197144,
1.15100093010657));
#14514=CARTESIAN_POINT('Ctrl Pts',(0.0671705316110708,-0.121950798202395,
1.15894309822935));
#14515=CARTESIAN_POINT('Ctrl Pts',(0.138891844802359,-0.00964017357273747,
1.16688526635212));
#14516=CARTESIAN_POINT('Ctrl Pts',(0.0833739592533277,0.111501840422208,
1.17482743447491));
#14517=CARTESIAN_POINT('Ctrl Pts',(-0.0485230383040216,0.130496713571114,
1.18276960259768));
#14518=CARTESIAN_POINT('Ctrl Pts',(-0.113150295826959,0.0561813708375219,
1.18863936159726));
#14519=CARTESIAN_POINT('Ctrl Pts',(-0.117872210070015,0.00861047923971886,
1.19186173122257));
#14520=CARTESIAN_POINT('Ctrl Pts',(-0.117793553451004,0.000106755881474891,
1.19243671147362));
#14521=CARTESIAN_POINT('Origin',(0.,0.,-0.0924367114736175));
#14522=CARTESIAN_POINT('',(-0.117641451221435,8.0229283111194E-5,1.08256328852638));
#14523=CARTESIAN_POINT('',(-0.117630591849015,-7.42484764288953E-5,1.09243671147362));
#14524=CARTESIAN_POINT('',(-0.117775,2.85464118895969E-14,-0.0924367114736175));
#14525=CARTESIAN_POINT('Ctrl Pts',(-0.117641451221435,8.02292831111745E-5,
1.08256328852638));
#14526=CARTESIAN_POINT('Ctrl Pts',(-0.117483998834985,-0.0250372639622414,
1.08425605245455));
#14527=CARTESIAN_POINT('Ctrl Pts',(-0.0972946570053161,-0.0896524615425008,
1.08859514626182));
#14528=CARTESIAN_POINT('Ctrl Pts',(0.00904258428980543,-0.13891320121148,
1.09558056994819));
#14529=CARTESIAN_POINT('Ctrl Pts',(0.121617839487272,-0.067732908692211,
1.1035195595855));
#14530=CARTESIAN_POINT('Ctrl Pts',(0.122860297649024,0.0654522196953821,
1.1114585492228));
#14531=CARTESIAN_POINT('Ctrl Pts',(0.0116325734791967,0.138720326685422,
1.11939753886011));
#14532=CARTESIAN_POINT('Ctrl Pts',(-0.096364912740844,0.0911171059582243,
1.1264324519613));
#14533=CARTESIAN_POINT('Ctrl Pts',(-0.117478530206868,0.0257550656131636,
1.13082103518339));
#14534=CARTESIAN_POINT('Ctrl Pts',(-0.117657565919426,-8.78585414499974E-5,
1.13256328852638));
#14535=CARTESIAN_POINT('Ctrl Pts',(-0.117630591849015,-7.42484764288814E-5,
1.09243671147362));
#14536=CARTESIAN_POINT('Ctrl Pts',(-0.117715241483118,-0.0147626739157663,
1.09342639206478));
#14537=CARTESIAN_POINT('Ctrl Pts',(-0.108350501834675,-0.0686384992808382,
1.0970634620302));
#14538=CARTESIAN_POINT('Ctrl Pts',(-0.0276126195379174,-0.136460326620484,
1.10334792136989));
#14539=CARTESIAN_POINT('Ctrl Pts',(0.0997182217817603,-0.0971604536002107,
1.11129008949267));
#14540=CARTESIAN_POINT('Ctrl Pts',(0.135696927507188,0.0311483765905046,
1.11923225761545));
#14541=CARTESIAN_POINT('Ctrl Pts',(0.0473633069609982,0.130922093830007,
1.12717442573822));
#14542=CARTESIAN_POINT('Ctrl Pts',(-0.0809210029008042,0.111284164335459,
1.13490924369095));
#14543=CARTESIAN_POINT('Ctrl Pts',(-0.117732242679493,0.0359183370635313,
1.13999667226941));
#14544=CARTESIAN_POINT('Ctrl Pts',(-0.117937823388479,-5.41724899699178E-5,
1.14243671147362));
#14545=CARTESIAN_POINT('Origin',(0.,0.,-0.0924367114736175));
#14546=CARTESIAN_POINT('',(-0.117948158721073,4.38502512853227E-5,1.03256328852638));
#14547=CARTESIAN_POINT('',(-0.117667547954054,9.20194976846214E-5,1.04243671147362));
#14548=CARTESIAN_POINT('',(-0.117775,2.85464118895969E-14,-0.0924367114736175));
#14549=CARTESIAN_POINT('Ctrl Pts',(-0.117948158721073,4.38502512853157E-5,
1.03256328852638));
#14550=CARTESIAN_POINT('Ctrl Pts',(-0.117773439871091,-0.0365306738650768,
1.03504473984661));
#14551=CARTESIAN_POINT('Ctrl Pts',(-0.0798690478914953,-0.112422454385097,
1.04017252104593));
#14552=CARTESIAN_POINT('Ctrl Pts',(0.0493427524230464,-0.130168884856471,
1.04794663212436));
#14553=CARTESIAN_POINT('Ctrl Pts',(0.136125055048066,-0.0291310004912345,
1.05588562176166));
#14554=CARTESIAN_POINT('Ctrl Pts',(0.0982941990358779,0.0985743183458784,
1.06382461139897));
#14555=CARTESIAN_POINT('Ctrl Pts',(-0.0295182596522469,0.136041604476578,
1.07176360103627));
#14556=CARTESIAN_POINT('Ctrl Pts',(-0.108818061611988,0.067537217334308,
1.07800982674541));
#14557=CARTESIAN_POINT('Ctrl Pts',(-0.11773014713001,0.0142293884972668,
1.08160972257545));
#14558=CARTESIAN_POINT('Ctrl Pts',(-0.117641451221435,8.02292831111745E-5,
1.08256328852638));
#14559=CARTESIAN_POINT('Ctrl Pts',(-0.117667547954054,9.20194976846197E-5,
1.04243671147362));
#14560=CARTESIAN_POINT('Ctrl Pts',(-0.117475882803567,-0.0261866690710452,
1.04420872248589));
#14561=CARTESIAN_POINT('Ctrl Pts',(-0.0957916308421219,-0.0920126959480487,
1.04862812287242));
#14562=CARTESIAN_POINT('Ctrl Pts',(0.0132451643780021,-0.13859452774087,
1.05569491263321));
#14563=CARTESIAN_POINT('Ctrl Pts',(0.123654649330263,-0.0639797248987874,
1.06363708075599));
#14564=CARTESIAN_POINT('Ctrl Pts',(0.120783771971213,0.0692470788374567,
1.07157924887876));
#14565=CARTESIAN_POINT('Ctrl Pts',(0.00726255089817806,0.139036444335888,
1.07952141700155));
#14566=CARTESIAN_POINT('Ctrl Pts',(-0.0979368667310299,0.0886295245336828,
1.08647390453316));
#14567=CARTESIAN_POINT('Ctrl Pts',(-0.117488804242801,0.0245287720112504,
1.09077900269052));
#14568=CARTESIAN_POINT('Ctrl Pts',(-0.117630591849015,-7.42484764288814E-5,
1.09243671147362));
#14569=CARTESIAN_POINT('Origin',(0.,0.,-0.0924367114736175));
#14570=CARTESIAN_POINT('',(-0.117771476475648,-0.000107683352847938,0.982563288526384));
#14571=CARTESIAN_POINT('',(-0.11796176292438,2.53781033017321E-5,0.992436711473616));
#14572=CARTESIAN_POINT('',(-0.117775,2.85464118895969E-14,-0.0924367114736175));
#14573=CARTESIAN_POINT('Ctrl Pts',(-0.117771476475648,-0.000107683352847945,
0.982563288526384));
#14574=CARTESIAN_POINT('Ctrl Pts',(-0.117856103358663,-0.00933799346614349,
0.983187097359559));
#14575=CARTESIAN_POINT('Ctrl Pts',(-0.112646870919438,-0.057630810124202,
0.986457236071836));
#14576=CARTESIAN_POINT('Ctrl Pts',(-0.0461590140787468,-0.131331607851033,
0.992373704663214));
#14577=CARTESIAN_POINT('Ctrl Pts',(0.0853128637208732,-0.110001641284132,
1.00031269430052));
#14578=CARTESIAN_POINT('Ctrl Pts',(0.138686661656432,0.0120272889735618,
1.00825168393783));
#14579=CARTESIAN_POINT('Ctrl Pts',(0.0651023256631918,0.123046060459907,
1.01619067357513));
#14580=CARTESIAN_POINT('Ctrl Pts',(-0.0680787277209358,0.121424596492465,
1.02412966321244));
#14581=CARTESIAN_POINT('Ctrl Pts',(-0.116790117880403,0.0438975063746073,
1.02958720152952));
#14582=CARTESIAN_POINT('Ctrl Pts',(-0.11795976781127,0.00247402277930658,
1.0323984099675));
#14583=CARTESIAN_POINT('Ctrl Pts',(-0.117948158721073,4.38502512853157E-5,
1.03256328852638));
#14584=CARTESIAN_POINT('Ctrl Pts',(-0.11796176292438,2.53781033017319E-5,
0.992436711473616));
#14585=CARTESIAN_POINT('Ctrl Pts',(-0.117851518882229,-0.0376119105440478,
0.994991052906992));
#14586=CARTESIAN_POINT('Ctrl Pts',(-0.077958511321084,-0.114458475672252,
1.00019278371463));
#14587=CARTESIAN_POINT('Ctrl Pts',(0.0529591494285269,-0.128760265574912,
1.00804190389653));
#14588=CARTESIAN_POINT('Ctrl Pts',(0.136912761112491,-0.0252739657289669,
1.0159840720193));
#14589=CARTESIAN_POINT('Ctrl Pts',(0.0954402180350474,0.101365883217864,
1.02392624014209));
#14590=CARTESIAN_POINT('Ctrl Pts',(-0.0334653697086341,0.135144169424284,
1.03186840826486));
#14591=CARTESIAN_POINT('Ctrl Pts',(-0.109792739119276,0.0652029671457737,
1.03803856537538));
#14592=CARTESIAN_POINT('Ctrl Pts',(-0.117762231070763,0.0130737646421874,
1.04156133311163));
#14593=CARTESIAN_POINT('Ctrl Pts',(-0.117667547954054,9.20194976846197E-5,
1.04243671147362));
#14594=CARTESIAN_POINT('Origin',(0.,0.,-0.0924367114736175));
#14595=CARTESIAN_POINT('',(-0.117585265278523,2.16484251076657E-5,0.932563288526384));
#14596=CARTESIAN_POINT('',(-0.117742563953077,-0.000107211314308964,0.942436711473616));
#14597=CARTESIAN_POINT('',(-0.117775,2.85464118895969E-14,-0.0924367114736175));
#14598=CARTESIAN_POINT('Ctrl Pts',(-0.117585265278523,2.16484251076635E-5,
0.932563288526384));
#14599=CARTESIAN_POINT('Ctrl Pts',(-0.117550805757046,-0.0209622679161363,
0.933975784751614));
#14600=CARTESIAN_POINT('Ctrl Pts',(-0.102172791552808,-0.0813069697478888,
0.938034610855947));
#14601=CARTESIAN_POINT('Ctrl Pts',(-0.00565790085648466,-0.139092177922979,
0.944739766839381));
#14602=CARTESIAN_POINT('Ctrl Pts',(0.113796373024222,-0.0801812402497705,
0.952678756476687));
#14603=CARTESIAN_POINT('Ctrl Pts',(0.129077866376032,0.0521301276928276,
0.960617746113992));
#14604=CARTESIAN_POINT('Ctrl Pts',(0.026197419344502,0.13671993644362,0.968556735751298));
#14605=CARTESIAN_POINT('Ctrl Pts',(-0.0906967139502387,0.0993396518733501,
0.975871916555428));
#14606=CARTESIAN_POINT('Ctrl Pts',(-0.117497098103867,0.02981894716558,
0.980540767480457));
#14607=CARTESIAN_POINT('Ctrl Pts',(-0.117771476475648,-0.000107683352847945,
0.982563288526384));
#14608=CARTESIAN_POINT('Ctrl Pts',(-0.117742563953077,-0.000107211314308957,
0.942436711473616));
#14609=CARTESIAN_POINT('Ctrl Pts',(-0.117833632602859,-0.0103126986533654,
0.943125993953839));
#14610=CARTESIAN_POINT('Ctrl Pts',(-0.111944766202914,-0.0596118697348184,
0.946462665808322));
#14611=CARTESIAN_POINT('Ctrl Pts',(-0.0428565117498991,-0.132465832952297,
0.952446727037066));
#14612=CARTESIAN_POINT('Ctrl Pts',(0.0880997963686447,-0.107806787258123,
0.960388895159846));
#14613=CARTESIAN_POINT('Ctrl Pts',(0.138347640177547,0.0156143509765511,
0.968331063282625));
#14614=CARTESIAN_POINT('Ctrl Pts',(0.061854832590724,0.124731139593481,
0.976273231405407));
#14615=CARTESIAN_POINT('Ctrl Pts',(-0.0713033562375951,0.119581390225944,
0.984215399528185));
#14616=CARTESIAN_POINT('Ctrl Pts',(-0.117322772537986,0.0417718924351975,
0.989603226217589));
#14617=CARTESIAN_POINT('Ctrl Pts',(-0.11796577882491,0.00139640554830399,
0.992343663532733));
#14618=CARTESIAN_POINT('Ctrl Pts',(-0.11796176292438,2.53781033017319E-5,
0.992436711473616));
#14619=CARTESIAN_POINT('Origin',(0.,0.,-0.0924367114736175));
#14620=CARTESIAN_POINT('',(-0.117850913371472,9.6525574830472E-5,0.882563288526384));
#14621=CARTESIAN_POINT('',(-0.117591231449503,3.54948526558943E-5,0.892436711473616));
#14622=CARTESIAN_POINT('',(-0.117775,2.85464118895969E-14,-0.0924367114736175));
#14623=CARTESIAN_POINT('Ctrl Pts',(-0.117850913371472,9.65255748304767E-5,
0.882563288526384));
#14624=CARTESIAN_POINT('Ctrl Pts',(-0.117563006813672,-0.0324172738354332,
0.884764472143669));
#14625=CARTESIAN_POINT('Ctrl Pts',(-0.0867151192651892,-0.104499852648429,
0.889611985640057));
#14626=CARTESIAN_POINT('Ctrl Pts',(0.0353397195745277,-0.134646760160997,
0.897105829015547));
#14627=CARTESIAN_POINT('Ctrl Pts',(0.132293719443212,-0.0433245611326863,
0.905044818652852));
#14628=CARTESIAN_POINT('Ctrl Pts',(0.108141885842356,0.0876583043865096,
0.912983808290157));
#14629=CARTESIAN_POINT('Ctrl Pts',(-0.0150064327997127,0.138395999855801,
0.920922797927463));
#14630=CARTESIAN_POINT('Ctrl Pts',(-0.104951114476159,0.0759553573435841,
0.927449291339539));
#14631=CARTESIAN_POINT('Ctrl Pts',(-0.117615366114572,0.01835136974357,
0.931329454872513));
#14632=CARTESIAN_POINT('Ctrl Pts',(-0.117585265278523,2.16484251076635E-5,
0.932563288526384));
#14633=CARTESIAN_POINT('Ctrl Pts',(-0.117591231449503,3.54948526559117E-5,
0.892436711473616));
#14634=CARTESIAN_POINT('Ctrl Pts',(-0.117532234588281,-0.0218238662162972,
0.893908324374946));
#14635=CARTESIAN_POINT('Ctrl Pts',(-0.101194437785642,-0.0830895288483654,
0.898027326650536));
#14636=CARTESIAN_POINT('Ctrl Pts',(-0.00250162451743248,-0.139203517821528,
0.904793718300386));
#14637=CARTESIAN_POINT('Ctrl Pts',(0.115632500949424,-0.0775435504945224,
0.912735886423165));
#14638=CARTESIAN_POINT('Ctrl Pts',(0.127835376168433,0.0551542754370876,
0.920678054545947));
#14639=CARTESIAN_POINT('Ctrl Pts',(0.0229279137899797,0.137325118854324,
0.928620222668725));
#14640=CARTESIAN_POINT('Ctrl Pts',(-0.0920562790907298,0.0974788594069619,
0.935873108311283));
#14641=CARTESIAN_POINT('Ctrl Pts',(-0.117483857027998,0.0288844367965532,
0.94047860457958));
#14642=CARTESIAN_POINT('Ctrl Pts',(-0.117742563953077,-0.000107211314308957,
0.942436711473616));
#14643=CARTESIAN_POINT('Origin',(0.,0.,-0.0924367114736175));
#14644=CARTESIAN_POINT('',(-0.11789232318732,-8.18790992476613E-5,0.832563288526384));
#14645=CARTESIAN_POINT('',(-0.117872825429845,8.99519344067963E-5,0.842436711473616));
#14646=CARTESIAN_POINT('',(-0.117775,2.85464118895969E-14,-0.0924367114736175));
#14647=CARTESIAN_POINT('Ctrl Pts',(-0.11789232318732,-8.18790992476734E-5,
0.832563288526384));
#14648=CARTESIAN_POINT('Ctrl Pts',(-0.117932494517479,-0.00515170743829337,
0.832906829656623));
#14649=CARTESIAN_POINT('Ctrl Pts',(-0.115332713682068,-0.0492334187378749,
0.835896700665964));
#14650=CARTESIAN_POINT('Ctrl Pts',(-0.059752088941783,-0.125731196083361,
0.841532901554406));
#14651=CARTESIAN_POINT('Ctrl Pts',(0.0732361146625898,-0.118385460722959,
0.849471891191712));
#14652=CARTESIAN_POINT('Ctrl Pts',(0.139181674492094,-0.00266594955618734,
0.857410880829018));
#14653=CARTESIAN_POINT('Ctrl Pts',(0.077715950067195,0.115494055719818,
0.865349870466323));
#14654=CARTESIAN_POINT('Ctrl Pts',(-0.0548934004223171,0.127927168308903,
0.87328886010363));
#14655=CARTESIAN_POINT('Ctrl Pts',(-0.114416768398411,0.0522742940766184,
0.879026666123649));
#14656=CARTESIAN_POINT('Ctrl Pts',(-0.117909136832228,0.0066718045071592,
0.882118142264567));
#14657=CARTESIAN_POINT('Ctrl Pts',(-0.117850913371472,9.65255748304767E-5,
0.882563288526384));
#14658=CARTESIAN_POINT('Ctrl Pts',(-0.117872825429845,8.99519344067998E-5,
0.842436711473616));
#14659=CARTESIAN_POINT('Ctrl Pts',(-0.117591169542271,-0.0331870933343037,
0.844690654796053));
#14660=CARTESIAN_POINT('Ctrl Pts',(-0.0854771005934613,-0.106025606004136,
0.84959198749275));
#14661=CARTESIAN_POINT('Ctrl Pts',(0.0380692928980519,-0.133920149482284,
0.857140709563706));
#14662=CARTESIAN_POINT('Ctrl Pts',(0.133179650076608,-0.0405839661022353,
0.865082877686486));
#14663=CARTESIAN_POINT('Ctrl Pts',(0.106283765719693,0.0899312995767124,
0.873025045809266));
#14664=CARTESIAN_POINT('Ctrl Pts',(-0.0179789669825735,0.138060255849953,
0.880967213932046));
#14665=CARTESIAN_POINT('Ctrl Pts',(-0.105798194743126,0.0742290978659706,
0.887437769153496));
#14666=CARTESIAN_POINT('Ctrl Pts',(-0.117638368248411,0.0175004969839459,
0.891260935000686));
#14667=CARTESIAN_POINT('Ctrl Pts',(-0.117591231449503,3.54948526559117E-5,
0.892436711473616));
#14668=CARTESIAN_POINT('Origin',(0.,0.,-0.0924367114736175));
#14669=CARTESIAN_POINT('',(-0.117598114366551,-4.51832715892789E-5,0.782563288526384));
#14670=CARTESIAN_POINT('',(-0.117874685330111,-8.92836445515327E-5,0.792436711473617));
#14671=CARTESIAN_POINT('',(-0.117775,2.85464118895969E-14,-0.0924367114736175));
#14672=CARTESIAN_POINT('Ctrl Pts',(-0.117598114366551,-4.518327158929E-5,
0.782563288526384));
#14673=CARTESIAN_POINT('Ctrl Pts',(-0.117656123976761,-0.0168608793038394,
0.783695517048678));
#14674=CARTESIAN_POINT('Ctrl Pts',(-0.106420815930739,-0.0729055463807818,
0.787474075450074));
#14675=CARTESIAN_POINT('Ctrl Pts',(-0.0202952816069424,-0.137719814645367,
0.793898963730571));
#14676=CARTESIAN_POINT('Ctrl Pts',(0.104705698854998,-0.0917352845351548,
0.801837953367879));
#14677=CARTESIAN_POINT('Ctrl Pts',(0.133855787965376,0.0382266115373486,
0.809776943005182));
#14678=CARTESIAN_POINT('Ctrl Pts',(0.0404700769297216,0.133194664588195,
0.81771593264249));
#14679=CARTESIAN_POINT('Ctrl Pts',(-0.0843190215395119,0.107398870964955,
0.825311381149555));
#14680=CARTESIAN_POINT('Ctrl Pts',(-0.117623050954756,0.0339016606582783,
0.830260499777521));
#14681=CARTESIAN_POINT('Ctrl Pts',(-0.11789232318732,-8.18790992476734E-5,
0.832563288526384));
#14682=CARTESIAN_POINT('Ctrl Pts',(-0.117874685330111,-8.9283644551537E-5,
0.792436711473617));
#14683=CARTESIAN_POINT('Ctrl Pts',(-0.11792303416021,-0.00583050672374999,
0.7928255958429));
#14684=CARTESIAN_POINT('Ctrl Pts',(-0.114931453360353,-0.0506053896743902,
0.795861869586443));
#14685=CARTESIAN_POINT('Ctrl Pts',(-0.0575513573065257,-0.126774282767806,
0.801545532704245));
#14686=CARTESIAN_POINT('Ctrl Pts',(0.0753527000357912,-0.117071978271622,
0.809487700827026));
#14687=CARTESIAN_POINT('Ctrl Pts',(0.139225942868322,-0.000119714417332432,
0.817429868949805));
#14688=CARTESIAN_POINT('Ctrl Pts',(0.0755539188089132,0.116942220141962,
0.825372037072586));
#14689=CARTESIAN_POINT('Ctrl Pts',(-0.0573332568284509,0.12687306712048,
0.833314205195366));
#14690=CARTESIAN_POINT('Ctrl Pts',(-0.114890414736801,0.0507419104293215,
0.839002429995709));
#14691=CARTESIAN_POINT('Ctrl Pts',(-0.117921990994851,0.00589875908008548,
0.842043265421793));
#14692=CARTESIAN_POINT('Ctrl Pts',(-0.117872825429845,8.99519344067998E-5,
0.842436711473616));
#14693=CARTESIAN_POINT('Origin',(0.,0.,-0.0924367114736175));
#14694=CARTESIAN_POINT('',(-0.11772691567491,0.000105512987197037,0.732563288526384));
#14695=CARTESIAN_POINT('',(-0.117591850253004,-3.65476421498312E-5,0.742436711473616));
#14696=CARTESIAN_POINT('',(-0.117775,2.85464118895969E-14,-0.0924367114736175));
#14697=CARTESIAN_POINT('Ctrl Pts',(-0.11772691567491,0.000105512987197042,
0.732563288526384));
#14698=CARTESIAN_POINT('Ctrl Pts',(-0.117479624464894,-0.0283451130369189,
0.734484204440733));
#14699=CARTESIAN_POINT('Ctrl Pts',(-0.0928318426870313,-0.096374559506161,
0.739051450234184));
#14700=CARTESIAN_POINT('Ctrl Pts',(0.0209425314183671,-0.137622876656644,
0.746265025906738));
#14701=CARTESIAN_POINT('Ctrl Pts',(0.126986869252672,-0.0570349089493802,
0.754204015544043));
#14702=CARTESIAN_POINT('Ctrl Pts',(0.11678343126468,0.0757646090434518,
0.762143005181349));
#14703=CARTESIAN_POINT('Ctrl Pts',(-0.000327234354877375,0.139206819944772,
0.770081994818654));
#14704=CARTESIAN_POINT('Ctrl Pts',(-0.100479183608201,0.0843410365921374,
0.776888755933667));
#14705=CARTESIAN_POINT('Ctrl Pts',(-0.117520539541507,0.0224420334666934,
0.781049187169576));
#14706=CARTESIAN_POINT('Ctrl Pts',(-0.117598114366551,-4.518327158929E-5,
0.782563288526384));
#14707=CARTESIAN_POINT('Ctrl Pts',(-0.117591850253004,-3.65476421498364E-5,
0.742436711473616));
#14708=CARTESIAN_POINT('Ctrl Pts',(-0.117640211257931,-0.0174335619022046,
0.743607926264006));
#14709=CARTESIAN_POINT('Ctrl Pts',(-0.105863856762799,-0.0740921523660566,
0.747426530428656));
#14710=CARTESIAN_POINT('Ctrl Pts',(-0.0182163644075178,-0.138029133036789,
0.753892523967566));
#14711=CARTESIAN_POINT('Ctrl Pts',(0.106128952536144,-0.0901139441634624,
0.761834692090347));
#14712=CARTESIAN_POINT('Ctrl Pts',(0.133249245915149,0.0403548753208232,
0.769776860213125));
#14713=CARTESIAN_POINT('Ctrl Pts',(0.0382995408207276,0.133854483197375,
0.777719028335907));
#14714=CARTESIAN_POINT('Ctrl Pts',(-0.0853693283863186,0.106155717082476,
0.785272312089402));
#14715=CARTESIAN_POINT('Ctrl Pts',(-0.117593892160246,0.0332537408718532,
0.79017820646864));
#14716=CARTESIAN_POINT('Ctrl Pts',(-0.117874685330111,-8.9283644551537E-5,
0.792436711473617));
#14717=CARTESIAN_POINT('Origin',(0.,0.,-0.0924367114736175));
#14718=CARTESIAN_POINT('',(-0.117964947617991,-1.73329198795185E-5,0.682563288526384));
#14719=CARTESIAN_POINT('',(-0.117740574064672,0.000107068518266168,0.692436711473616));
#14720=CARTESIAN_POINT('',(-0.117775,2.85464118895969E-14,-0.0924367114736175));
#14721=CARTESIAN_POINT('Ctrl Pts',(-0.117964947617991,-1.73329198795367E-5,
0.682563288526384));
#14722=CARTESIAN_POINT('Ctrl Pts',(-0.117966864156947,-0.000949576032666658,
0.682626561953687));
#14723=CARTESIAN_POINT('Ctrl Pts',(-0.117534558560489,-0.0408698671952461,
0.685336165260092));
#14724=CARTESIAN_POINT('Ctrl Pts',(-0.0726787294560835,-0.118728463672822,
0.690692098445597));
#14725=CARTESIAN_POINT('Ctrl Pts',(0.0603425395611779,-0.125448888878168,
0.698631088082904));
#14726=CARTESIAN_POINT('Ctrl Pts',(0.138124349154501,-0.0173294538893964,
0.706570077720209));
#14727=CARTESIAN_POINT('Ctrl Pts',(0.0894627833767505,0.106653908470079,
0.714509067357515));
#14728=CARTESIAN_POINT('Ctrl Pts',(-0.0410958292974484,0.133002927094911,
0.72244805699482));
#14729=CARTESIAN_POINT('Ctrl Pts',(-0.111546724107196,0.0606813038481789,
0.728466130717777));
#14730=CARTESIAN_POINT('Ctrl Pts',(-0.117820302634623,0.0108495967181263,
0.731837874561632));
#14731=CARTESIAN_POINT('Ctrl Pts',(-0.11772691567491,0.000105512987197042,
0.732563288526384));
#14732=CARTESIAN_POINT('Ctrl Pts',(-0.117740574064672,0.000107068518266165,
0.692436711473616));
#14733=CARTESIAN_POINT('Ctrl Pts',(-0.117483171888848,-0.0288182833237499,
0.694390256685113));
#14734=CARTESIAN_POINT('Ctrl Pts',(-0.0921515028359353,-0.0973455904149804,
0.698991191270869));
#14735=CARTESIAN_POINT('Ctrl Pts',(0.022691720100341,-0.137364345221032,
0.706239515230886));
#14736=CARTESIAN_POINT('Ctrl Pts',(0.127740337615313,-0.0553740340325759,
0.714181683353665));
#14737=CARTESIAN_POINT('Ctrl Pts',(0.115765682611161,0.077344581120379,
0.722123851476446));
#14738=CARTESIAN_POINT('Ctrl Pts',(-0.00226223072526165,0.139207614056346,
0.730066019599226));
#14739=CARTESIAN_POINT('Ctrl Pts',(-0.101117998472899,0.083225715609228,
0.736836972931616));
#14740=CARTESIAN_POINT('Ctrl Pts',(-0.117530897055598,0.0218902846491045,
0.740960536889746));
#14741=CARTESIAN_POINT('Ctrl Pts',(-0.117591850253004,-3.65476421498364E-5,
0.742436711473616));
#14742=CARTESIAN_POINT('Origin',(0.,0.,-0.0924367114736175));
#14743=CARTESIAN_POINT('',(-0.117676160015555,-9.46906955630148E-5,0.632563288526383));
#14744=CARTESIAN_POINT('',(-0.117962383120995,-2.41598447144192E-5,0.642436711473616));
#14745=CARTESIAN_POINT('',(-0.117775,2.85464118895969E-14,-0.0924367114736175));
#14746=CARTESIAN_POINT('Ctrl Pts',(-0.117676160015555,-9.46906955630045E-5,
0.632563288526383));
#14747=CARTESIAN_POINT('Ctrl Pts',(-0.117771520970562,-0.0127268345011372,
0.633415249345741));
#14748=CARTESIAN_POINT('Ctrl Pts',(-0.110078248258936,-0.064483421762156,
0.636913540044201));
#14749=CARTESIAN_POINT('Ctrl Pts',(-0.0347063025259737,-0.134811417789573,
0.643058160621763));
#14750=CARTESIAN_POINT('Ctrl Pts',(0.0944472082050275,-0.102266175560326,
0.65099715025907));
#14751=CARTESIAN_POINT('Ctrl Pts',(0.137140772714236,0.0238967416356601,
0.658936139896373));
#14752=CARTESIAN_POINT('Ctrl Pts',(0.054291358674537,0.128183829614862,
0.666875129533682));
#14753=CARTESIAN_POINT('Ctrl Pts',(-0.0772016597727435,0.11523146575827,
0.674750845743682));
#14754=CARTESIAN_POINT('Ctrl Pts',(-0.117886707375211,0.0380402955314478,
0.679980232074585));
#14755=CARTESIAN_POINT('Ctrl Pts',(-0.117964947617991,-1.73329198795367E-5,
0.682563288526384));
#14756=CARTESIAN_POINT('Ctrl Pts',(-0.117962383120995,-2.41598447144253E-5,
0.642436711473616));
#14757=CARTESIAN_POINT('Ctrl Pts',(-0.117966033213387,-0.0013279541977536,
0.642525197731959));
#14758=CARTESIAN_POINT('Ctrl Pts',(-0.117355585052125,-0.0416360146359673,
0.645261073364563));
#14759=CARTESIAN_POINT('Ctrl Pts',(-0.0715088964667609,-0.119458592094588,
0.650644338371427));
#14760=CARTESIAN_POINT('Ctrl Pts',(0.0616402393688536,-0.124837327709565,
0.658586506494205));
#14761=CARTESIAN_POINT('Ctrl Pts',(0.138320583400205,-0.0158522461166236,
0.666528674616987));
#14762=CARTESIAN_POINT('Ctrl Pts',(0.0882850628235238,0.107655121482266,
0.674470842739765));
#14763=CARTESIAN_POINT('Ctrl Pts',(-0.0426286451686149,0.132539337972556,
0.682413010862546));
#14764=CARTESIAN_POINT('Ctrl Pts',(-0.111894847147975,0.059748848130285,
0.68840163377383));
#14765=CARTESIAN_POINT('Ctrl Pts',(-0.117831996057943,0.0103805377030848,
0.691742867310853));
#14766=CARTESIAN_POINT('Ctrl Pts',(-0.117740574064672,0.000107068518266165,
0.692436711473616));
#14767=CARTESIAN_POINT('Origin',(0.,0.,-0.0924367114736175));
#14768=CARTESIAN_POINT('',(-0.117626285855324,7.11112359239178E-5,0.582563288526384));
#14769=CARTESIAN_POINT('',(-0.11766919235599,-9.26074537421634E-5,0.592436711473616));
#14770=CARTESIAN_POINT('',(-0.117775,2.85464118895969E-14,-0.0924367114736175));
#14771=CARTESIAN_POINT('Ctrl Pts',(-0.117626285855324,7.11112359239024E-5,
0.582563288526383));
#14772=CARTESIAN_POINT('Ctrl Pts',(-0.117492102008102,-0.0242809575267813,
0.584203936737797));
#14773=CARTESIAN_POINT('Ctrl Pts',(-0.0982512120079041,-0.0881067492982899,
0.588490914828312));
#14774=CARTESIAN_POINT('Ctrl Pts',(0.00631176444456456,-0.139064040754811,
0.595424222797929));
#14775=CARTESIAN_POINT('Ctrl Pts',(0.120263693490807,-0.0701091280034811,
0.603363212435234));
#14776=CARTESIAN_POINT('Ctrl Pts',(0.124122453355413,0.0630258865426945,
0.611302202072541));
#14777=CARTESIAN_POINT('Ctrl Pts',(0.0143556138404206,0.138465021405133,
0.619241191709845));
#14778=CARTESIAN_POINT('Ctrl Pts',(-0.0953630726970595,0.0926558297308384,
0.626328220527794));
#14779=CARTESIAN_POINT('Ctrl Pts',(-0.117475314221613,0.0265106736450616,
0.630768919466639));
#14780=CARTESIAN_POINT('Ctrl Pts',(-0.117676160015555,-9.46906955630045E-5,
0.632563288526383));
#14781=CARTESIAN_POINT('Ctrl Pts',(-0.11766919235599,-9.26074537421669E-5,
0.592436711473616));
#14782=CARTESIAN_POINT('Ctrl Pts',(-0.117764072896019,-0.0130062487266101,
0.593307528153066));
#14783=CARTESIAN_POINT('Ctrl Pts',(-0.109848366281979,-0.0650658641993071,
0.596825734206776));
#14784=CARTESIAN_POINT('Ctrl Pts',(-0.0336977294021144,-0.135086418755761,
0.602991329634746));
#14785=CARTESIAN_POINT('Ctrl Pts',(0.0952657566843092,-0.101529863106778,
0.610933497757526));
#14786=CARTESIAN_POINT('Ctrl Pts',(0.136956022624868,0.025038477707157,
0.618875665880307));
#14787=CARTESIAN_POINT('Ctrl Pts',(0.0531805018142573,0.128669000640787,
0.626817834003085));
#14788=CARTESIAN_POINT('Ctrl Pts',(-0.0778376600742765,0.114584191752874,
0.634671515867523));
#14789=CARTESIAN_POINT('Ctrl Pts',(-0.117856827377429,0.0376798124439797,
0.639877808357699));
#14790=CARTESIAN_POINT('Ctrl Pts',(-0.117962383120995,-2.41598447144253E-5,
0.642436711473616));
#14791=CARTESIAN_POINT('Origin',(0.,0.,-0.0924367114736175));
#14792=CARTESIAN_POINT('',(-0.117934829819181,5.63106208242181E-5,0.532563288526383));
#14793=CARTESIAN_POINT('',(-0.117629301205424,7.34277634442948E-5,0.542436711473615));
#14794=CARTESIAN_POINT('',(-0.117775,2.85464118895969E-14,-0.0924367114736175));
#14795=CARTESIAN_POINT('Ctrl Pts',(-0.117934829819181,5.63106208242166E-5,
0.532563288526383));
#14796=CARTESIAN_POINT('Ctrl Pts',(-0.117723349859012,-0.0357608023914865,
0.534992624129852));
#14797=CARTESIAN_POINT('Ctrl Pts',(-0.0811985738067347,-0.110967619805887,
0.540068289612422));
#14798=CARTESIAN_POINT('Ctrl Pts',(0.0467759446245483,-0.131113145053959,
0.547790284974095));
#14799=CARTESIAN_POINT('Ctrl Pts',(0.135526478334676,-0.031799677225719,
0.555729274611401));
#14800=CARTESIAN_POINT('Ctrl Pts',(0.100211809365564,0.0966242157284558,
0.563668264248707));
#14801=CARTESIAN_POINT('Ctrl Pts',(-0.0268399031138932,0.136595261273209,
0.571607253886012));
#14802=CARTESIAN_POINT('Ctrl Pts',(-0.108142973925314,0.0691035501437442,
0.577905595311905));
#14803=CARTESIAN_POINT('Ctrl Pts',(-0.117708537635025,0.0149983997031143,
0.581557606858695));
#14804=CARTESIAN_POINT('Ctrl Pts',(-0.117626285855324,7.11112359239024E-5,
0.582563288526383));
#14805=CARTESIAN_POINT('Ctrl Pts',(-0.117629301205424,7.34277634442983E-5,
0.542436711473615));
#14806=CARTESIAN_POINT('Ctrl Pts',(-0.11748956090956,-0.0244625652698295,
0.544089858574172));
#14807=CARTESIAN_POINT('Ctrl Pts',(-0.0980201725405651,-0.0884941619373469,
0.548390395048989));
#14808=CARTESIAN_POINT('Ctrl Pts',(0.00702343738442799,-0.139048728244533,
0.555338320898066));
#14809=CARTESIAN_POINT('Ctrl Pts',(0.12066450826877,-0.0694546898587181,
0.563280489020846));
#14810=CARTESIAN_POINT('Ctrl Pts',(0.123764493242992,0.063766979789076,
0.571222657143626));
#14811=CARTESIAN_POINT('Ctrl Pts',(0.0134834875971477,0.13857154491934,
0.579164825266405));
#14812=CARTESIAN_POINT('Ctrl Pts',(-0.0957036897026042,0.092147346049863,
0.586236176709736));
#14813=CARTESIAN_POINT('Ctrl Pts',(-0.117475624432153,0.0262528025703711,
0.590660138778806));
#14814=CARTESIAN_POINT('Ctrl Pts',(-0.11766919235599,-9.26074537421669E-5,
0.592436711473616));
#14815=CARTESIAN_POINT('Origin',(0.,0.,-0.0924367114736175));
#14816=CARTESIAN_POINT('',(-0.117794891956694,-0.000106411733115368,0.482563288526384));
#14817=CARTESIAN_POINT('',(-0.117936566864074,5.52347650140707E-5,0.492436711473616));
#14818=CARTESIAN_POINT('',(-0.117775,2.85464118895969E-14,-0.0924367114736175));
#14819=CARTESIAN_POINT('Ctrl Pts',(-0.117794891956694,-0.000106411733115381,
0.482563288526384));
#14820=CARTESIAN_POINT('Ctrl Pts',(-0.117872998614688,-0.00856127641466401,
0.483134981642805));
#14821=CARTESIAN_POINT('Ctrl Pts',(-0.113184542395844,-0.0560672187853419,
0.486353004638329));
#14822=CARTESIAN_POINT('Ctrl Pts',(-0.0487302328423073,-0.130399425645183,
0.492217357512954));
#14823=CARTESIAN_POINT('Ctrl Pts',(0.0831353173341669,-0.111656458896056,
0.50015634715026));
#14824=CARTESIAN_POINT('Ctrl Pts',(0.13889618212661,0.00930034365552528,
0.508095336787567));
#14825=CARTESIAN_POINT('Ctrl Pts',(0.0675071113591811,0.12174331898465,
0.516034326424871));
#14826=CARTESIAN_POINT('Ctrl Pts',(-0.0656800932930844,0.122738629397884,
0.523973316062178));
#14827=CARTESIAN_POINT('Ctrl Pts',(-0.116384786286051,0.04545243224792,
0.529482970096015));
#14828=CARTESIAN_POINT('Ctrl Pts',(-0.117953719733239,0.00325558390455253,
0.53234629425075));
#14829=CARTESIAN_POINT('Ctrl Pts',(-0.117934829819181,5.63106208242166E-5,
0.532563288526383));
#14830=CARTESIAN_POINT('Ctrl Pts',(-0.117936566864074,5.52347650140663E-5,
0.492436711473616));
#14831=CARTESIAN_POINT('Ctrl Pts',(-0.117728017843002,-0.0358510361847084,
0.494872188995279));
#14832=CARTESIAN_POINT('Ctrl Pts',(-0.0810366231971402,-0.111156550628637,
0.499955055891203));
#14833=CARTESIAN_POINT('Ctrl Pts',(0.0471380885036503,-0.131003351527116,
0.507685312161385));
#14834=CARTESIAN_POINT('Ctrl Pts',(0.135643160584381,-0.031381690295376,
0.515627480284167));
#14835=CARTESIAN_POINT('Ctrl Pts',(0.0998851624184703,0.0969888232104648,
0.523569648406945));
#14836=CARTESIAN_POINT('Ctrl Pts',(-0.0273779061153799,0.136507610615132,
0.531511816529727));
#14837=CARTESIAN_POINT('Ctrl Pts',(-0.108290992649607,0.0687756007668377,
0.537800837551949));
#14838=CARTESIAN_POINT('Ctrl Pts',(-0.117713344367368,0.0148299618267192,
0.541442469199912));
#14839=CARTESIAN_POINT('Ctrl Pts',(-0.117629301205424,7.34277634442983E-5,
0.542436711473615));
#14840=CARTESIAN_POINT('Origin',(0.,0.,-0.0924367114736175));
#14841=CARTESIAN_POINT('',(-0.117582256074849,9.06819982020624E-6,0.432563288526383));
#14842=CARTESIAN_POINT('',(-0.11779560903417,-0.000106574656651148,0.442436711473616));
#14843=CARTESIAN_POINT('',(-0.117775,2.85464118895969E-14,-0.0924367114736175));
#14844=CARTESIAN_POINT('Ctrl Pts',(-0.117582256074849,9.06819982019261E-6,
0.432563288526383));
#14845=CARTESIAN_POINT('Ctrl Pts',(-0.117568373935691,-0.020201912089319,
0.43392366903486));
#14846=CARTESIAN_POINT('Ctrl Pts',(-0.10300922874285,-0.0797477867736473,
0.437930379422439));
#14847=CARTESIAN_POINT('Ctrl Pts',(-0.00838939967687663,-0.138954178686792,
0.44458341968912));
#14848=CARTESIAN_POINT('Ctrl Pts',(0.11219917790857,-0.0824013973067221,
0.452522409326426));
#14849=CARTESIAN_POINT('Ctrl Pts',(0.13007709763057,0.0495842159710775,
0.460461398963732));
#14850=CARTESIAN_POINT('Ctrl Pts',(0.0288783492374893,0.136178877755608,
0.468400388601037));
#14851=CARTESIAN_POINT('Ctrl Pts',(-0.0895654556576369,0.100852400902523,
0.475767685121922));
#14852=CARTESIAN_POINT('Ctrl Pts',(-0.117511448025972,0.0305757367622385,
0.480488651763704));
#14853=CARTESIAN_POINT('Ctrl Pts',(-0.117794891956694,-0.000106411733115381,
0.482563288526384));
#14854=CARTESIAN_POINT('Ctrl Pts',(-0.11779560903417,-0.000106574656651151,
0.442436711473616));
#14855=CARTESIAN_POINT('Ctrl Pts',(-0.117873644338608,-0.00854245500997505,
0.443007130042126));
#14856=CARTESIAN_POINT('Ctrl Pts',(-0.113196618671047,-0.056044542179559,
0.446224937984896));
#14857=CARTESIAN_POINT('Ctrl Pts',(-0.0487473834415776,-0.130413074907061,
0.452090135301926));
#14858=CARTESIAN_POINT('Ctrl Pts',(0.0831820848081396,-0.111645054821459,
0.460032303424706));
#14859=CARTESIAN_POINT('Ctrl Pts',(0.138908217753341,0.00940130521287039,
0.467974471547486));
#14860=CARTESIAN_POINT('Ctrl Pts',(0.0673801526530663,0.121835103839429,
0.475916639670265));
#14861=CARTESIAN_POINT('Ctrl Pts',(-0.0658750545035054,0.12265543075329,
0.483858807793047));
#14862=CARTESIAN_POINT('Ctrl Pts',(-0.116424939330292,0.0453161125527027,
0.489365498394162));
#14863=CARTESIAN_POINT('Ctrl Pts',(-0.11795471279604,0.00317945345687678,
0.492224799621019));
#14864=CARTESIAN_POINT('Ctrl Pts',(-0.117936566864074,5.52347650140663E-5,
0.492436711473616));
#14865=CARTESIAN_POINT('Origin',(0.,0.,-0.0924367114736175));
#14866=CARTESIAN_POINT('',(-0.117828183671793,0.000101754196006455,0.382563288526383));
#14867=CARTESIAN_POINT('',(-0.117581664177921,7.09484545444172E-6,0.392436711473616));
#14868=CARTESIAN_POINT('',(-0.117775,2.85464118895969E-14,-0.0924367114736175));
#14869=CARTESIAN_POINT('Ctrl Pts',(-0.117828183671793,0.000101754196006446,
0.382563288526384));
#14870=CARTESIAN_POINT('Ctrl Pts',(-0.117538790254565,-0.0316580736410773,
0.384712356426916));
#14871=CARTESIAN_POINT('Ctrl Pts',(-0.0879068326507716,-0.103002379129266,
0.38950775420655));
#14872=CARTESIAN_POINT('Ctrl Pts',(0.0326876424682324,-0.135315053971568,
0.396949481865287));
#14873=CARTESIAN_POINT('Ctrl Pts',(0.13141703692502,-0.0459152284901983,
0.404888471502591));
#14874=CARTESIAN_POINT('Ctrl Pts',(0.109843140674695,0.0855168418978295,
0.412827461139898));
#14875=CARTESIAN_POINT('Ctrl Pts',(-0.0122846228212416,0.13866410438033,
0.420766450777203));
#14876=CARTESIAN_POINT('Ctrl Pts',(-0.104166535924894,0.0775181589932739,
0.427345059906032));
#14877=CARTESIAN_POINT('Ctrl Pts',(-0.117595378674006,0.0191142356295008,
0.431277339155758));
#14878=CARTESIAN_POINT('Ctrl Pts',(-0.117582256074849,9.06819982019261E-6,
0.432563288526383));
#14879=CARTESIAN_POINT('Ctrl Pts',(-0.117581664177921,7.09484545444172E-6,
0.392436711473616));
#14880=CARTESIAN_POINT('Ctrl Pts',(-0.117570873504463,-0.0200907396801347,
0.393789460463232));
#14881=CARTESIAN_POINT('Ctrl Pts',(-0.10312708440739,-0.079535468422451,
0.397789598827109));
#14882=CARTESIAN_POINT('Ctrl Pts',(-0.00873482453528946,-0.138951719454826,
0.404437126565246));
#14883=CARTESIAN_POINT('Ctrl Pts',(0.112042812448737,-0.0826455423945668,
0.412379294688026));
#14884=CARTESIAN_POINT('Ctrl Pts',(0.130177722634257,0.049372441998279,
0.420321462810806));
#14885=CARTESIAN_POINT('Ctrl Pts',(0.0290564652212241,0.136160197297018,
0.428263630933586));
#14886=CARTESIAN_POINT('Ctrl Pts',(-0.0895090212855029,0.100936776489487,
0.435635380487856));
#14887=CARTESIAN_POINT('Ctrl Pts',(-0.117511471984497,0.0306096014671689,
0.440359740667866));
#14888=CARTESIAN_POINT('Ctrl Pts',(-0.11779560903417,-0.000106574656651151,
0.442436711473616));
#14889=CARTESIAN_POINT('Origin',(0.,0.,-0.0924367114736175));
#14890=CARTESIAN_POINT('',(-0.117911328466355,-7.22474488887591E-5,0.332563288526384));
#14891=CARTESIAN_POINT('',(-0.117821685414254,0.000103165543095151,0.342436711473616));
#14892=CARTESIAN_POINT('',(-0.117775,2.85464118895969E-14,-0.0924367114736175));
#14893=CARTESIAN_POINT('Ctrl Pts',(-0.117911328466355,-7.22474488887752E-5,
0.332563288526384));
#14894=CARTESIAN_POINT('Ctrl Pts',(-0.117942332027964,-0.00437115939612809,
0.332854713939869));
#14895=CARTESIAN_POINT('Ctrl Pts',(-0.115777752883067,-0.0476754067323583,
0.335792469232457));
#14896=CARTESIAN_POINT('Ctrl Pts',(-0.0622106591311991,-0.12453304658572,
0.341376554404146));
#14897=CARTESIAN_POINT('Ctrl Pts',(0.0708961914151981,-0.119801401679107,
0.349315544041452));
#14898=CARTESIAN_POINT('Ctrl Pts',(0.1391024375543,-0.00539978406154301,
0.357254533678757));
#14899=CARTESIAN_POINT('Ctrl Pts',(0.0799699354250877,0.113944965792994,
0.365193523316063));
#14900=CARTESIAN_POINT('Ctrl Pts',(-0.0523695618881846,0.128980908622551,
0.373132512953369));
#14901=CARTESIAN_POINT('Ctrl Pts',(-0.113921748517257,0.0538356345748906,
0.378922434690143));
#14902=CARTESIAN_POINT('Ctrl Pts',(-0.117895144954496,0.00745050051778832,
0.382066026547814));
#14903=CARTESIAN_POINT('Ctrl Pts',(-0.117828183671793,0.000101754196006446,
0.382563288526384));
#14904=CARTESIAN_POINT('Ctrl Pts',(-0.117821685414254,0.000103165543095145,
0.342436711473616));
#14905=CARTESIAN_POINT('Ctrl Pts',(-0.117532262555972,-0.0314544122979593,
0.344571790884339));
#14906=CARTESIAN_POINT('Ctrl Pts',(-0.0882170202347594,-0.102616110661261,
0.349354259669323));
#14907=CARTESIAN_POINT('Ctrl Pts',(0.0320320385160992,-0.135491055083419,
0.356784117828566));
#14908=CARTESIAN_POINT('Ctrl Pts',(0.131227975626944,-0.0465090949381858,
0.364726285951346));
#14909=CARTESIAN_POINT('Ctrl Pts',(0.110205605501345,0.0850799742312894,
0.372668454074126));
#14910=CARTESIAN_POINT('Ctrl Pts',(-0.0117764211155082,0.138727046407055,
0.380610622196906));
#14911=CARTESIAN_POINT('Ctrl Pts',(-0.10403099481448,0.0777947493501838,
0.387200041330069));
#14912=CARTESIAN_POINT('Ctrl Pts',(-0.117591991327853,0.019241607989002,
0.391142071088973));
#14913=CARTESIAN_POINT('Ctrl Pts',(-0.117581664177921,7.09484545444172E-6,
0.392436711473616));
#14914=CARTESIAN_POINT('Origin',(0.,0.,-0.0924367114736175));
#14915=CARTESIAN_POINT('',(-0.117608153246896,-5.64262068778628E-5,0.282563288526383));
#14916=CARTESIAN_POINT('',(-0.117918861549493,-6.80329776671096E-5,0.292436711473615));
#14917=CARTESIAN_POINT('',(-0.117775,2.85464118895969E-14,-0.0924367114736175));
#14918=CARTESIAN_POINT('Ctrl Pts',(-0.117608153246896,-5.64262068778604E-5,
0.282563288526383));
#14919=CARTESIAN_POINT('Ctrl Pts',(-0.117677606263852,-0.0160946837114709,
0.283643401331924));
#14920=CARTESIAN_POINT('Ctrl Pts',(-0.107144424846824,-0.0713401098021974,
0.287369844016567));
#14921=CARTESIAN_POINT('Ctrl Pts',(-0.0229969941138309,-0.137294515779738,
0.293742616580312));
#14922=CARTESIAN_POINT('Ctrl Pts',(0.102883268653204,-0.0937746172089793,
0.301681606217617));
#14923=CARTESIAN_POINT('Ctrl Pts',(0.134580950019115,0.0355895166223291,
0.309620595854923));
#14924=CARTESIAN_POINT('Ctrl Pts',(0.0430789950773988,0.13237388709478,
0.317559585492229));
#14925=CARTESIAN_POINT('Ctrl Pts',(-0.0830523456774332,0.10887452531409,
0.325207149716049));
#14926=CARTESIAN_POINT('Ctrl Pts',(-0.11766079978112,0.0346657214219864,
0.330208384060767));
#14927=CARTESIAN_POINT('Ctrl Pts',(-0.117911328466355,-7.22474488887752E-5,
0.332563288526384));
#14928=CARTESIAN_POINT('Ctrl Pts',(-0.117918861549493,-6.80329776671157E-5,
0.292436711473616));
#14929=CARTESIAN_POINT('Ctrl Pts',(-0.117946256357307,-0.00405052459867665,
0.292706731931186));
#14930=CARTESIAN_POINT('Ctrl Pts',(-0.11595553950755,-0.0470512577090033,
0.295624141763016));
#14931=CARTESIAN_POINT('Ctrl Pts',(-0.0631725212350128,-0.124068972994571,
0.301188940969106));
#14932=CARTESIAN_POINT('Ctrl Pts',(0.0700327441786229,-0.12032993078169,
0.309131109091886));
#14933=CARTESIAN_POINT('Ctrl Pts',(0.139080821187468,-0.00635631000930847,
0.317073277214666));
#14934=CARTESIAN_POINT('Ctrl Pts',(0.0807165776729536,0.11344034374014,
0.325015445337446));
#14935=CARTESIAN_POINT('Ctrl Pts',(-0.0515923433190751,0.129313988454311,
0.332957613460226));
#14936=CARTESIAN_POINT('Ctrl Pts',(-0.113774867115171,0.0543021652640841,
0.338764702172283));
#14937=CARTESIAN_POINT('Ctrl Pts',(-0.117891132111753,0.00767537174388221,
0.341924401510079));
#14938=CARTESIAN_POINT('Ctrl Pts',(-0.117821685414254,0.000103165543095145,
0.342436711473616));
#14939=CARTESIAN_POINT('Origin',(0.,0.,-0.0924367114736175));
#14940=CARTESIAN_POINT('',(-0.117705188630573,0.000102098618198066,0.232563288526383));
#14941=CARTESIAN_POINT('',(-0.1176142238744,-6.23262858038681E-5,0.242436711473616));
#14942=CARTESIAN_POINT('',(-0.117775,2.85464118895969E-14,-0.0924367114736175));
#14943=CARTESIAN_POINT('Ctrl Pts',(-0.117705188630573,0.000102098618198071,
0.232563288526383));
#14944=CARTESIAN_POINT('Ctrl Pts',(-0.117475649963863,-0.0275896003179174,
0.234432088723979));
#14945=CARTESIAN_POINT('Ctrl Pts',(-0.0938913217252411,-0.0948462909608301,
0.238947218800678));
#14946=CARTESIAN_POINT('Ctrl Pts',(0.0182347644767634,-0.138007750384372,
0.246108678756477));
#14947=CARTESIAN_POINT('Ctrl Pts',(0.125841858853055,-0.0595186723796334,
0.254047668393783));
#14948=CARTESIAN_POINT('Ctrl Pts',(0.118249355954961,0.073455671106145,
0.261986658031089));
#14949=CARTESIAN_POINT('Ctrl Pts',(0.00240767183786234,0.139186381940956,
0.269925647668394));
#14950=CARTESIAN_POINT('Ctrl Pts',(-0.0995777503027144,0.0858938305448248,
0.27678452450016));
#14951=CARTESIAN_POINT('Ctrl Pts',(-0.117507442931816,0.0231998416616275,
0.280997071452822));
#14952=CARTESIAN_POINT('Ctrl Pts',(-0.117608153246896,-5.64262068778604E-5,
0.282563288526383));
#14953=CARTESIAN_POINT('Ctrl Pts',(-0.1176142238744,-6.2326285803882E-5,
0.242436711473616));
#14954=CARTESIAN_POINT('Ctrl Pts',(-0.117689148257971,-0.0156863246439697,
0.243489062352292));
#14955=CARTESIAN_POINT('Ctrl Pts',(-0.107519643382358,-0.0705218816827611,
0.247188802605229));
#14956=CARTESIAN_POINT('Ctrl Pts',(-0.024381182195918,-0.137074561658528,
0.253535932232426));
#14957=CARTESIAN_POINT('Ctrl Pts',(0.101985705091022,-0.094777599970642,
0.261478100355206));
#14958=CARTESIAN_POINT('Ctrl Pts',(0.134923209124943,0.0343453801629359,
0.269420268477986));
#14959=CARTESIAN_POINT('Ctrl Pts',(0.0442571924125319,0.132004463632409,
0.277362436600766));
#14960=CARTESIAN_POINT('Ctrl Pts',(-0.0824920331482911,0.109525057495754,
0.285034584265976));
#14961=CARTESIAN_POINT('Ctrl Pts',(-0.117677666622401,0.0349954280503056,
0.290059342556926));
#14962=CARTESIAN_POINT('Ctrl Pts',(-0.117918861549493,-6.80329776671157E-5,
0.292436711473616));
#14963=CARTESIAN_POINT('Origin',(0.,0.,-0.0924367114736175));
#14964=CARTESIAN_POINT('',(-0.117967994073432,-3.0724305424694E-6,0.182563288526383));
#14965=CARTESIAN_POINT('',(-0.117691121003631,9.91971943564221E-5,0.192436711473615));
#14966=CARTESIAN_POINT('',(-0.117775,2.85464118895969E-14,-0.0924367114736175));
#14967=CARTESIAN_POINT('Ctrl Pts',(-0.117967994073432,-3.07243054247449E-6,
0.182563288526383));
#14968=CARTESIAN_POINT('Ctrl Pts',(-0.117968057042159,-0.000167453844217198,
0.182574446236933));
#14969=CARTESIAN_POINT('Ctrl Pts',(-0.117893299674953,-0.0393189363008842,
0.185231933826584));
#14970=CARTESIAN_POINT('Ctrl Pts',(-0.0749972298318695,-0.11727771015962,
0.190535751295337));
#14971=CARTESIAN_POINT('Ctrl Pts',(0.0578663373665801,-0.126610160769685,
0.198474740932643));
#14972=CARTESIAN_POINT('Ctrl Pts',(0.13775723856723,-0.0200396862227523,
0.206413730569949));
#14973=CARTESIAN_POINT('Ctrl Pts',(0.091540828968026,0.104875747581476,
0.214352720207254));
#14974=CARTESIAN_POINT('Ctrl Pts',(-0.0384749358425138,0.133784622116252,
0.22229170984456));
#14975=CARTESIAN_POINT('Ctrl Pts',(-0.110955338697302,0.0622468391270206,
0.22836189928427));
#14976=CARTESIAN_POINT('Ctrl Pts',(-0.11780069007939,0.0116234575531164,
0.231785758844877));
#14977=CARTESIAN_POINT('Ctrl Pts',(-0.117705188630573,0.000102098618198071,
0.232563288526383));
#14978=CARTESIAN_POINT('Ctrl Pts',(-0.117691121003631,9.91971943564221E-5,
0.192436711473615));
#14979=CARTESIAN_POINT('Ctrl Pts',(-0.117474218986382,-0.0270951350261672,
0.194271392773399));
#14980=CARTESIAN_POINT('Ctrl Pts',(-0.0945676524372527,-0.0938598508209937,
0.198753463447442));
#14981=CARTESIAN_POINT('Ctrl Pts',(0.0165156171993534,-0.138242945169174,
0.205882923495746));
#14982=CARTESIAN_POINT('Ctrl Pts',(0.125131592687617,-0.061040658666823,
0.213825091618526));
#14983=CARTESIAN_POINT('Ctrl Pts',(0.119114174013628,0.0720811421096423,
0.221767259741306));
#14984=CARTESIAN_POINT('Ctrl Pts',(0.0039759348809324,0.139169211541763,
0.229709427864086));
#14985=CARTESIAN_POINT('Ctrl Pts',(-0.0990660356104632,0.0867677816679632,
0.236599245108189));
#14986=CARTESIAN_POINT('Ctrl Pts',(-0.117500661679058,0.0236188235484957,
0.240841672978032));
#14987=CARTESIAN_POINT('Ctrl Pts',(-0.1176142238744,-6.2326285803882E-5,
0.242436711473616));
#14988=CARTESIAN_POINT('Origin',(0.,0.,-0.0924367114736175));
#14989=CARTESIAN_POINT('',(-0.117696212882312,-0.000100181105204699,0.132563288526383));
#14990=CARTESIAN_POINT('',(-0.117967699956222,8.3697257429456E-6,0.142436711473616));
#14991=CARTESIAN_POINT('',(-0.117775,2.85464118895969E-14,-0.0924367114736175));
#14992=CARTESIAN_POINT('Ctrl Pts',(-0.117696212882312,-0.000100181105204706,
0.132563288526383));
#14993=CARTESIAN_POINT('Ctrl Pts',(-0.117792074781153,-0.0119544960022407,
0.133363133628988));
#14994=CARTESIAN_POINT('Ctrl Pts',(-0.110696412003459,-0.0629173266909915,
0.136809308610694));
#14995=CARTESIAN_POINT('Ctrl Pts',(-0.0373480950846616,-0.134103559412242,
0.142901813471503));
#14996=CARTESIAN_POINT('Ctrl Pts',(0.0924198687735613,-0.104101940294199,
0.150840803108809));
#14997=CARTESIAN_POINT('Ctrl Pts',(0.137583777756591,0.0211978768359354,
0.158779792746114));
#14998=CARTESIAN_POINT('Ctrl Pts',(0.0567991668878991,0.127092487218924,
0.16671878238342));
#14999=CARTESIAN_POINT('Ctrl Pts',(-0.0757945745091616,0.116657324056303,
0.174646614310176));
#15000=CARTESIAN_POINT('Ctrl Pts',(-0.117953122434976,0.0388197061692436,
0.179928116357831));
#15001=CARTESIAN_POINT('Ctrl Pts',(-0.117967994073432,-3.07243054247449E-6,
0.182563288526383));
#15002=CARTESIAN_POINT('Ctrl Pts',(-0.117967699956222,8.3697257429579E-6,
0.142436711473616));
#15003=CARTESIAN_POINT('Ctrl Pts',(-0.117928252023989,-0.038547130539091,
0.145053723194506));
#15004=CARTESIAN_POINT('Ctrl Pts',(-0.0762804946418446,-0.116178754198862,
0.150318124289656));
#15005=CARTESIAN_POINT('Ctrl Pts',(0.0559861945572589,-0.127473226882309,
0.158229914759066));
#15006=CARTESIAN_POINT('Ctrl Pts',(0.137471621702818,-0.0220324926503626,
0.166172082881846));
#15007=CARTESIAN_POINT('Ctrl Pts',(0.0930189202108026,0.103592267873211,
0.174114251004626));
#15008=CARTESIAN_POINT('Ctrl Pts',(-0.0366486683060043,0.134315868829211,
0.182056419127406));
#15009=CARTESIAN_POINT('Ctrl Pts',(-0.110544190454925,0.0633195416932908,
0.188163905950403));
#15010=CARTESIAN_POINT('Ctrl Pts',(-0.11778720200735,0.0121454601492482,
0.191624003399139));
#15011=CARTESIAN_POINT('Ctrl Pts',(-0.117691121003631,9.91971943564221E-5,
0.192436711473615));
#15012=CARTESIAN_POINT('Origin',(0.,0.,-0.0924367114736175));
#15013=CARTESIAN_POINT('',(-0.117613109409711,6.11591708146705E-5,0.0825632885263832));
#15014=CARTESIAN_POINT('',(-0.117715749944134,-0.000104199409386274,0.0924367114736155));
#15015=CARTESIAN_POINT('',(-0.117775,2.85464118895969E-14,-0.0924367114736175));
#15016=CARTESIAN_POINT('Ctrl Pts',(-0.117613109409711,6.11591708146765E-5,
0.0825632885263832));
#15017=CARTESIAN_POINT('Ctrl Pts',(-0.117502393620717,-0.0235240259785673,
0.0841518210210431));
#15018=CARTESIAN_POINT('Ctrl Pts',(-0.0991849320095013,-0.0865581493706475,
0.088386683394805));
#15019=CARTESIAN_POINT('Ctrl Pts',(0.00357853460314598,-0.139161043603659,
0.0952678756476685));
#15020=CARTESIAN_POINT('Ctrl Pts',(0.118863112008681,-0.0724583686054966,
0.103206865284975));
#15021=CARTESIAN_POINT('Ctrl Pts',(0.125336705278751,0.0605752693714656,
0.11114585492228));
#15022=CARTESIAN_POINT('Ctrl Pts',(0.0170731091066207,0.138156245709763,
0.119084844559586));
#15023=CARTESIAN_POINT('Ctrl Pts',(-0.094337657277608,0.0941904991302726,
0.126223989094287));
#15024=CARTESIAN_POINT('Ctrl Pts',(-0.11747491061231,0.0272661325996615,
0.130716803749886));
#15025=CARTESIAN_POINT('Ctrl Pts',(-0.117696212882312,-0.000100181105204706,
0.132563288526383));
#15026=CARTESIAN_POINT('Ctrl Pts',(-0.117715749944134,-0.000104199409386274,
0.0924367114736155));
#15027=CARTESIAN_POINT('Ctrl Pts',(-0.117810584636384,-0.011244028442556,
0.0931886642413524));
#15028=CARTESIAN_POINT('Ctrl Pts',(-0.111246641208053,-0.0614941526881817,
0.0965880063833492));
#15029=CARTESIAN_POINT('Ctrl Pts',(-0.0397151780004399,-0.133441281507892,
0.102634737899606));
#15030=CARTESIAN_POINT('Ctrl Pts',(0.0906220264938673,-0.105695447092796,
0.110576906022386));
#15031=CARTESIAN_POINT('Ctrl Pts',(0.137940159127448,0.0188783162799928,
0.118519074145166));
#15032=CARTESIAN_POINT('Ctrl Pts',(0.0588909273047484,0.126157580947307,
0.126461242267946));
#15033=CARTESIAN_POINT('Ctrl Pts',(-0.074108440039672,0.117863552156501,
0.134403410390726));
#15034=CARTESIAN_POINT('Ctrl Pts',(-0.117763087033452,0.0399060678969832,
0.139728566792616));
#15035=CARTESIAN_POINT('Ctrl Pts',(-0.117968157858494,0.000455912857932787,
0.142406333820246));
#15036=CARTESIAN_POINT('Ctrl Pts',(-0.117967699956222,8.3697257429579E-6,
0.142436711473616));
#15037=CARTESIAN_POINT('Origin',(0.,0.,-0.0924367114736175));
#15038=CARTESIAN_POINT('',(-0.117917485785546,7.60014832213593E-5,0.0325632885263832));
#15039=CARTESIAN_POINT('',(-0.117600989619072,5.04992496179954E-5,0.0424367114736154));
#15040=CARTESIAN_POINT('',(-0.117775,2.85464118895969E-14,-0.0924367114736175));
#15041=CARTESIAN_POINT('Ctrl Pts',(-0.117917485785546,7.60014832213644E-5,
0.0325632885263832));
#15042=CARTESIAN_POINT('Ctrl Pts',(-0.117676727567847,-0.0349830640657269,
0.0349405084130983));
#15043=CARTESIAN_POINT('Ctrl Pts',(-0.0825043195215805,-0.109517225708346,
0.0399640581789154));
#15044=CARTESIAN_POINT('Ctrl Pts',(0.0441923146003338,-0.131999388615902,
0.0476339378238343));
#15045=CARTESIAN_POINT('Ctrl Pts',(0.134874939024977,-0.034459980695041,
0.0555729274611401));
#15046=CARTESIAN_POINT('Ctrl Pts',(0.102091080224759,0.094638871230671,
0.0635119170984456));
#15047=CARTESIAN_POINT('Ctrl Pts',(-0.0241513666277066,0.137095110112719,
0.0714509067357516));
#15048=CARTESIAN_POINT('Ctrl Pts',(-0.107448046275642,0.0706698818446754,
0.0778013638783972));
#15049=CARTESIAN_POINT('Ctrl Pts',(-0.117686834607281,0.0157664388843013,
0.0815054911419412));
#15050=CARTESIAN_POINT('Ctrl Pts',(-0.117613109409711,6.11591708146765E-5,
0.0825632885263832));
#15051=CARTESIAN_POINT('Ctrl Pts',(-0.117600989619072,5.04992496179954E-5,
0.0424367114736154));
#15052=CARTESIAN_POINT('Ctrl Pts',(-0.117514779739531,-0.0227353060542692,
0.043970994662459));
#15053=CARTESIAN_POINT('Ctrl Pts',(-0.100129952091853,-0.0849605109884783,
0.0481526672255625));
#15054=CARTESIAN_POINT('Ctrl Pts',(0.000787973702835166,-0.139222729671589,
0.054981729162926));
#15055=CARTESIAN_POINT('Ctrl Pts',(0.117431922513572,-0.0747907597173192,
0.0629238972857061));
#15056=CARTESIAN_POINT('Ctrl Pts',(0.126496838785129,0.0581591461343325,
0.070866065408486));
#15057=CARTESIAN_POINT('Ctrl Pts',(0.0196773008918215,0.137828289815661,
0.0788082335312661));
#15058=CARTESIAN_POINT('Ctrl Pts',(-0.0933482651079043,0.0956446566614129,
0.085998448886309));
#15059=CARTESIAN_POINT('Ctrl Pts',(-0.11747670148927,0.0279758085988667,
0.0905412748670923));
#15060=CARTESIAN_POINT('Ctrl Pts',(-0.117715749944134,-0.000104199409386274,
0.0924367114736155));
#15061=CARTESIAN_POINT('Origin',(0.,0.,1.55));
#15062=CARTESIAN_POINT('',(-0.143211704627722,-5.70397197726547E-6,1.50700023576178));
#15063=CARTESIAN_POINT('Ctrl Pts',(-0.0334019664626774,0.112939183906323,
1.532225));
#15064=CARTESIAN_POINT('Ctrl Pts',(-0.0250606930336426,0.115799676338094,
1.53184761307169));
#15065=CARTESIAN_POINT('Ctrl Pts',(-0.0164287086124659,0.117635554524944,
1.53147359869818));
#15066=CARTESIAN_POINT('Ctrl Pts',(-0.00767226928320402,0.118510614220874,
1.53110056493424));
#15067=CARTESIAN_POINT('Ctrl Pts',(-0.0042150196872779,0.118856108509867,
1.53095328237096));
#15068=CARTESIAN_POINT('Ctrl Pts',(-0.000736351480830917,0.119051293525916,
1.53080607672538));
#15069=CARTESIAN_POINT('Ctrl Pts',(0.00274830211697625,0.119097943881266,
1.53065904037218));
#15070=CARTESIAN_POINT('Ctrl Pts',(0.00972321854123044,0.119191319684798,
1.53036473098213));
#15071=CARTESIAN_POINT('Ctrl Pts',(0.0166907125456733,0.118690968429664,
1.53007241075126));
#15072=CARTESIAN_POINT('Ctrl Pts',(0.0235721318645625,0.11762150546261,
1.52978094357425));
#15073=CARTESIAN_POINT('Ctrl Pts',(0.0273478463565568,0.117034709826966,
1.52962102062912));
#15074=CARTESIAN_POINT('Ctrl Pts',(0.0310977188904398,0.116276259986281,
1.52946135449799));
#15075=CARTESIAN_POINT('Ctrl Pts',(0.0348087249896146,0.115347945392283,
1.52930175751644));
#15076=CARTESIAN_POINT('Ctrl Pts',(0.0378768737129624,0.114580442682688,
1.52916980751093));
#15077=CARTESIAN_POINT('Ctrl Pts',(0.0409182562642153,0.113696477767379,
1.52903790896105));
#15078=CARTESIAN_POINT('Ctrl Pts',(0.0439120268522727,0.112701821307647,
1.52890655030309));
#15079=CARTESIAN_POINT('Ctrl Pts',(0.0504861734289241,0.110517613410832,
1.52861809430882));
#15080=CARTESIAN_POINT('Ctrl Pts',(0.0568477403450367,0.107796947733889,
1.528331525126));
#15081=CARTESIAN_POINT('Ctrl Pts',(0.0629211062797432,0.10455513280498,
1.52804576869741));
#15082=CARTESIAN_POINT('Ctrl Pts',(0.0667529140263229,0.102509807084265,
1.52786547926507));
#15083=CARTESIAN_POINT('Ctrl Pts',(0.0704699809867569,0.100256700264741,
1.52768551335768));
#15084=CARTESIAN_POINT('Ctrl Pts',(0.0740519796445933,0.0977963961590643,
1.52750560123222));
#15085=CARTESIAN_POINT('Ctrl Pts',(0.0761474027326905,0.0963571499395001,
1.52740035495562));
#15086=CARTESIAN_POINT('Ctrl Pts',(0.0781972522873126,0.0948464165467323,
1.52729509152825));
#15087=CARTESIAN_POINT('Ctrl Pts',(0.0801950758490376,0.0932655888959708,
1.52718986717129));
#15088=CARTESIAN_POINT('Ctrl Pts',(0.0872135629190184,0.0877120362002772,
1.52682020700562));
#15089=CARTESIAN_POINT('Ctrl Pts',(0.0935342345834078,0.0813437113039547,
1.52645409167081));
#15090=CARTESIAN_POINT('Ctrl Pts',(0.0991216768718319,0.0743433873765979,
1.52608928877518));
#15091=CARTESIAN_POINT('Ctrl Pts',(0.101857856375295,0.0709153174549959,
1.52591064420861));
#15092=CARTESIAN_POINT('Ctrl Pts',(0.104417791592617,0.0673349702414553,
1.52573231437502));
#15093=CARTESIAN_POINT('Ctrl Pts',(0.106794530290299,0.0636205708890664,
1.52555403711528));
#15094=CARTESIAN_POINT('Ctrl Pts',(0.108394385735532,0.0611202951812291,
1.52543403324399));
#15095=CARTESIAN_POINT('Ctrl Pts',(0.109912312880749,0.0585571637778213,
1.52531395827658));
#15096=CARTESIAN_POINT('Ctrl Pts',(0.111341951189028,0.0559432008961949,
1.5251940432238));
#15097=CARTESIAN_POINT('Ctrl Pts',(0.115894033640165,0.0476201345006791,
1.52481222412716));
#15098=CARTESIAN_POINT('Ctrl Pts',(0.119530893641226,0.0388304356906876,
1.52443409356659));
#15099=CARTESIAN_POINT('Ctrl Pts',(0.122195159250079,0.0297595052710396,
1.52405718851832));
#15100=CARTESIAN_POINT('Ctrl Pts',(0.123464283518865,0.0254385629829291,
1.52387764960816));
#15101=CARTESIAN_POINT('Ctrl Pts',(0.124512110981915,0.0210533134598664,
1.52369838877875));
#15102=CARTESIAN_POINT('Ctrl Pts',(0.12532867129748,0.0166220814218575,
1.52351913980531));
#15103=CARTESIAN_POINT('Ctrl Pts',(0.126067828800149,0.012610891624201,
1.52335688207487));
#15104=CARTESIAN_POINT('Ctrl Pts',(0.12661735951473,0.00855739899605222,
1.52319445303817));
#15105=CARTESIAN_POINT('Ctrl Pts',(0.126966826155483,0.00450415768051923,
1.52303280899981));
#15106=CARTESIAN_POINT('Ctrl Pts',(0.127602972227412,-0.00287409603749457,
1.52273856283131));
#15107=CARTESIAN_POINT('Ctrl Pts',(0.12758177643555,-0.010267620141741,
1.52244625042084));
#15108=CARTESIAN_POINT('Ctrl Pts',(0.126865581413421,-0.0175939782534482,
1.52215473434257));
#15109=CARTESIAN_POINT('Ctrl Pts',(0.126426462283551,-0.0220859726121444,
1.52197599770985));
#15110=CARTESIAN_POINT('Ctrl Pts',(0.12572570473317,-0.0265528301690258,
1.52179756043894));
#15111=CARTESIAN_POINT('Ctrl Pts',(0.124776542651163,-0.0309793260681717,
1.52161916036391));
#15112=CARTESIAN_POINT('Ctrl Pts',(0.124151644840291,-0.0338935887106027,
1.52150170748789));
#15113=CARTESIAN_POINT('Ctrl Pts',(0.123418330834614,-0.0367926408403149,
1.52138417707714));
#15114=CARTESIAN_POINT('Ctrl Pts',(0.122581975874549,-0.0396644408336013,
1.52126680258073));
#15115=CARTESIAN_POINT('Ctrl Pts',(0.120074191833131,-0.0482754427851461,
1.52091485884509));
#15116=CARTESIAN_POINT('Ctrl Pts',(0.116656903439717,-0.0566007293654626,
1.52056600333313));
#15117=CARTESIAN_POINT('Ctrl Pts',(0.112443760417108,-0.0645262187619275,
1.52021830866717));
#15118=CARTESIAN_POINT('Ctrl Pts',(0.109356904590302,-0.0703330102694749,
1.51996356219884));
#15119=CARTESIAN_POINT('Ctrl Pts',(0.105841781173658,-0.0759253337267248,
1.51970943888381));
#15120=CARTESIAN_POINT('Ctrl Pts',(0.101930367117466,-0.0812537151913617,
1.51945518067311));
#15121=CARTESIAN_POINT('Ctrl Pts',(0.100130771446666,-0.0837052409256295,
1.51933819945644));
#15122=CARTESIAN_POINT('Ctrl Pts',(0.0982476276828181,-0.0860996963839449,
1.51922123442864));
#15123=CARTESIAN_POINT('Ctrl Pts',(0.0962924325256194,-0.0884227179472683,
1.51910469697823));
#15124=CARTESIAN_POINT('Ctrl Pts',(0.0906946176521128,-0.0950736369671782,
1.51877104482549));
#15125=CARTESIAN_POINT('Ctrl Pts',(0.0844921899154374,-0.101162815315101,
1.51843983772287));
#15126=CARTESIAN_POINT('Ctrl Pts',(0.0777644521522082,-0.106582693579069,
1.51810941878));
#15127=CARTESIAN_POINT('Ctrl Pts',(0.0731067700043679,-0.110334931124879,
1.5178806663426));
#15128=CARTESIAN_POINT('Ctrl Pts',(0.0681966627772886,-0.113766151308436,
1.51765229166508));
#15129=CARTESIAN_POINT('Ctrl Pts',(0.0630541948599911,-0.116833686038022,
1.5174237449583));
#15130=CARTESIAN_POINT('Ctrl Pts',(0.0607686815400033,-0.118197018118406,
1.51732216988754));
#15131=CARTESIAN_POINT('Ctrl Pts',(0.0584414404741937,-0.119485783651375,
1.51722075040181));
#15132=CARTESIAN_POINT('Ctrl Pts',(0.0560784264268894,-0.12069488199044,
1.51711960151386));
#15133=CARTESIAN_POINT('Ctrl Pts',(0.0475595529450054,-0.125053787850271,
1.51675495087613));
#15134=CARTESIAN_POINT('Ctrl Pts',(0.038563113830939,-0.128389854466075,
1.51639315730301));
#15135=CARTESIAN_POINT('Ctrl Pts',(0.0292711048986314,-0.130741856378471,
1.51603205677802));
#15136=CARTESIAN_POINT('Ctrl Pts',(0.0254547302664753,-0.13170786066222,
1.51588374709674));
#15137=CARTESIAN_POINT('Ctrl Pts',(0.0215881861914954,-0.132507324978224,
1.51573555432397));
#15138=CARTESIAN_POINT('Ctrl Pts',(0.0176832233642019,-0.13314066674995,
1.51558732853105));
#15139=CARTESIAN_POINT('Ctrl Pts',(0.0144414794405867,-0.133666441752394,
1.51546427740745));
#15140=CARTESIAN_POINT('Ctrl Pts',(0.0111713231872828,-0.134077605234841,
1.5153411329761));
#15141=CARTESIAN_POINT('Ctrl Pts',(0.00789687394913892,-0.134372952697723,
1.51521845803943));
#15142=CARTESIAN_POINT('Ctrl Pts',(-0.00208492598009478,-0.135273287095873,
1.51484449692866));
#15143=CARTESIAN_POINT('Ctrl Pts',(-0.0121386692885745,-0.135107999768821,
1.51447364169918));
#15144=CARTESIAN_POINT('Ctrl Pts',(-0.0220717676774029,-0.133899092645375,
1.51410356562093));
#15145=CARTESIAN_POINT('Ctrl Pts',(-0.0271373055616968,-0.133282591671289,
1.51391483957382));
#15146=CARTESIAN_POINT('Ctrl Pts',(-0.0321716696217597,-0.132393849601707,
1.51372631615657));
#15147=CARTESIAN_POINT('Ctrl Pts',(-0.0371491047637803,-0.131230566976147,
1.51353768678866));
#15148=CARTESIAN_POINT('Ctrl Pts',(-0.0401763453142056,-0.130523066780721,
1.51342296375255));
#15149=CARTESIAN_POINT('Ctrl Pts',(-0.0431793745847511,-0.129714439573166,
1.51330831773957));
#15150=CARTESIAN_POINT('Ctrl Pts',(-0.0461427198170546,-0.128807808452418,
1.51319405707679));
#15151=CARTESIAN_POINT('Ctrl Pts',(-0.0557912886485991,-0.125855842991896,
1.51282202756853));
#15152=CARTESIAN_POINT('Ctrl Pts',(-0.0650506639775802,-0.121862017750276,
1.51245293010828));
#15153=CARTESIAN_POINT('Ctrl Pts',(-0.0737251756215706,-0.116823260910032,
1.51208446868514));
#15154=CARTESIAN_POINT('Ctrl Pts',(-0.0774533877539874,-0.114657657224767,
1.51192610791459));
#15155=CARTESIAN_POINT('Ctrl Pts',(-0.0810733781510443,-0.112298364258586,
1.51176786463208));
#15156=CARTESIAN_POINT('Ctrl Pts',(-0.0845783705992567,-0.109758519633299,
1.51160955655689));
#15157=CARTESIAN_POINT('Ctrl Pts',(-0.0871260289206952,-0.107912394030924,
1.51149448786814));
#15158=CARTESIAN_POINT('Ctrl Pts',(-0.0896122610481647,-0.105970921032248,
1.51137940572563));
#15159=CARTESIAN_POINT('Ctrl Pts',(-0.0920243025666997,-0.10394826075131,
1.51126473391974));
#15160=CARTESIAN_POINT('Ctrl Pts',(-0.0995315444015674,-0.0976529296958118,
1.51090782920982));
#15161=CARTESIAN_POINT('Ctrl Pts',(-0.106349817996106,-0.090554906599088,
1.51055366538392));
#15162=CARTESIAN_POINT('Ctrl Pts',(-0.112409916721278,-0.0828189535999138,
1.51020021897155));
#15163=CARTESIAN_POINT('Ctrl Pts',(-0.11567060314877,-0.0786565598680515,
1.51001004419521));
#15164=CARTESIAN_POINT('Ctrl Pts',(-0.118711357121208,-0.0743087544864998,
1.50982007711492));
#15165=CARTESIAN_POINT('Ctrl Pts',(-0.121517490738653,-0.0697974244982526,
1.50963000253165));
#15166=CARTESIAN_POINT('Ctrl Pts',(-0.123184827969132,-0.0671169005197731,
1.50951706477726));
#15167=CARTESIAN_POINT('Ctrl Pts',(-0.124768226583796,-0.064379797453554,
1.50940414472167));
#15168=CARTESIAN_POINT('Ctrl Pts',(-0.12625918933752,-0.0616017405091787,
1.50929161182319));
#15169=CARTESIAN_POINT('Ctrl Pts',(-0.131254477666307,-0.0522942005345653,
1.50891458411209));
#15170=CARTESIAN_POINT('Ctrl Pts',(-0.135235816373665,-0.0424980109473837,
1.50854057440173));
#15171=CARTESIAN_POINT('Ctrl Pts',(-0.138100316247284,-0.0323932585971084,
1.50816719719795));
#15172=CARTESIAN_POINT('Ctrl Pts',(-0.139428601593765,-0.027707625827389,
1.5079940600046));
#15173=CARTESIAN_POINT('Ctrl Pts',(-0.140516076092011,-0.0229552175461711,
1.50782105881478));
#15174=CARTESIAN_POINT('Ctrl Pts',(-0.14134846970832,-0.01815262603916,
1.50764795577689));
#15175=CARTESIAN_POINT('Ctrl Pts',(-0.141840021659925,-0.0153165600461233,
1.5075457335416));
#15176=CARTESIAN_POINT('Ctrl Pts',(-0.142241997144177,-0.0124651428186592,
1.50744355431084));
#15177=CARTESIAN_POINT('Ctrl Pts',(-0.142550993842162,-0.00961078035088443,
1.50734168592779));
#15178=CARTESIAN_POINT('Ctrl Pts',(-0.142847161918882,-0.00687492249914849,
1.50724404681617));
#15179=CARTESIAN_POINT('Ctrl Pts',(-0.143058332724879,-0.00413406598225375,
1.5071466105924));
#15180=CARTESIAN_POINT('Ctrl Pts',(-0.143182669649515,-0.00139134585336764,
1.50704933585643));
#15181=CARTESIAN_POINT('Ctrl Pts',(-0.143203595382121,-0.00092974984559876,
1.50703296465278));
#15182=CARTESIAN_POINT('Ctrl Pts',(-0.143222061023464,-0.000468100854706259,
1.50701659802318));
#15183=CARTESIAN_POINT('Ctrl Pts',(-0.143238079070951,-6.41379011939899E-6,
1.50700023577028));
#15184=CARTESIAN_POINT('',(-0.00156744678985144,0.146109855568756,1.50365));
#15185=CARTESIAN_POINT('Ctrl Pts',(-0.00156962371672063,0.146072546381438,
1.50365));
#15186=CARTESIAN_POINT('Ctrl Pts',(-0.011711474284147,0.144648739717271,
1.50495065132295));
#15187=CARTESIAN_POINT('Ctrl Pts',(-0.0216501921041044,0.142222471223284,
1.50626105010813));
#15188=CARTESIAN_POINT('Ctrl Pts',(-0.0312062965385204,0.138804788898175,
1.50759029209282));
#15189=CARTESIAN_POINT('Ctrl Pts',(-0.0379863325344082,0.136379950477271,
1.50853338648503));
#15190=CARTESIAN_POINT('Ctrl Pts',(-0.0445735484268955,0.133455002060128,
1.5094859663039));
#15191=CARTESIAN_POINT('Ctrl Pts',(-0.0508923708069948,0.130021662144985,
1.51045128011208));
#15192=CARTESIAN_POINT('Ctrl Pts',(-0.053607485163773,0.128546401418451,
1.51086606268101));
#15193=CARTESIAN_POINT('Ctrl Pts',(-0.0562647183424556,0.126981576978965,
1.51128195276517));
#15194=CARTESIAN_POINT('Ctrl Pts',(-0.0588579379029418,0.125328026221608,
1.51169910067666));
#15195=CARTESIAN_POINT('Ctrl Pts',(-0.0624505046767585,0.123037247762191,
1.51227700458785));
#15196=CARTESIAN_POINT('Ctrl Pts',(-0.0659209207101175,0.120575889029892,
1.51285741907924));
#15197=CARTESIAN_POINT('Ctrl Pts',(-0.0692542752175272,0.117943487410649,
1.51344114883776));
#15198=CARTESIAN_POINT('Ctrl Pts',(-0.0735613784355843,0.114542101371374,
1.51419539934302));
#15199=CARTESIAN_POINT('Ctrl Pts',(-0.0776398170223455,0.110855132244726,
1.51495518495604));
#15200=CARTESIAN_POINT('Ctrl Pts',(-0.0814741368103916,0.106911749311875,
1.51572224163114));
#15201=CARTESIAN_POINT('Ctrl Pts',(-0.0845038784997064,0.103795829845314,
1.51632834224744));
#15202=CARTESIAN_POINT('Ctrl Pts',(-0.087381117690253,0.10051973853988,
1.51693898261853));
#15203=CARTESIAN_POINT('Ctrl Pts',(-0.0900959757046659,0.0970973798321736,
1.51755501917095));
#15204=CARTESIAN_POINT('Ctrl Pts',(-0.0920052356275281,0.0946905606587243,
1.51798825505079));
#15205=CARTESIAN_POINT('Ctrl Pts',(-0.093830595110286,0.092215607777745,
1.51842338946406));
#15206=CARTESIAN_POINT('Ctrl Pts',(-0.0955653742165971,0.0896840982544811,
1.51885969689116));
#15207=CARTESIAN_POINT('Ctrl Pts',(-0.0997851775729162,0.0835262696618028,
1.51992100293214));
#15208=CARTESIAN_POINT('Ctrl Pts',(-0.103479134251024,0.0770231540939269,
1.52099120961793));
#15209=CARTESIAN_POINT('Ctrl Pts',(-0.106606394578922,0.0702509006766953,
1.52207541818308));
#15210=CARTESIAN_POINT('Ctrl Pts',(-0.108879606303698,0.0653281362576702,
1.52286353153598));
#15211=CARTESIAN_POINT('Ctrl Pts',(-0.110852991156964,0.0602629640702717,
1.52365904329275));
#15212=CARTESIAN_POINT('Ctrl Pts',(-0.112503888351057,0.0550849881514033,
1.524463912762));
#15213=CARTESIAN_POINT('Ctrl Pts',(-0.113450017754745,0.0521174894567802,
1.52492518356294));
#15214=CARTESIAN_POINT('Ctrl Pts',(-0.114289979676541,0.0491121240008169,
1.52538965304266));
#15215=CARTESIAN_POINT('Ctrl Pts',(-0.115015874151616,0.0460903162170444,
1.52585530945224));
#15216=CARTESIAN_POINT('Ctrl Pts',(-0.117053612444637,0.0376074669234184,
1.52716250482259));
#15217=CARTESIAN_POINT('Ctrl Pts',(-0.118206139871793,0.0289652499882669,
1.52848357355921));
#15218=CARTESIAN_POINT('Ctrl Pts',(-0.11838625730212,0.0202925750432425,
1.52982832573377));
#15219=CARTESIAN_POINT('Ctrl Pts',(-0.118492077855379,0.015197303257165,
1.53061837930521));
#15220=CARTESIAN_POINT('Ctrl Pts',(-0.118261361656021,0.0100916471271278,
1.53141660760476));
#15221=CARTESIAN_POINT('Ctrl Pts',(-0.11766859746431,0.00500517689818842,
1.532225));
#15222=CARTESIAN_POINT('',(-0.115079981391543,0.0902137050004572,1.50365));
#15223=CARTESIAN_POINT('Origin',(0.,0.,1.50365));
#15224=CARTESIAN_POINT('Ctrl Pts',(-0.143238079070951,-6.41379011939899E-6,
1.50700023577028));
#15225=CARTESIAN_POINT('Ctrl Pts',(-0.143514357617001,0.00795674345750163,
1.50671802038504));
#15226=CARTESIAN_POINT('Ctrl Pts',(-0.14306421847979,0.0159310909218757,
1.50643710681857));
#15227=CARTESIAN_POINT('Ctrl Pts',(-0.141940608246003,0.023841490005315,
1.50615648267927));
#15228=CARTESIAN_POINT('Ctrl Pts',(-0.141317731836386,0.0282266413964,1.50600091791928));
#15229=CARTESIAN_POINT('Ctrl Pts',(-0.14048752132733,0.0325921818867556,
1.50584544210227));
#15230=CARTESIAN_POINT('Ctrl Pts',(-0.139456452513291,0.0369250818702156,
1.5056898827608));
#15231=CARTESIAN_POINT('Ctrl Pts',(-0.138790989895207,0.0397215809279161,
1.50558948313156));
#15232=CARTESIAN_POINT('Ctrl Pts',(-0.138042009924554,0.0425029011667524,
1.50548910366784));
#15233=CARTESIAN_POINT('Ctrl Pts',(-0.137214434473447,0.0452564915355094,
1.50538902890071));
#15234=CARTESIAN_POINT('Ctrl Pts',(-0.134176751889031,0.0553637675507716,
1.50502169637912));
#15235=CARTESIAN_POINT('Ctrl Pts',(-0.130076454936343,0.0651325632434767,
1.50465723703036));
#15236=CARTESIAN_POINT('Ctrl Pts',(-0.125018127980614,0.0743940890034878,
1.50429344851366));
#15237=CARTESIAN_POINT('Ctrl Pts',(-0.122034683484208,0.0798566160996726,
1.50407888293545));
#15238=CARTESIAN_POINT('Ctrl Pts',(-0.118716925567465,0.0851425936725427,
1.50386455072235));
#15239=CARTESIAN_POINT('Ctrl Pts',(-0.115078604842436,0.0902138214954005,
1.50365));
#15240=CARTESIAN_POINT('',(-0.05,-6.12323399573677E-18,1.6));
#15241=CARTESIAN_POINT('',(-0.1,-1.22464679914735E-17,1.55));
#15242=CARTESIAN_POINT('Origin',(0.,0.,1.6));
#15243=CARTESIAN_POINT('Ctrl Pts',(0.0850780204044575,-0.11908002747757,
-0.0164977839420936));
#15244=CARTESIAN_POINT('Ctrl Pts',(0.124677800165771,-0.0907875342533835,
-0.0138514540629917));
#15245=CARTESIAN_POINT('Ctrl Pts',(0.172751483861701,0.00791416360185712,
-0.00855879430478784));
#15246=CARTESIAN_POINT('Ctrl Pts',(0.0868617128612901,0.149726167188418,
-0.000619804667482127));
#15247=CARTESIAN_POINT('Ctrl Pts',(-0.078614020905812,0.154028602276276,
0.00731918496982359));
#15248=CARTESIAN_POINT('Ctrl Pts',(-0.172087192378165,0.0175525219725009,
0.0152581746071293));
#15249=CARTESIAN_POINT('Ctrl Pts',(-0.108045720411827,-0.135108484733225,
0.0231971642444351));
#15250=CARTESIAN_POINT('Ctrl Pts',(0.0549144151285058,-0.164025561655164,
0.0311361538817407));
#15251=CARTESIAN_POINT('Ctrl Pts',(0.167598788591005,-0.0428207868793744,
0.0390751435190465));
#15252=CARTESIAN_POINT('Ctrl Pts',(0.126860790413016,0.117600499296196,
0.0470141331563521));
#15253=CARTESIAN_POINT('Ctrl Pts',(-0.0300110592737492,0.170357625684536,
0.054953122793658));
#15254=CARTESIAN_POINT('Ctrl Pts',(-0.159409054995301,0.0671687418111174,
0.0628921124309635));
#15255=CARTESIAN_POINT('Ctrl Pts',(-0.142879399887002,-0.0975110083167992,
0.0708311020682695));
#15256=CARTESIAN_POINT('Ctrl Pts',(0.00444677171871267,-0.172924803493063,
0.078770091705575));
#15257=CARTESIAN_POINT('Ctrl Pts',(0.147702113712341,-0.0900384822365835,
0.0867090813428809));
#15258=CARTESIAN_POINT('Ctrl Pts',(0.155746353789385,0.0752722621313087,
0.0946480709801864));
#15259=CARTESIAN_POINT('Ctrl Pts',(0.021215449100004,0.17167621786987,0.102587060617492));
#15260=CARTESIAN_POINT('Ctrl Pts',(-0.132736728465598,0.110922462699857,
0.110526050254798));
#15261=CARTESIAN_POINT('Ctrl Pts',(-0.165177537004225,-0.0513732581591355,
0.118465039892104));
#15262=CARTESIAN_POINT('Ctrl Pts',(-0.0464096261145344,-0.166640254043574,
0.126404029529409));
#15263=CARTESIAN_POINT('Ctrl Pts',(0.114843114370719,-0.129359532685675,
0.134343019166715));
#15264=CARTESIAN_POINT('Ctrl Pts',(0.170964855654229,0.0263409830179588,
0.142282008804021));
#15265=CARTESIAN_POINT('Ctrl Pts',(0.0705799878925336,0.157928129946847,
0.150220998441327));
#15266=CARTESIAN_POINT('Ctrl Pts',(-0.0944160212638482,0.144942899583874,
0.158159988078632));
#15267=CARTESIAN_POINT('Ctrl Pts',(-0.172980633894512,-0.000727622896455919,
0.166098977715938));
#15268=CARTESIAN_POINT('Ctrl Pts',(-0.0931933312323777,-0.145732055885043,
0.174037967353244));
#15269=CARTESIAN_POINT('Ctrl Pts',(0.0719060791645076,-0.157328779695546,
0.181976956990549));
#15270=CARTESIAN_POINT('Ctrl Pts',(0.171180402159323,-0.0249017879745179,
0.189915946627855));
#15271=CARTESIAN_POINT('Ctrl Pts',(0.113750798721884,0.13032108391891,0.197854936265161));
#15272=CARTESIAN_POINT('Ctrl Pts',(-0.0478098650864174,0.16624393501773,
0.205793925902467));
#15273=CARTESIAN_POINT('Ctrl Pts',(-0.16560387403618,0.0499818570245514,
0.213732915539772));
#15274=CARTESIAN_POINT('Ctrl Pts',(-0.131798885878402,-0.112035185581475,
0.221671905177078));
#15275=CARTESIAN_POINT('Ctrl Pts',(0.0226589495323734,-0.171491694067101,
0.229610894814384));
#15276=CARTESIAN_POINT('Ctrl Pts',(0.156374069566079,-0.073959309724122,
0.237549884451689));
#15277=CARTESIAN_POINT('Ctrl Pts',(0.146939445926624,0.0912777539068999,
0.245488874088995));
#15278=CARTESIAN_POINT('Ctrl Pts',(0.00299182995941577,0.172956289510158,
0.253427863726301));
#15279=CARTESIAN_POINT('Ctrl Pts',(-0.143694601292225,0.0963051955349955,
0.261366853363607));
#15280=CARTESIAN_POINT('Ctrl Pts',(-0.15883847309497,-0.0685067047260848,
0.269305843000912));
#15281=CARTESIAN_POINT('Ctrl Pts',(-0.0285766086907934,-0.170605411881679,
0.277244832638218));
#15282=CARTESIAN_POINT('Ctrl Pts',(0.12784518248692,-0.116526556812001,
0.285183822275524));
#15283=CARTESIAN_POINT('Ctrl Pts',(0.167233470900423,0.0442243749325307,
0.293122811912829));
#15284=CARTESIAN_POINT('Ctrl Pts',(0.0535309779628647,0.164490922320707,
0.301061801550136));
#15285=CARTESIAN_POINT('Ctrl Pts',(-0.109175456582181,0.134177303623408,
0.309000791187441));
#15286=CARTESIAN_POINT('Ctrl Pts',(-0.171939242908932,-0.0189664407699395,
0.316939780824747));
#15287=CARTESIAN_POINT('Ctrl Pts',(-0.0773044361184472,-0.154747708493488,
0.324878770462053));
#15288=CARTESIAN_POINT('Ctrl Pts',(0.0880972839194656,-0.148868054644337,
0.332817760099358));
#15289=CARTESIAN_POINT('Ctrl Pts',(0.172851978230285,-0.00670989936239309,
0.340756749736664));
#15290=CARTESIAN_POINT('Ctrl Pts',(0.0993725327910066,0.141590708926387,
0.34869573937397));
#15291=CARTESIAN_POINT('Ctrl Pts',(-0.0650756559739905,0.160274727038081,
0.356634729011275));
#15292=CARTESIAN_POINT('Ctrl Pts',(-0.169951541620772,0.0322382168908211,
0.364573718648582));
#15293=CARTESIAN_POINT('Ctrl Pts',(-0.119248438453561,-0.125310171390688,
0.372512708285886));
#15294=CARTESIAN_POINT('Ctrl Pts',(0.0406184374886585,-0.168145685830938,
0.380451697923193));
#15295=CARTESIAN_POINT('Ctrl Pts',(0.163301917673335,-0.0570553486694088,
0.388390687560498));
#15296=CARTESIAN_POINT('Ctrl Pts',(0.136493684039406,0.106265249940549,
0.396329677197804));
#15297=CARTESIAN_POINT('Ctrl Pts',(-0.0152651628095069,0.172307295063139,
0.404268666835109));
#15298=CARTESIAN_POINT('Ctrl Pts',(-0.153049799296248,0.0806138205455782,
0.412207656472416));
#15299=CARTESIAN_POINT('Ctrl Pts',(-0.150727833715048,-0.0848760818555219,
0.420146646109721));
#15300=CARTESIAN_POINT('Ctrl Pts',(-0.0104248664208018,-0.172667748255674,
0.428085635747027));
#15301=CARTESIAN_POINT('Ctrl Pts',(0.139421351618932,-0.10239392482138,
0.436024625384332));
#15302=CARTESIAN_POINT('Ctrl Pts',(0.16163687742079,0.0616145192729195,
0.443963615021638));
#15303=CARTESIAN_POINT('Ctrl Pts',(0.0358849196425865,0.169219093691645,
0.451902604658944));
#15304=CARTESIAN_POINT('Ctrl Pts',(-0.122717222714247,0.121915185177559,
0.45984159429625));
#15305=CARTESIAN_POINT('Ctrl Pts',(-0.168980158036723,-0.0369937199732681,
0.467780583933555));
#15306=CARTESIAN_POINT('Ctrl Pts',(-0.0605533396431397,-0.162037409833775,
0.475719573570861));
#15307=CARTESIAN_POINT('Ctrl Pts',(0.103305911202344,-0.138746956140414,
0.483658563208167));
#15308=CARTESIAN_POINT('Ctrl Pts',(0.172595680358559,0.0115568269495825,
0.491597552845473));
#15309=CARTESIAN_POINT('Ctrl Pts',(0.0838859329010004,0.151281127008313,
0.499536542482778));
#15310=CARTESIAN_POINT('Ctrl Pts',(-0.0816156370489812,0.152517923263679,
0.507475532120084));
#15311=CARTESIAN_POINT('Ctrl Pts',(-0.172403684765527,0.0141350135070757,
0.51541452175739));
#15312=CARTESIAN_POINT('Ctrl Pts',(-0.105367974675403,-0.137187532379513,
0.523353511394695));
#15313=CARTESIAN_POINT('Ctrl Pts',(0.0581248948911363,-0.162924294448283,
0.531292501032001));
#15314=CARTESIAN_POINT('Ctrl Pts',(0.168408406744046,-0.039515030880773,
0.539231490669306));
#15315=CARTESIAN_POINT('Ctrl Pts',(0.124525564004667,0.120067535316156,
0.547170480306613));
#15316=CARTESIAN_POINT('Ctrl Pts',(-0.0333518982867267,0.169736501696743,
0.555109469943918));
#15317=CARTESIAN_POINT('Ctrl Pts',(-0.160697983451488,0.0640233335761385,
0.563048459581225));
#15318=CARTESIAN_POINT('Ctrl Pts',(-0.14093607811848,-0.100298808627811,
0.570987449218529));
#15319=CARTESIAN_POINT('Ctrl Pts',(0.00784314775175556,-0.172804265459278,
0.578926438855836));
#15320=CARTESIAN_POINT('Ctrl Pts',(0.149442509381278,-0.0871192603125336,
0.586865428493141));
#15321=CARTESIAN_POINT('Ctrl Pts',(0.154237495636292,0.0783174569774929,
0.594804418130446));
#15322=CARTESIAN_POINT('Ctrl Pts',(0.0178386252221998,0.172059909850489,
0.602743407767753));
#15323=CARTESIAN_POINT('Ctrl Pts',(-0.134890284021987,0.108293307291099,
0.610682397405058));
#15324=CARTESIAN_POINT('Ctrl Pts',(-0.164136382878957,-0.0546083962682395,
0.618621387042364));
#15325=CARTESIAN_POINT('Ctrl Pts',(-0.0431268722112106,-0.167519855601819,
0.62656037667967));
#15326=CARTESIAN_POINT('Ctrl Pts',(0.117362334288317,-0.127078368017432,
0.634499366316975));
#15327=CARTESIAN_POINT('Ctrl Pts',(0.170414367112955,0.0296946562375699,
0.642438355954282));
#15328=CARTESIAN_POINT('Ctrl Pts',(0.0674637261050104,0.159284257814778,
0.650377345591586));
#15329=CARTESIAN_POINT('Ctrl Pts',(-0.0972453325609638,0.143060037825677,
0.658316335228894));
#15330=CARTESIAN_POINT('Ctrl Pts',(-0.172932953925271,-0.00412584224812367,
0.666255324866198));
#15331=CARTESIAN_POINT('Ctrl Pts',(-0.0903123078403481,-0.147534796506203,
0.674194314503505));
#15332=CARTESIAN_POINT('Ctrl Pts',(0.0749830665657334,-0.155885755782802,
0.68213330414081));
#15333=CARTESIAN_POINT('Ctrl Pts',(0.17163658245605,-0.021533989188811,
0.690072293778116));
#15334=CARTESIAN_POINT('Ctrl Pts',(0.11116857013107,0.132530668686874,0.698011283415421));
#15335=CARTESIAN_POINT('Ctrl Pts',(-0.0510666492692211,0.165272582299639,
0.705950273052727));
#15336=CARTESIAN_POINT('Ctrl Pts',(-0.166553851089581,0.0467187736868841,
0.713889262690032));
#15337=CARTESIAN_POINT('Ctrl Pts',(-0.129572416918314,-0.114602870389546,
0.721828252327339));
#15338=CARTESIAN_POINT('Ctrl Pts',(0.0260236847639906,-0.171013440871999,
0.729767241964644));
#15339=CARTESIAN_POINT('Ctrl Pts',(0.157796886564457,-0.0708729265526718,
0.73770623160195));
#15340=CARTESIAN_POINT('Ctrl Pts',(0.145117853242075,0.0941468947867542,
0.745645221239255));
#15341=CARTESIAN_POINT('Ctrl Pts',(-0.000406629147419015,0.172981686256994,
0.753584210876562));
#15342=CARTESIAN_POINT('Ctrl Pts',(-0.145558870420566,0.0934635991681543,
0.761523200513868));
#15343=CARTESIAN_POINT('Ctrl Pts',(-0.157461941624574,-0.0716140074803496,
0.769462190151172));
#15344=CARTESIAN_POINT('Ctrl Pts',(-0.0252193968429213,-0.17113389830906,
0.777401179788479));
#15345=CARTESIAN_POINT('Ctrl Pts',(0.130109777350283,-0.113992433807847,
0.785340169425784));
#15346=CARTESIAN_POINT('Ctrl Pts',(0.166332367384696,0.0475012914327479,
0.793279159063091));
#15347=CARTESIAN_POINT('Ctrl Pts',(0.0502890745800368,0.165510839842773,
0.801218148700395));
#15348=CARTESIAN_POINT('Ctrl Pts',(-0.111790419467279,0.132006557575396,
0.809157138337702));
#15349=CARTESIAN_POINT('Ctrl Pts',(-0.171533445990104,-0.0223406811520247,
0.817096127975007));
#15350=CARTESIAN_POINT('Ctrl Pts',(-0.0742493586638003,-0.156236557391639,
0.825035117612313));
#15351=CARTESIAN_POINT('Ctrl Pts',(0.0910049278783345,-0.147108572929777,
0.832974107249618));
#15352=CARTESIAN_POINT('Ctrl Pts',(0.172950439922886,-0.00331277195964383,
0.840913096886925));
#15353=CARTESIAN_POINT('Ctrl Pts',(0.0965716772857839,0.143515644700454,
0.848852086524229));
#15354=CARTESIAN_POINT('Ctrl Pts',(-0.0682118374171683,0.158965324406771,
0.856791076161536));
#15355=CARTESIAN_POINT('Ctrl Pts',(-0.170552089827228,0.0288931442238776,
0.864730065798841));
#15356=CARTESIAN_POINT('Ctrl Pts',(-0.116763592698541,-0.127628729319482,
0.872669055436147));
#15357=CARTESIAN_POINT('Ctrl Pts',(0.0439139712140358,-0.167315248138923,
0.880608045073453));
#15358=CARTESIAN_POINT('Ctrl Pts',(0.164391304101163,-0.0538361241500125,
0.888547034710759));
#15359=CARTESIAN_POINT('Ctrl Pts',(0.134379664555536,0.108926281867684,
0.896486024348063));
#15360=CARTESIAN_POINT('Ctrl Pts',(-0.018647348250808,0.17197414204115,
0.904425013985371));
#15361=CARTESIAN_POINT('Ctrl Pts',(-0.154603991719776,0.0775914613336281,
0.912364003622676));
#15362=CARTESIAN_POINT('Ctrl Pts',(-0.149031276472826,-0.0878208845346985,
0.920302993259982));
#15363=CARTESIAN_POINT('Ctrl Pts',(-0.00703064139541984,-0.172839229369798,
0.928241982897287));
#15364=CARTESIAN_POINT('Ctrl Pts',(0.141406064038169,-0.099635105162837,
0.936180972534593));
#15365=CARTESIAN_POINT('Ctrl Pts',(0.160395209035295,0.064778129380991,
0.944119962171899));
#15366=CARTESIAN_POINT('Ctrl Pts',(0.03255353276219,0.169891426011666,0.952058951809204));
#15367=CARTESIAN_POINT('Ctrl Pts',(-0.125088671715395,0.119480765548496,
0.959997941446511));
#15368=CARTESIAN_POINT('Ctrl Pts',(-0.168220770124088,-0.040306347222682,
0.967936931083815));
#15369=CARTESIAN_POINT('Ctrl Pts',(-0.0573582824064844,-0.163195761485875,
0.975875920721122));
#15370=CARTESIAN_POINT('Ctrl Pts',(0.106011781834435,-0.136690640644722,
0.983814910358427));
#15371=CARTESIAN_POINT('Ctrl Pts',(0.17233532526783,0.014945393685262,0.991753899995733));
#15372=CARTESIAN_POINT('Ctrl Pts',(0.0808976893297158,0.152899944371113,
0.999692889633039));
#15373=CARTESIAN_POINT('Ctrl Pts',(-0.0845962369090198,0.150885074902754,
1.00763187927034));
#15374=CARTESIAN_POINT('Ctrl Pts',(-0.172648106016301,0.0107452601904448,
1.01557086890765));
#15375=CARTESIAN_POINT('Ctrl Pts',(-0.102652466413112,-0.13923110380544,
1.02350985854496));
#15376=CARTESIAN_POINT('Ctrl Pts',(0.0613144709582997,-0.161750934398167,
1.03144884818226));
#15377=CARTESIAN_POINT('Ctrl Pts',(0.169152212322519,-0.0361988700648799,
1.03938783781957));
#15378=CARTESIAN_POINT('Ctrl Pts',(0.122142696063681,0.12249077894222,1.04732682745687));
#15379=CARTESIAN_POINT('Ctrl Pts',(-0.0366800874558037,0.169048514669047,
1.05526581709418));
#15380=CARTESIAN_POINT('Ctrl Pts',(-0.161924764760067,0.0608539208677085,
1.06320480673148));
#15381=CARTESIAN_POINT('Ctrl Pts',(-0.138938417355371,-0.103048266896446,
1.07114379636879));
#15382=CARTESIAN_POINT('Ctrl Pts',(0.011236529066559,-0.172616828675865,
1.0790827860061));
#15383=CARTESIAN_POINT('Ctrl Pts',(0.151125203217684,-0.0841665140064042,
1.0870217756434));
#15384=CARTESIAN_POINT('Ctrl Pts',(0.152669111109608,0.0813324759279986,
1.09496076528071));
#15385=CARTESIAN_POINT('Ctrl Pts',(0.0144549108781955,0.172377158228925,
1.10289975491801));
#15386=CARTESIAN_POINT('Ctrl Pts',(-0.136991769602464,0.10562236594946,
1.11083874455532));
#15387=CARTESIAN_POINT('Ctrl Pts',(-0.163031873671196,-0.0578224635832477,
1.11877773419263));
#15388=CARTESIAN_POINT('Ctrl Pts',(-0.0398274706979539,-0.168334790537727,
1.12671672382993));
#15389=CARTESIAN_POINT('Ctrl Pts',(0.119836252144435,-0.124748153491552,
1.13465571346724));
#15390=CARTESIAN_POINT('Ctrl Pts',(0.169798099063322,0.0330368685268242,
1.14259470310454));
#15391=CARTESIAN_POINT('Ctrl Pts',(0.0643214233134591,0.160578901573361,
1.15053369274185));
#15392=CARTESIAN_POINT('Ctrl Pts',(-0.100037107244844,0.141121955420339,
1.15847268237915));
#15393=CARTESIAN_POINT('Ctrl Pts',(-0.172818522111203,-0.00752246920075927,
1.16641167201646));
#15394=CARTESIAN_POINT('Ctrl Pts',(-0.0873964240115842,-0.149280588817046,
1.17435066165376));
#15395=CARTESIAN_POINT('Ctrl Pts',(0.0780311106025284,-0.154382560238235,
1.18228965129107));
#15396=CARTESIAN_POINT('Ctrl Pts',(0.172026511281289,-0.01815787828917,
1.19022864092837));
#15397=CARTESIAN_POINT('Ctrl Pts',(0.10854343062882,0.134689096792963,1.19816763056568));
#15398=CARTESIAN_POINT('Ctrl Pts',(-0.0543037217972188,0.164237434607784,
1.20610662020299));
#15399=CARTESIAN_POINT('Ctrl Pts',(-0.167439538594998,0.0434376569656869,
1.21404560984029));
#15400=CARTESIAN_POINT('Ctrl Pts',(-0.127295933190098,-0.117126318651471,
1.2219845994776));
#15401=CARTESIAN_POINT('Ctrl Pts',(0.0293783748903316,-0.170469176734012,
1.2299235891149));
#15402=CARTESIAN_POINT('Ctrl Pts',(0.159158794190081,-0.0677591865323411,
1.23786257875221));
#15403=CARTESIAN_POINT('Ctrl Pts',(0.143240245273553,0.0969796950995427,
1.24580156838952));
#15404=CARTESIAN_POINT('Ctrl Pts',(-0.00380493129617075,0.172940312320012,
1.25374055802682));
#15405=CARTESIAN_POINT('Ctrl Pts',(-0.147366954032488,0.0905859259858403,
1.26167954766413));
#15406=CARTESIAN_POINT('Ctrl Pts',(-0.156024630070406,-0.074693667330688,
1.26961853730143));
#15407=CARTESIAN_POINT('Ctrl Pts',(-0.0218524503424686,-0.171596327294885,
1.27755752693874));
#15408=CARTESIAN_POINT('Ctrl Pts',(0.132324150022753,-0.111414309889572,
1.28549651657604));
#15409=CARTESIAN_POINT('Ctrl Pts',(0.165367059817933,0.0507598725070622,
1.29343550621335));
#15410=CARTESIAN_POINT('Ctrl Pts',(0.0470277596764783,0.166466870408131,
1.30137449585065));
#15411=CARTESIAN_POINT('Ctrl Pts',(-0.114362231391601,0.129784857201791,
1.30931348548797));
#15412=CARTESIAN_POINT('Ctrl Pts',(-0.171061437441431,-0.0257062980954763,
1.31725247512526));
#15413=CARTESIAN_POINT('Ctrl Pts',(-0.071165620995849,-0.157665099140374,
1.32519146476257));
#15414=CARTESIAN_POINT('Ctrl Pts',(0.0938774439379855,-0.145292307632914,
1.33313045439988));
#15415=CARTESIAN_POINT('Ctrl Pts',(0.172982143233999,8.56343898915854E-5,
1.34106944403719));
#15416=CARTESIAN_POINT('Ctrl Pts',(0.0937335447930804,0.145385183220099,
1.34900843367449));
#15417=CARTESIAN_POINT('Ctrl Pts',(-0.0713216883190155,0.157594562185848,
1.3569474233118));
#15418=CARTESIAN_POINT('Ctrl Pts',(-0.171086806821499,0.0255369173285507,
1.3648864129491));
#15419=CARTESIAN_POINT('Ctrl Pts',(-0.114233673229396,-0.129898019862958,
1.37282540258641));
#15420=CARTESIAN_POINT('Ctrl Pts',(0.0471925482590101,-0.166420232464351,
1.38076439222371));
#15421=CARTESIAN_POINT('Ctrl Pts',(0.165417247017141,-0.0505961085897048,
1.38870338186102));
#15422=CARTESIAN_POINT('Ctrl Pts',(0.132213753266125,0.111545248710567,
1.39664237149832));
#15423=CARTESIAN_POINT('Ctrl Pts',(-0.0220222951247444,0.17157464463752,
1.40458136113563));
#15424=CARTESIAN_POINT('Ctrl Pts',(-0.156098584526576,0.0745390809398717,
1.41252035077293));
#15425=CARTESIAN_POINT('Ctrl Pts',(-0.147277046608992,-0.0907316537045687,
1.42045934041024));
#15426=CARTESIAN_POINT('Ctrl Pts',(-0.00363398118293899,-0.172944250658386,
1.42839833004755));
#15427=CARTESIAN_POINT('Ctrl Pts',(0.143336722904634,-0.0968373407211472,
1.43633731968485));
#15428=CARTESIAN_POINT('Ctrl Pts',(0.159090624036536,0.0679158129692223,
1.44427630932216));
#15429=CARTESIAN_POINT('Ctrl Pts',(0.0292114869387437,0.170499931406899,
1.45221529895946));
#15430=CARTESIAN_POINT('Ctrl Pts',(-0.127415456569397,0.116996902323752,
1.46015428859677));
#15431=CARTESIAN_POINT('Ctrl Pts',(-0.167389576437263,-0.0435971050111283,
1.46809327823408));
#15432=CARTESIAN_POINT('Ctrl Pts',(-0.0541541359620402,-0.164303103757731,
1.47603226787138));
#15433=CARTESIAN_POINT('Ctrl Pts',(0.108701533888403,-0.13455879509903,
1.48397125750869));
#15434=CARTESIAN_POINT('Ctrl Pts',(0.171961157005542,0.0182848320604298,
1.49191024714599));
#15435=CARTESIAN_POINT('Ctrl Pts',(0.0779697431325927,0.154543202561513,
1.4998492367833));
#15436=CARTESIAN_POINT('Ctrl Pts',(-0.0877325682749983,0.149025855561406,
1.5077882264206));
#15437=CARTESIAN_POINT('Ctrl Pts',(-0.144149484752264,0.0548439265155397,
1.51308088617881));
#15438=CARTESIAN_POINT('Ctrl Pts',(-0.146217781693078,0.00621955116994065,
1.51572721605791));
#15439=CARTESIAN_POINT('Ctrl Pts',(0.0795408277542855,-0.111329858282327,
-0.0109985226280624));
#15440=CARTESIAN_POINT('Ctrl Pts',(0.116563307192903,-0.0848787452970238,
-0.00835219274896048));
#15441=CARTESIAN_POINT('Ctrl Pts',(0.16150817751539,0.00739908052493189,
-0.00305953299075667));
#15442=CARTESIAN_POINT('Ctrl Pts',(0.0812084309002137,0.139981433724326,
0.00487945664654907));
#15443=CARTESIAN_POINT('Ctrl Pts',(-0.0734975292821143,0.144003850402812,
0.0128184462838548));
#15444=CARTESIAN_POINT('Ctrl Pts',(-0.160887120581772,0.0164101388376342,
0.0207574359211605));
#15445=CARTESIAN_POINT('Ctrl Pts',(-0.101013704785435,-0.126315124179183,
0.0286964255584662));
#15446=CARTESIAN_POINT('Ctrl Pts',(0.0513403816191153,-0.153350170642076,
0.0366354151957719));
#15447=CARTESIAN_POINT('Ctrl Pts',(0.156690838735662,-0.0400338514845966,
0.0445744048330777));
#15448=CARTESIAN_POINT('Ctrl Pts',(0.118604220350264,0.109946623274354,
0.0525133944703833));
#15449=CARTESIAN_POINT('Ctrl Pts',(-0.0280578283917351,0.15927012049393,
0.0604523841076892));
#15450=CARTESIAN_POINT('Ctrl Pts',(-0.14903412333264,0.0627971513379326,
0.0683913737449947));
#15451=CARTESIAN_POINT('Ctrl Pts',(-0.133580279395553,-0.0911646307683348,
0.0763303633823007));
#15452=CARTESIAN_POINT('Ctrl Pts',(0.0041573593468571,-0.161670216863261,
0.0842693530196062));
#15453=CARTESIAN_POINT('Ctrl Pts',(0.138089113144455,-0.0841784443595545,
0.0922083426569122));
#15454=CARTESIAN_POINT('Ctrl Pts',(0.14560980428584,0.0703732645446943,
0.100147332294218));
#15455=CARTESIAN_POINT('Ctrl Pts',(0.0198346691022095,0.160502893816501,
0.108086321931524));
#15456=CARTESIAN_POINT('Ctrl Pts',(-0.124097730593135,0.103703218031488,
0.116025311568829));
#15457=CARTESIAN_POINT('Ctrl Pts',(-0.154427171169137,-0.0480296962598115,
0.123964301206135));
#15458=CARTESIAN_POINT('Ctrl Pts',(-0.0433891157712434,-0.155794689166463,
0.13190329084344));
#15459=CARTESIAN_POINT('Ctrl Pts',(0.107368699171666,-0.12094033522185,
0.139842280480747));
#15460=CARTESIAN_POINT('Ctrl Pts',(0.15983782968835,0.0246266142906177,
0.147781270118052));
#15461=CARTESIAN_POINT('Ctrl Pts',(0.0659863808909888,0.147649582370873,
0.155720259755358));
#15462=CARTESIAN_POINT('Ctrl Pts',(-0.0882710769349216,0.135509478890084,
0.163659249392663));
#15463=CARTESIAN_POINT('Ctrl Pts',(-0.161722413615419,-0.00068026650363694,
0.171598239029969));
#15464=CARTESIAN_POINT('Ctrl Pts',(-0.0871279640988751,-0.136247273976568,
0.179537228667275));
#15465=CARTESIAN_POINT('Ctrl Pts',(0.0672261652318651,-0.147089240053593,
0.187476218304581));
#15466=CARTESIAN_POINT('Ctrl Pts',(0.160039347628626,-0.023281087390596,
0.195415207941886));
#15467=CARTESIAN_POINT('Ctrl Pts',(0.106347475470598,0.121839305139765,
0.203354197579192));
#15468=CARTESIAN_POINT('Ctrl Pts',(-0.0446982220051161,0.15542416405057,
0.211293187216498));
#15469=CARTESIAN_POINT('Ctrl Pts',(-0.154825760608133,0.0467288526640558,
0.219232176853804));
#15470=CARTESIAN_POINT('Ctrl Pts',(-0.12322092627477,-0.104743520787053,
0.227171166491109));
#15471=CARTESIAN_POINT('Ctrl Pts',(0.0211842211805034,-0.160330379506191,
0.235110156128415));
#15472=CARTESIAN_POINT('Ctrl Pts',(0.146196665995071,-0.0691457639426259,
0.24304914576572));
#15473=CARTESIAN_POINT('Ctrl Pts',(0.137376082602736,0.0853370596399817,
0.250988135403027));
#15474=CARTESIAN_POINT('Ctrl Pts',(0.00279711058556459,0.161699653653757,
0.258927125040332));
#15475=CARTESIAN_POINT('Ctrl Pts',(-0.134342424474264,0.0900372967480426,
0.266866114677638));
#15476=CARTESIAN_POINT('Ctrl Pts',(-0.148500677015507,-0.0640480346713102,
0.274805104314944));
#15477=CARTESIAN_POINT('Ctrl Pts',(-0.0267167371651392,-0.159501779847699,
0.282744093952249));
#15478=CARTESIAN_POINT('Ctrl Pts',(0.119524544542348,-0.108942576944327,
0.290683083589556));
#15479=CARTESIAN_POINT('Ctrl Pts',(0.156349297273321,0.0413460888291301,
0.29862207322686));
#15480=CARTESIAN_POINT('Ctrl Pts',(0.0500469836677093,0.153785243912065,
0.306561062864167));
#15481=CARTESIAN_POINT('Ctrl Pts',(-0.102069913541897,0.125444547784578,
0.314500052501472));
#15482=CARTESIAN_POINT('Ctrl Pts',(-0.160748800211922,-0.0177320345633525,
0.322439042138778));
#15483=CARTESIAN_POINT('Ctrl Pts',(-0.0722731771226978,-0.144676154524232,
0.330378031776084));
#15484=CARTESIAN_POINT('Ctrl Pts',(0.082363586418043,-0.139179170322594,
0.338317021413389));
#15485=CARTESIAN_POINT('Ctrl Pts',(0.16160213133829,-0.00627319426210969,
0.346256011050695));
#15486=CARTESIAN_POINT('Ctrl Pts',(0.0929050003357002,0.132375461215256,
0.354195000688001));
#15487=CARTESIAN_POINT('Ctrl Pts',(-0.0608402912787218,0.149843454232904,
0.362133990325306));
#15488=CARTESIAN_POINT('Ctrl Pts',(-0.158890465884947,0.0301400343429239,
0.370072979962613));
#15489=CARTESIAN_POINT('Ctrl Pts',(-0.1114873084483,-0.117154521356547,
0.378011969599918));
#15490=CARTESIAN_POINT('Ctrl Pts',(0.0379748391485164,-0.157202141877815,
0.385950959237223));
#15491=CARTESIAN_POINT('Ctrl Pts',(0.152673624090564,-0.0533419752763387,
0.39388994887453));
#15492=CARTESIAN_POINT('Ctrl Pts',(0.127610169584502,0.0993491139263089,
0.401828938511835));
#15493=CARTESIAN_POINT('Ctrl Pts',(-0.014271649480085,0.16109289816887,
0.409767928149142));
#15494=CARTESIAN_POINT('Ctrl Pts',(-0.143088751545671,0.0753671745551693,
0.417706917786446));
#15495=CARTESIAN_POINT('Ctrl Pts',(-0.140917908083783,-0.0793520321139836,
0.425645907423752));
#15496=CARTESIAN_POINT('Ctrl Pts',(-0.00974637750615997,-0.161429891732714,
0.433584897061058));
#15497=CARTESIAN_POINT('Ctrl Pts',(0.130347293715478,-0.0957297489831606,
0.441523886698364));
#15498=CARTESIAN_POINT('Ctrl Pts',(0.15111695082405,0.0576044181723055,
0.449462876335669));
#15499=CARTESIAN_POINT('Ctrl Pts',(0.0335493961742207,0.158205688379633,
0.457401865972975));
#15500=CARTESIAN_POINT('Ctrl Pts',(-0.114730331382826,0.113980493419335,
0.465340855610281));
#15501=CARTESIAN_POINT('Ctrl Pts',(-0.157982303542021,-0.03458603167299,
0.473279845247587));
#15502=CARTESIAN_POINT('Ctrl Pts',(-0.0566123040428622,-0.151491415104245,
0.481218834884892));
#15503=CARTESIAN_POINT('Ctrl Pts',(0.0965823799129518,-0.129716790392294,
0.489157824522198));
#15504=CARTESIAN_POINT('Ctrl Pts',(0.161362514281243,0.0108046658515635,
0.497096814159504));
#15505=CARTESIAN_POINT('Ctrl Pts',(0.0784263257203939,0.141435191000425,
0.50503580379681));
#15506=CARTESIAN_POINT('Ctrl Pts',(-0.076303789130349,0.14259149197508,
0.512974793434115));
#15507=CARTESIAN_POINT('Ctrl Pts',(-0.161183014472451,0.0132150544797126,
0.520913783071421));
#15508=CARTESIAN_POINT('Ctrl Pts',(-0.0985102366584373,-0.128258859705,
0.528852772708727));
#15509=CARTESIAN_POINT('Ctrl Pts',(0.0543419114689404,-0.152320577983508,
0.536791762346032));
#15510=CARTESIAN_POINT('Ctrl Pts',(0.157447763940923,-0.0369432463290883,
0.544730751983338));
#15511=CARTESIAN_POINT('Ctrl Pts',(0.116420979124965,0.112253095453589,
0.552669741620643));
#15512=CARTESIAN_POINT('Ctrl Pts',(-0.0311812332291155,0.158689421555565,
0.56060873125795));
#15513=CARTESIAN_POINT('Ctrl Pts',(-0.150239163551416,0.0598564579197502,
0.568547720895255));
#15514=CARTESIAN_POINT('Ctrl Pts',(-0.131763436204723,-0.0937709907106254,
0.576486710532561));
#15515=CARTESIAN_POINT('Ctrl Pts',(0.00733268664935855,-0.161557523891122,
0.584425700169866));
#15516=CARTESIAN_POINT('Ctrl Pts',(0.139716237417787,-0.0814492162095161,
0.592364689807173));
#15517=CARTESIAN_POINT('Ctrl Pts',(0.144199148209332,0.0732202668325601,
0.600303679444478));
#15518=CARTESIAN_POINT('Ctrl Pts',(0.0166776214282734,0.160861613702037,
0.608242669081784));
#15519=CARTESIAN_POINT('Ctrl Pts',(-0.126111124778327,0.101245177793678,
0.616181658719089));
#15520=CARTESIAN_POINT('Ctrl Pts',(-0.153453779210204,-0.0510542795996006,
0.624120648356396));
#15521=CARTESIAN_POINT('Ctrl Pts',(-0.0403200156494649,-0.156617042997737,
0.6320596379937));
#15522=CARTESIAN_POINT('Ctrl Pts',(0.10972395892722,-0.118807637198397,
0.639998627631007));
#15523=CARTESIAN_POINT('Ctrl Pts',(0.159323168980049,0.0277620180369333,
0.647937617268312));
#15524=CARTESIAN_POINT('Ctrl Pts',(0.0630729369615192,0.148917448414806,
0.655876606905618));
#15525=CARTESIAN_POINT('Ctrl Pts',(-0.0909162461746061,0.133749160748195,
0.663815596542924));
#15526=CARTESIAN_POINT('Ctrl Pts',(-0.161677836835157,-0.00385731715476066,
0.671754586180229));
#15527=CARTESIAN_POINT('Ctrl Pts',(-0.0844344483789265,-0.137932685561743,
0.679693575817536));
#15528=CARTESIAN_POINT('Ctrl Pts',(0.0701028908975481,-0.145740133481257,
0.687632565454841));
#15529=CARTESIAN_POINT('Ctrl Pts',(0.1604658380222,-0.0201324774223393,
0.695571555092147));
#15530=CARTESIAN_POINT('Ctrl Pts',(0.10393330787963,0.123905081947942,0.703510544729453));
#15531=CARTESIAN_POINT('Ctrl Pts',(-0.0477430426119635,0.15451603056473,
0.711449534366758));
#15532=CARTESIAN_POINT('Ctrl Pts',(-0.155713909636705,0.0436781428746717,
0.719388524004064));
#15533=CARTESIAN_POINT('Ctrl Pts',(-0.121139364160222,-0.10714409115852,
0.72732751364137));
#15534=CARTESIAN_POINT('Ctrl Pts',(0.0243299669821161,-0.159883252800214,
0.735266503278675));
#15535=CARTESIAN_POINT('Ctrl Pts',(0.147526880793862,-0.0662602540182413,
0.743205492915981));
#15536=CARTESIAN_POINT('Ctrl Pts',(0.135673045916277,0.0880194662056535,
0.751144482553287));
#15537=CARTESIAN_POINT('Ctrl Pts',(-0.000380164216571841,0.161723397486253,
0.759083472190592));
#15538=CARTESIAN_POINT('Ctrl Pts',(-0.136085360063504,0.0873806419964673,
0.767022461827899));
#15539=CARTESIAN_POINT('Ctrl Pts',(-0.147213735311121,-0.0669531026545853,
0.774961451465203));
#15540=CARTESIAN_POINT('Ctrl Pts',(-0.023578025097595,-0.159995870421162,
0.78290044110251));
#15541=CARTESIAN_POINT('Ctrl Pts',(0.121641751185188,-0.106573384050283,
0.790839430739816));
#15542=CARTESIAN_POINT('Ctrl Pts',(0.155506840911589,0.0444097314676148,
0.798778420377121));
#15543=CARTESIAN_POINT('Ctrl Pts',(0.047016075363265,0.15473878142458,0.806717410014428));
#15544=CARTESIAN_POINT('Ctrl Pts',(-0.104514684958047,0.123415081928621,
0.814656399651731));
#15545=CARTESIAN_POINT('Ctrl Pts',(-0.16036941405942,-0.020886666885039,
0.82259538928904));
#15546=CARTESIAN_POINT('Ctrl Pts',(-0.0694169354231278,-0.146068103622213,
0.830534378926343));
#15547=CARTESIAN_POINT('Ctrl Pts',(0.085081990139753,-0.137534202194171,
0.838473368563651));
#15548=CARTESIAN_POINT('Ctrl Pts',(0.161694184779289,-0.00309716449182502,
0.846412358200955));
#15549=CARTESIAN_POINT('Ctrl Pts',(0.0902864348795877,0.134175115040242,
0.854351347838261));
#15550=CARTESIAN_POINT('Ctrl Pts',(-0.0637723584188847,0.148619272374149,
0.862290337475567));
#15551=CARTESIAN_POINT('Ctrl Pts',(-0.159451928190027,0.0270126713934565,
0.870229327112872));
#15552=CARTESIAN_POINT('Ctrl Pts',(-0.109164185657521,-0.119322178948671,
0.878168316750179));
#15553=CARTESIAN_POINT('Ctrl Pts',(0.0410558873341998,-0.156425752146281,
0.886107306387484));
#15554=CARTESIAN_POINT('Ctrl Pts',(0.153692109215179,-0.0503322698109037,
0.894046296024789));
#15555=CARTESIAN_POINT('Ctrl Pts',(0.125633738317809,0.101836956040625,
0.901985285662096));
#15556=CARTESIAN_POINT('Ctrl Pts',(-0.0174337097671096,0.160781427979367,
0.909924275299401));
#15557=CARTESIAN_POINT('Ctrl Pts',(-0.144541791370401,0.072541521673891,
0.917863264936708));
#15558=CARTESIAN_POINT('Ctrl Pts',(-0.13933176907,-0.082105176128868,0.925802254574012));
#15559=CARTESIAN_POINT('Ctrl Pts',(-0.00657306121577474,-0.161590212220858,
0.933741244211319));
#15560=CARTESIAN_POINT('Ctrl Pts',(0.132202833700187,-0.0931504835251481,
0.941680233848624));
#15561=CARTESIAN_POINT('Ctrl Pts',(0.149956094815541,0.0605621288182698,
0.949619223485929));
#15562=CARTESIAN_POINT('Ctrl Pts',(0.0304348282896272,0.158834262822317,
0.957558213123236));
#15563=CARTESIAN_POINT('Ctrl Pts',(-0.116947437700435,0.111704514835484,
0.965497202760542));
#15564=CARTESIAN_POINT('Ctrl Pts',(-0.157272339407096,-0.0376830608728604,
0.973436192397847));
#15565=CARTESIAN_POINT('Ctrl Pts',(-0.0536251929639052,-0.152574376940928,
0.981375182035153));
#15566=CARTESIAN_POINT('Ctrl Pts',(0.0991121424632477,-0.127794307524525,
0.989314171672459));
#15567=CARTESIAN_POINT('Ctrl Pts',(0.161119104064031,0.0139726921146952,
0.997253161309763));
#15568=CARTESIAN_POINT('Ctrl Pts',(0.0756325681075411,0.142948649734045,
1.00519215094707));
#15569=CARTESIAN_POINT('Ctrl Pts',(-0.0790904005129918,0.141064915432658,
1.01313114058437));
#15570=CARTESIAN_POINT('Ctrl Pts',(-0.161411527883023,0.0100459188627121,
1.02107013022168));
#15571=CARTESIAN_POINT('Ctrl Pts',(-0.095971463730607,-0.130169427934261,
1.02900911985899));
#15572=CARTESIAN_POINT('Ctrl Pts',(0.0573238981132153,-0.151223584550935,
1.03694810949629));
#15573=CARTESIAN_POINT('Ctrl Pts',(0.158143159897702,-0.0338429135403315,
1.0448870991336));
#15574=CARTESIAN_POINT('Ctrl Pts',(0.114193197054413,0.114518625410106,
1.0528260887709));
#15575=CARTESIAN_POINT('Ctrl Pts',(-0.0342928115212847,0.158046211271557,
1.06076507840821));
#15576=CARTESIAN_POINT('Ctrl Pts',(-0.151386101389109,0.0568933223281485,
1.06870406804552));
#15577=CARTESIAN_POINT('Ctrl Pts',(-0.129895790602315,-0.0963415040526547,
1.07664305768282));
#15578=CARTESIAN_POINT('Ctrl Pts',(0.0105052141409744,-0.161382286187737,
1.08458204732013));
#15579=CARTESIAN_POINT('Ctrl Pts',(0.141289415307547,-0.0786886455683398,
1.09252103695743));
#15580=CARTESIAN_POINT('Ctrl Pts',(0.14273283995608,0.076039057183793,1.10046002659474));
#15581=CARTESIAN_POINT('Ctrl Pts',(0.013514131745196,0.161158214381091,
1.10839901623204));
#15582=CARTESIAN_POINT('Ctrl Pts',(-0.128075837894479,0.0987480712062529,
1.11633800586935));
#15583=CARTESIAN_POINT('Ctrl Pts',(-0.152421155552179,-0.0540591635106084,
1.12427699550666));
#15584=CARTESIAN_POINT('Ctrl Pts',(-0.0372353514058616,-0.157378938949945,
1.13221598514396));
#15585=CARTESIAN_POINT('Ctrl Pts',(0.11203686504723,-0.116629081663695,
1.14015497478127));
#15586=CARTESIAN_POINT('Ctrl Pts',(0.158747009937404,0.0308867067726846,
1.14809396441857));
#15587=CARTESIAN_POINT('Ctrl Pts',(0.0601351468730053,0.150127831962932,
1.15603295405588));
#15588=CARTESIAN_POINT('Ctrl Pts',(-0.0935263218228598,0.13193721592339,
1.16397194369318));
#15589=CARTESIAN_POINT('Ctrl Pts',(-0.161570852667341,-0.00703287904607843,
1.17191093333049));
#15590=CARTESIAN_POINT('Ctrl Pts',(-0.0817083410685703,-0.13956485524354,
1.17984992296779));
#15591=CARTESIAN_POINT('Ctrl Pts',(0.0729525569401478,-0.144334771469742,
1.1877889126051));
#15592=CARTESIAN_POINT('Ctrl Pts',(0.160830388835411,-0.016976096323307,
1.19572790224241));
#15593=CARTESIAN_POINT('Ctrl Pts',(0.101479022178261,0.125923031559255,
1.20366689187971));
#15594=CARTESIAN_POINT('Ctrl Pts',(-0.0507694344715009,0.153548254118279,
1.21160588151702));
#15595=CARTESIAN_POINT('Ctrl Pts',(-0.15654195331917,0.0406105733811438,
1.21954487115432));
#15596=CARTESIAN_POINT('Ctrl Pts',(-0.119011042423884,-0.109503304062093,
1.22748386079163));
#15597=CARTESIAN_POINT('Ctrl Pts',(0.0274663214511058,-0.159374411387982,
1.23542285042894));
#15598=CARTESIAN_POINT('Ctrl Pts',(0.148800150427453,-0.0633491677300162,
1.24336184006624));
#15599=CARTESIAN_POINT('Ctrl Pts',(0.133917639627974,0.0906678973829495,
1.25130082970354));
#15600=CARTESIAN_POINT('Ctrl Pts',(-0.00355729227603857,0.161684716318317,
1.25923981934086));
#15601=CARTESIAN_POINT('Ctrl Pts',(-0.137775766897813,0.0846902584421788,
1.26717880897816));
#15602=CARTESIAN_POINT('Ctrl Pts',(-0.14586996931591,-0.0698323268364953,
1.27511779861547));
#15603=CARTESIAN_POINT('Ctrl Pts',(-0.0204302119447119,-0.160428202816007,
1.28305678825277));
#15604=CARTESIAN_POINT('Ctrl Pts',(0.123712004283314,-0.104163053984564,
1.29099577789008));
#15605=CARTESIAN_POINT('Ctrl Pts',(0.15460435913624,0.0474562320176185,
1.29893476752738));
#15606=CARTESIAN_POINT('Ctrl Pts',(0.043967018911749,0.155632589980133,
1.30687375716469));
#15607=CARTESIAN_POINT('Ctrl Pts',(-0.106919113837756,0.121337978043289,
1.31481274680199));
#15608=CARTESIAN_POINT('Ctrl Pts',(-0.159928125575155,-0.0240332370134145,
1.3227517364393));
#15609=CARTESIAN_POINT('Ctrl Pts',(-0.0665338988230771,-0.147403670583407,
1.33069072607661));
#15610=CARTESIAN_POINT('Ctrl Pts',(0.0877675522160205,-0.135836146169277,
1.33862971571391));
#15611=CARTESIAN_POINT('Ctrl Pts',(0.161723824721502,8.00609866524728E-5,
1.34656870535122));
#15612=CARTESIAN_POINT('Ctrl Pts',(0.0876330185603928,0.135922977069285,
1.35450769498852));
#15613=CARTESIAN_POINT('Ctrl Pts',(-0.0666798087068602,0.147337724435113,
1.36244668462583));
#15614=CARTESIAN_POINT('Ctrl Pts',(-0.159951843822013,0.0238748801740983,
1.37038567426313));
#15615=CARTESIAN_POINT('Ctrl Pts',(-0.106798922716859,-0.121443775659372,
1.37832466390044));
#15616=CARTESIAN_POINT('Ctrl Pts',(0.0441210824430389,-0.155588987406456,
1.38626365353774));
#15617=CARTESIAN_POINT('Ctrl Pts',(0.154651279966657,-0.0473031264624986,
1.39420264317505));
#15618=CARTESIAN_POINT('Ctrl Pts',(0.123608792556459,0.10428547082216,1.40214163281236));
#15619=CARTESIAN_POINT('Ctrl Pts',(-0.020589002599541,0.160407931346284,
1.41008062244966));
#15620=CARTESIAN_POINT('Ctrl Pts',(-0.145939110542184,0.0696878015005003,
1.41801961208697));
#15621=CARTESIAN_POINT('Ctrl Pts',(-0.137691710982408,-0.0848265016612731,
1.42595860172427));
#15622=CARTESIAN_POINT('Ctrl Pts',(-0.00339746822928561,-0.161688398335044,
1.43389759136158));
#15623=CARTESIAN_POINT('Ctrl Pts',(0.134007838137522,-0.0905348079547059,
1.44183658099889));
#15624=CARTESIAN_POINT('Ctrl Pts',(0.148736417039967,0.0634956003383226,
1.44977557063619));
#15625=CARTESIAN_POINT('Ctrl Pts',(0.0273102951854726,0.159403164432859,
1.4577145602735));
#15626=CARTESIAN_POINT('Ctrl Pts',(-0.119122786779006,0.109382310628272,
1.4656535499108));
#15627=CARTESIAN_POINT('Ctrl Pts',(-0.156495242883694,-0.0407596439572756,
1.47359253954811));
#15628=CARTESIAN_POINT('Ctrl Pts',(-0.0506295842364637,-0.153609649276743,
1.48153152918541));
#15629=CARTESIAN_POINT('Ctrl Pts',(0.10162683549218,-0.125801210382132,
1.48947051882272));
#15630=CARTESIAN_POINT('Ctrl Pts',(0.160769288057966,0.017094787472962,
1.49740950846002));
#15631=CARTESIAN_POINT('Ctrl Pts',(0.0728951834924312,0.144484958595688,
1.50534849809733));
#15632=CARTESIAN_POINT('Ctrl Pts',(-0.0820226078184241,0.139326700971572,
1.51328748773464));
#15633=CARTESIAN_POINT('Ctrl Pts',(-0.134767702434085,0.0512744806661359,
1.51858014749284));
#15634=CARTESIAN_POINT('Ctrl Pts',(-0.136701386950156,0.00581475974600206,
1.52122647737194));
#15635=CARTESIAN_POINT('Ctrl Pts',(0.0740036351041134,-0.103579689087085,
-0.0054992613140312));
#15636=CARTESIAN_POINT('Ctrl Pts',(0.108448814220036,-0.0789699563406641,
-0.00285293143492929));
#15637=CARTESIAN_POINT('Ctrl Pts',(0.150264871169078,0.00688399744800666,
0.00243972832327453));
#15638=CARTESIAN_POINT('Ctrl Pts',(0.0755551489391376,0.130236700260234,
0.0103787179605803));
#15639=CARTESIAN_POINT('Ctrl Pts',(-0.0683810376584167,0.133979098529349,
0.0183177075978859));
#15640=CARTESIAN_POINT('Ctrl Pts',(-0.14968704878538,0.0152677557027674,
0.0262566972351917));
#15641=CARTESIAN_POINT('Ctrl Pts',(-0.0939816891590436,-0.11752176362514,
0.0341956868724974));
#15642=CARTESIAN_POINT('Ctrl Pts',(0.0477663481097245,-0.142674779628989,
0.0421346765098031));
#15643=CARTESIAN_POINT('Ctrl Pts',(0.14578288888032,-0.0372469160898187,
0.0500736661471088));
#15644=CARTESIAN_POINT('Ctrl Pts',(0.110347650287512,0.102292747252513,
0.0580126557844146));
#15645=CARTESIAN_POINT('Ctrl Pts',(-0.0261045975097209,0.148182615303324,
0.0659516454217203));
#15646=CARTESIAN_POINT('Ctrl Pts',(-0.13865919166998,0.0584255608647477,
0.073890635059026));
#15647=CARTESIAN_POINT('Ctrl Pts',(-0.124281158904105,-0.0848182532198701,
0.0818296246963318));
#15648=CARTESIAN_POINT('Ctrl Pts',(0.00386794697500161,-0.15041563023346,
0.0897686143336374));
#15649=CARTESIAN_POINT('Ctrl Pts',(0.128476112576568,-0.0783184064825255,
0.0977076039709433));
#15650=CARTESIAN_POINT('Ctrl Pts',(0.135473254782295,0.0654742669580799,
0.105646593608249));
#15651=CARTESIAN_POINT('Ctrl Pts',(0.0184538891044151,0.149329569763132,
0.113585583245555));
#15652=CARTESIAN_POINT('Ctrl Pts',(-0.115458732720671,0.096483973363118,
0.12152457288286));
#15653=CARTESIAN_POINT('Ctrl Pts',(-0.143676805334049,-0.0446861343604874,
0.129463562520166));
#15654=CARTESIAN_POINT('Ctrl Pts',(-0.0403686054279526,-0.144949124289353,
0.137402552157472));
#15655=CARTESIAN_POINT('Ctrl Pts',(0.0998942839726139,-0.112521137758025,
0.145341541794778));
#15656=CARTESIAN_POINT('Ctrl Pts',(0.14871080372247,0.0229122455632766,
0.153280531432083));
#15657=CARTESIAN_POINT('Ctrl Pts',(0.0613927738894439,0.137371034794898,
0.161219521069389));
#15658=CARTESIAN_POINT('Ctrl Pts',(-0.0821261326059948,0.126076058196294,
0.169158510706695));
#15659=CARTESIAN_POINT('Ctrl Pts',(-0.150464193336327,-0.000632910110818063,
0.177097500344));
#15660=CARTESIAN_POINT('Ctrl Pts',(-0.0810625969653723,-0.126762492068094,
0.185036489981306));
#15661=CARTESIAN_POINT('Ctrl Pts',(0.0625462512992226,-0.136849700411639,
0.192975479618612));
#15662=CARTESIAN_POINT('Ctrl Pts',(0.148898293097928,-0.0216603868066741,
0.200914469255917));
#15663=CARTESIAN_POINT('Ctrl Pts',(0.0989441522193119,0.113357526360621,
0.208853458893223));
#15664=CARTESIAN_POINT('Ctrl Pts',(-0.0415865789238149,0.144604393083411,
0.216792448530529));
#15665=CARTESIAN_POINT('Ctrl Pts',(-0.144047647180085,0.0434758483035601,
0.224731438167835));
#15666=CARTESIAN_POINT('Ctrl Pts',(-0.114642966671137,-0.0974518559926297,
0.232670427805141));
#15667=CARTESIAN_POINT('Ctrl Pts',(0.0197094928286333,-0.149169064945282,
0.240609417442446));
#15668=CARTESIAN_POINT('Ctrl Pts',(0.136019262424063,-0.0643322181611298,
0.248548407079752));
#15669=CARTESIAN_POINT('Ctrl Pts',(0.127812719278849,0.0793963653730636,
0.256487396717058));
#15670=CARTESIAN_POINT('Ctrl Pts',(0.00260239121171357,0.150443017797356,
0.264426386354363));
#15671=CARTESIAN_POINT('Ctrl Pts',(-0.124990247656303,0.0837693979610897,
0.272365375991669));
#15672=CARTESIAN_POINT('Ctrl Pts',(-0.138162880936044,-0.0595893646165358,
0.280304365628975));
#15673=CARTESIAN_POINT('Ctrl Pts',(-0.0248568656394851,-0.148398147813718,
0.288243355266281));
#15674=CARTESIAN_POINT('Ctrl Pts',(0.111203906597776,-0.101358597076653,
0.296182344903586));
#15675=CARTESIAN_POINT('Ctrl Pts',(0.145465123646218,0.0384678027257296,
0.304121334540892));
#15676=CARTESIAN_POINT('Ctrl Pts',(0.0465629893725541,0.143079565503422,
0.312060324178198));
#15677=CARTESIAN_POINT('Ctrl Pts',(-0.0949643705016135,0.116711791945748,
0.319999313815503));
#15678=CARTESIAN_POINT('Ctrl Pts',(-0.149558357514911,-0.0164976283567656,
0.327938303452809));
#15679=CARTESIAN_POINT('Ctrl Pts',(-0.0672419181269484,-0.134604600554976,
0.335877293090115));
#15680=CARTESIAN_POINT('Ctrl Pts',(0.0766298889166206,-0.12949028600085,
0.343816282727421));
#15681=CARTESIAN_POINT('Ctrl Pts',(0.150352284446295,-0.00583648916182633,
0.351755272364726));
#15682=CARTESIAN_POINT('Ctrl Pts',(0.0864374678803939,0.123160213504125,
0.359694262002032));
#15683=CARTESIAN_POINT('Ctrl Pts',(-0.0566049265834532,0.139412181427728,
0.367633251639338));
#15684=CARTESIAN_POINT('Ctrl Pts',(-0.147829390149123,0.0280418517950267,
0.375572241276644));
#15685=CARTESIAN_POINT('Ctrl Pts',(-0.103726178443039,-0.108998871322406,
0.383511230913949));
#15686=CARTESIAN_POINT('Ctrl Pts',(0.0353312408083745,-0.146258597924691,
0.391450220551255));
#15687=CARTESIAN_POINT('Ctrl Pts',(0.142045330507792,-0.0496286018832686,
0.399389210188561));
#15688=CARTESIAN_POINT('Ctrl Pts',(0.118726655129599,0.0924329779120693,
0.407328199825866));
#15689=CARTESIAN_POINT('Ctrl Pts',(-0.0132781361506635,0.1498785012746,
0.415267189463172));
#15690=CARTESIAN_POINT('Ctrl Pts',(-0.133127703795094,0.0701205285647604,
0.423206179100478));
#15691=CARTESIAN_POINT('Ctrl Pts',(-0.131107982452518,-0.0738279823724454,
0.431145168737783));
#15692=CARTESIAN_POINT('Ctrl Pts',(-0.00906788859151817,-0.150192035209753,
0.439084158375089));
#15693=CARTESIAN_POINT('Ctrl Pts',(0.121273235812024,-0.0890655731449414,
0.447023148012395));
#15694=CARTESIAN_POINT('Ctrl Pts',(0.14059702422731,0.0535943170716914,
0.4549621376497));
#15695=CARTESIAN_POINT('Ctrl Pts',(0.031213872705855,0.14719228306762,0.462901127287006));
#15696=CARTESIAN_POINT('Ctrl Pts',(-0.106743440051405,0.106045801661112,
0.470840116924312));
#15697=CARTESIAN_POINT('Ctrl Pts',(-0.146984449047318,-0.0321783433727119,
0.478779106561618));
#15698=CARTESIAN_POINT('Ctrl Pts',(-0.0526712684425847,-0.140945420374714,
0.486718096198923));
#15699=CARTESIAN_POINT('Ctrl Pts',(0.0898588486235595,-0.120686624644175,
0.49465708583623));
#15700=CARTESIAN_POINT('Ctrl Pts',(0.150129348203927,0.0100525047535443,
0.502596075473534));
#15701=CARTESIAN_POINT('Ctrl Pts',(0.0729667185397875,0.131589254992538,
0.510535065110842));
#15702=CARTESIAN_POINT('Ctrl Pts',(-0.0709919412117167,0.132665060686482,
0.518474054748145));
#15703=CARTESIAN_POINT('Ctrl Pts',(-0.149962344179375,0.0122950954523496,
0.526413044385453));
#15704=CARTESIAN_POINT('Ctrl Pts',(-0.0916524986414713,-0.119330187030486,
0.534352034022757));
#15705=CARTESIAN_POINT('Ctrl Pts',(0.0505589280467443,-0.141716861518734,
0.542291023660064));
#15706=CARTESIAN_POINT('Ctrl Pts',(0.146487121137799,-0.0343714617774037,
0.550230013297369));
#15707=CARTESIAN_POINT('Ctrl Pts',(0.108316394245265,0.104438655591022,
0.558169002934674));
#15708=CARTESIAN_POINT('Ctrl Pts',(-0.0290105681715044,0.147642341414387,
0.566107992571982));
#15709=CARTESIAN_POINT('Ctrl Pts',(-0.139780343651344,0.0556895822633619,
0.574046982209285));
#15710=CARTESIAN_POINT('Ctrl Pts',(-0.122590794290966,-0.0872431727934394,
0.581985971846593));
#15711=CARTESIAN_POINT('Ctrl Pts',(0.00682222554696161,-0.150310782322966,
0.589924961483898));
#15712=CARTESIAN_POINT('Ctrl Pts',(0.129989965454297,-0.0757791721064987,
0.597863951121203));
#15713=CARTESIAN_POINT('Ctrl Pts',(0.134160800782372,0.0681230766876274,
0.60580294075851));
#15714=CARTESIAN_POINT('Ctrl Pts',(0.015516617634347,0.149663317553585,
0.613741930395814));
#15715=CARTESIAN_POINT('Ctrl Pts',(-0.117331965534667,0.0941970482962578,
0.621680920033121));
#15716=CARTESIAN_POINT('Ctrl Pts',(-0.142771175541451,-0.0475001629309618,
0.629619909670426));
#15717=CARTESIAN_POINT('Ctrl Pts',(-0.0375131590877193,-0.145714230393655,
0.637558899307733));
#15718=CARTESIAN_POINT('Ctrl Pts',(0.102085583566124,-0.110536906379362,
0.645497888945037));
#15719=CARTESIAN_POINT('Ctrl Pts',(0.148231970847143,0.0258293798362968,
0.653436878582344));
#15720=CARTESIAN_POINT('Ctrl Pts',(0.0586821478180281,0.138550639014834,
0.661375868219649));
#15721=CARTESIAN_POINT('Ctrl Pts',(-0.0845871597882484,0.124438283670714,
0.669314857856955));
#15722=CARTESIAN_POINT('Ctrl Pts',(-0.150422719745043,-0.00358879206139753,
0.67725384749426));
#15723=CARTESIAN_POINT('Ctrl Pts',(-0.078556588917505,-0.128330574617282,
0.685192837131567));
#15724=CARTESIAN_POINT('Ctrl Pts',(0.065222715229363,-0.135594511179713,
0.693131826768872));
#15725=CARTESIAN_POINT('Ctrl Pts',(0.149295093588351,-0.0187309656558678,
0.701070816406178));
#15726=CARTESIAN_POINT('Ctrl Pts',(0.0966980456281902,0.11527949520901,
0.709009806043483));
#15727=CARTESIAN_POINT('Ctrl Pts',(-0.044419435954706,0.14375947882982,
0.716948795680789));
#15728=CARTESIAN_POINT('Ctrl Pts',(-0.144873968183829,0.0406375120624596,
0.724887785318095));
#15729=CARTESIAN_POINT('Ctrl Pts',(-0.112706311402131,-0.099685311927494,
0.732826774955401));
#15730=CARTESIAN_POINT('Ctrl Pts',(0.0226362492002416,-0.148753064728429,
0.740765764592706));
#15731=CARTESIAN_POINT('Ctrl Pts',(0.137256875023267,-0.0616475814838108,
0.748704754230013));
#15732=CARTESIAN_POINT('Ctrl Pts',(0.126228238590478,0.0818920376245527,
0.756643743867318));
#15733=CARTESIAN_POINT('Ctrl Pts',(-0.000353699285724532,0.150465108715513,
0.764582733504624));
#15734=CARTESIAN_POINT('Ctrl Pts',(-0.126611849706441,0.0812976848247803,
0.772521723141928));
#15735=CARTESIAN_POINT('Ctrl Pts',(-0.136965528997667,-0.0622921978288208,
0.780460712779236));
#15736=CARTESIAN_POINT('Ctrl Pts',(-0.0219366533522686,-0.148857842533265,
0.788399702416541));
#15737=CARTESIAN_POINT('Ctrl Pts',(0.113173725020093,-0.0991543342927188,
0.796338692053846));
#15738=CARTESIAN_POINT('Ctrl Pts',(0.144681314438483,0.0413181715024817,
0.804277681691154));
#15739=CARTESIAN_POINT('Ctrl Pts',(0.0437430761464933,0.143966723006387,
0.812216671328456));
#15740=CARTESIAN_POINT('Ctrl Pts',(-0.0972389504488157,0.114823606281847,
0.820155660965765));
#15741=CARTESIAN_POINT('Ctrl Pts',(-0.149205382128735,-0.0194326526180533,
0.828094650603069));
#15742=CARTESIAN_POINT('Ctrl Pts',(-0.0645845121824554,-0.135899649852787,
0.836033640240376));
#15743=CARTESIAN_POINT('Ctrl Pts',(0.0791590524011713,-0.127959831458565,
0.843972629877681));
#15744=CARTESIAN_POINT('Ctrl Pts',(0.150437929635691,-0.00288155702400619,
0.851911619514986));
#15745=CARTESIAN_POINT('Ctrl Pts',(0.0840011924733913,0.12483458538003,
0.859850609152293));
#15746=CARTESIAN_POINT('Ctrl Pts',(-0.0593328794206009,0.138273220341526,
0.867789598789597));
#15747=CARTESIAN_POINT('Ctrl Pts',(-0.148351766552825,0.0251321985630355,
0.875728588426904));
#15748=CARTESIAN_POINT('Ctrl Pts',(-0.1015647786165,-0.111015628577859,
0.883667578064211));
#15749=CARTESIAN_POINT('Ctrl Pts',(0.0381978034543637,-0.145536256153639,
0.891606567701514));
#15750=CARTESIAN_POINT('Ctrl Pts',(0.142992914329196,-0.046828415471795,
0.899545557338823));
#15751=CARTESIAN_POINT('Ctrl Pts',(0.116887812080083,0.0947476302135675,
0.907484546976125));
#15752=CARTESIAN_POINT('Ctrl Pts',(-0.0162200712834111,0.149588713917584,
0.915423536613434));
#15753=CARTESIAN_POINT('Ctrl Pts',(-0.134479591021026,0.067491582014154,
0.923362526250738));
#15754=CARTESIAN_POINT('Ctrl Pts',(-0.129632261667175,-0.0763894677230377,
0.931301515888044));
#15755=CARTESIAN_POINT('Ctrl Pts',(-0.00611548103612966,-0.150341195071919,
0.93924050552535));
#15756=CARTESIAN_POINT('Ctrl Pts',(0.122999603362204,-0.0866658618874593,
0.947179495162656));
#15757=CARTESIAN_POINT('Ctrl Pts',(0.139516980595786,0.0563461282555487,
0.95511848479996));
#15758=CARTESIAN_POINT('Ctrl Pts',(0.0283161238170646,0.147777099632969,
0.963057474437267));
#15759=CARTESIAN_POINT('Ctrl Pts',(-0.108806203685475,0.103928264122473,
0.970996464074573));
#15760=CARTESIAN_POINT('Ctrl Pts',(-0.146323908690103,-0.0350597745230392,
0.978935453711877));
#15761=CARTESIAN_POINT('Ctrl Pts',(-0.049892103521326,-0.14195299239598,
0.986874443349185));
#15762=CARTESIAN_POINT('Ctrl Pts',(0.0922125030920605,-0.118897974404329,
0.994813432986488));
#15763=CARTESIAN_POINT('Ctrl Pts',(0.149902882860231,0.0129999905441286,
1.0027524226238));
#15764=CARTESIAN_POINT('Ctrl Pts',(0.0703674468853664,0.132997355096976,
1.0106914122611));
#15765=CARTESIAN_POINT('Ctrl Pts',(-0.0735845641169637,0.131244755962562,
1.01863040189841));
#15766=CARTESIAN_POINT('Ctrl Pts',(-0.150174949749745,0.00934657753497952,
1.02656939153571));
#15767=CARTESIAN_POINT('Ctrl Pts',(-0.0892904610481016,-0.121107752063083,
1.03450838117302));
#15768=CARTESIAN_POINT('Ctrl Pts',(0.0533333252681307,-0.140696234703703,
1.04244737081032));
#15769=CARTESIAN_POINT('Ctrl Pts',(0.147134107472884,-0.031486957015783,
1.05038636044763));
#15770=CARTESIAN_POINT('Ctrl Pts',(0.106243698045146,0.106546471877992,
1.05832535008494));
#15771=CARTESIAN_POINT('Ctrl Pts',(-0.0319055355867657,0.147043907874068,
1.06626433972224));
#15772=CARTESIAN_POINT('Ctrl Pts',(-0.14084743801815,0.0529327237885883,
1.07420332935955));
#15773=CARTESIAN_POINT('Ctrl Pts',(-0.120853163849259,-0.0896347412088629,
1.08214231899685));
#15774=CARTESIAN_POINT('Ctrl Pts',(0.00977389921538986,-0.150147743699608,
1.09008130863416));
#15775=CARTESIAN_POINT('Ctrl Pts',(0.13145362739741,-0.0732107771302755,
1.09802029827146));
#15776=CARTESIAN_POINT('Ctrl Pts',(0.132796568802552,0.0707456384395876,
1.10595928790877));
#15777=CARTESIAN_POINT('Ctrl Pts',(0.0125733526121963,0.149939270533256,
1.11389827754607));
#15778=CARTESIAN_POINT('Ctrl Pts',(-0.119159906186493,0.0918737764630459,
1.12183726718338));
#15779=CARTESIAN_POINT('Ctrl Pts',(-0.141810437433163,-0.0502958634379693,
1.12977625682069));
#15780=CARTESIAN_POINT('Ctrl Pts',(-0.0346432321137694,-0.146423087362162,
1.13771524645799));
#15781=CARTESIAN_POINT('Ctrl Pts',(0.104237477950025,-0.108510009835838,
1.1456542360953));
#15782=CARTESIAN_POINT('Ctrl Pts',(0.147695920811486,0.0287365450185451,
1.1535932257326));
#15783=CARTESIAN_POINT('Ctrl Pts',(0.0559488704325515,0.139676762352502,
1.16153221536991));
#15784=CARTESIAN_POINT('Ctrl Pts',(-0.0870155364008756,0.12275247642644,
1.16947120500722));
#15785=CARTESIAN_POINT('Ctrl Pts',(-0.150323183223479,-0.00654328889139735,
1.17741019464452));
#15786=CARTESIAN_POINT('Ctrl Pts',(-0.0760202581255566,-0.129849121670035,
1.18534918428183));
#15787=CARTESIAN_POINT('Ctrl Pts',(0.0678740032777675,-0.134286982701248,
1.19328817391913));
#15788=CARTESIAN_POINT('Ctrl Pts',(0.149634266389533,-0.0157943143574443,
1.20122716355644));
#15789=CARTESIAN_POINT('Ctrl Pts',(0.0944146137277022,0.117156966325547,
1.20916615319374));
#15790=CARTESIAN_POINT('Ctrl Pts',(-0.047235147145783,0.142859073628774,
1.21710514283105));
#15791=CARTESIAN_POINT('Ctrl Pts',(-0.145644368043342,0.037783489796601,
1.22504413246835));
#15792=CARTESIAN_POINT('Ctrl Pts',(-0.11072615165767,-0.101880289472715,
1.23298312210566));
#15793=CARTESIAN_POINT('Ctrl Pts',(0.0255542680118797,-0.148279646041953,
1.24092211174296));
#15794=CARTESIAN_POINT('Ctrl Pts',(0.138441506664824,-0.0589391489276913,
1.24886110138027));
#15795=CARTESIAN_POINT('Ctrl Pts',(0.124595033982396,0.0843560996663564,
1.25680009101758));
#15796=CARTESIAN_POINT('Ctrl Pts',(-0.00330965325590636,0.150429120316621,
1.26473908065488));
#15797=CARTESIAN_POINT('Ctrl Pts',(-0.128184579763139,0.0787945908985174,
1.27267807029219));
#15798=CARTESIAN_POINT('Ctrl Pts',(-0.135715308561414,-0.0649709863423027,
1.2806170599295));
#15799=CARTESIAN_POINT('Ctrl Pts',(-0.0190079735469551,-0.149260078337129,
1.2885560495668));
#15800=CARTESIAN_POINT('Ctrl Pts',(0.115099858543875,-0.0969117980795561,
1.29649503920411));
#15801=CARTESIAN_POINT('Ctrl Pts',(0.143841658454547,0.0441525915281748,
1.30443402884141));
#15802=CARTESIAN_POINT('Ctrl Pts',(0.0409062781470196,0.144798309552134,
1.31237301847872));
#15803=CARTESIAN_POINT('Ctrl Pts',(-0.0994759962839106,0.112891098884786,
1.32031200811602));
#15804=CARTESIAN_POINT('Ctrl Pts',(-0.148794813708878,-0.0223601759313527,
1.32825099775333));
#15805=CARTESIAN_POINT('Ctrl Pts',(-0.0619021766503053,-0.13714224202644,
1.33618998739064));
#15806=CARTESIAN_POINT('Ctrl Pts',(0.0816576604940555,-0.126379984705639,
1.34412897702794));
#15807=CARTESIAN_POINT('Ctrl Pts',(0.150465506209006,7.4487583413377E-5,
1.35206796666525));
#15808=CARTESIAN_POINT('Ctrl Pts',(0.0815324923277053,0.126460770918471,
1.36000695630255));
#15809=CARTESIAN_POINT('Ctrl Pts',(-0.062037929094705,0.137080886684378,
1.36794594593986));
#15810=CARTESIAN_POINT('Ctrl Pts',(-0.148816880822527,0.0222128430196456,
1.37588493557716));
#15811=CARTESIAN_POINT('Ctrl Pts',(-0.0993641722043223,-0.112989531455785,
1.38382392521447));
#15812=CARTESIAN_POINT('Ctrl Pts',(0.0410496166270677,-0.144757742348562,
1.39176291485178));
#15813=CARTESIAN_POINT('Ctrl Pts',(0.143885312916173,-0.0440101443352923,
1.39970190448908));
#15814=CARTESIAN_POINT('Ctrl Pts',(0.115003831846793,0.0970256929337524,
1.40764089412639));
#15815=CARTESIAN_POINT('Ctrl Pts',(-0.0191557100743377,0.149241218055048,
1.41557988376369));
#15816=CARTESIAN_POINT('Ctrl Pts',(-0.135779636557791,0.0648365220611291,
1.423518873401));
#15817=CARTESIAN_POINT('Ctrl Pts',(-0.128106375355825,-0.0789213496179777,
1.4314578630383));
#15818=CARTESIAN_POINT('Ctrl Pts',(-0.00316095527563228,-0.150432546011701,
1.43939685267561));
#15819=CARTESIAN_POINT('Ctrl Pts',(0.12467895337041,-0.0842322751882648,
1.44733584231291));
#15820=CARTESIAN_POINT('Ctrl Pts',(0.138382210043398,0.0590753877074232,
1.45527483195022));
#15821=CARTESIAN_POINT('Ctrl Pts',(0.0254091034322018,0.148306397458819,
1.46321382158753));
#15822=CARTESIAN_POINT('Ctrl Pts',(-0.110830116988615,0.101767718932792,
1.47115281122483));
#15823=CARTESIAN_POINT('Ctrl Pts',(-0.145600909330124,-0.0379221829034233,
1.47909180086214));
#15824=CARTESIAN_POINT('Ctrl Pts',(-0.0471050325108872,-0.142916194795756,
1.48703079049945));
#15825=CARTESIAN_POINT('Ctrl Pts',(0.0945521370959566,-0.117043625665234,
1.49496978013675));
#15826=CARTESIAN_POINT('Ctrl Pts',(0.14957741911039,0.0159047428854941,
1.50290876977406));
#15827=CARTESIAN_POINT('Ctrl Pts',(0.0678206238522695,0.134426714629862,
1.51084775941136));
#15828=CARTESIAN_POINT('Ctrl Pts',(-0.0763126473618499,0.129627546381738,
1.51878674904867));
#15829=CARTESIAN_POINT('Ctrl Pts',(-0.125385920115907,0.0477050348167321,
1.52407940880687));
#15830=CARTESIAN_POINT('Ctrl Pts',(-0.127184992207234,0.00540996832206346,
1.52672573868597));
#15831=CARTESIAN_POINT('Ctrl Pts',(0.0684664424539414,-0.095829519891843,
-1.38777878078145E-17));
#15832=CARTESIAN_POINT('Ctrl Pts',(0.100334321247169,-0.0730611673843044,
0.00264632987910189));
#15833=CARTESIAN_POINT('Ctrl Pts',(0.139021564822767,0.00636891437108143,
0.00793898963730573));
#15834=CARTESIAN_POINT('Ctrl Pts',(0.0699018669780613,0.120491966796142,
0.0158779792746114));
#15835=CARTESIAN_POINT('Ctrl Pts',(-0.0632645460347191,0.123954346655885,
0.0238169689119172));
#15836=CARTESIAN_POINT('Ctrl Pts',(-0.138486976988987,0.0141253725679007,
0.0317559585492228));
#15837=CARTESIAN_POINT('Ctrl Pts',(-0.0869496735326521,-0.108728403071097,
0.0396949481865287));
#15838=CARTESIAN_POINT('Ctrl Pts',(0.0441923146003338,-0.131999388615902,
0.0476339378238343));
#15839=CARTESIAN_POINT('Ctrl Pts',(0.134874939024977,-0.034459980695041,
0.0555729274611401));
#15840=CARTESIAN_POINT('Ctrl Pts',(0.102091080224759,0.094638871230671,
0.0635119170984456));
#15841=CARTESIAN_POINT('Ctrl Pts',(-0.0241513666277066,0.137095110112719,
0.0714509067357516));
#15842=CARTESIAN_POINT('Ctrl Pts',(-0.128284260007319,0.0540539703915629,
0.0793898963730571));
#15843=CARTESIAN_POINT('Ctrl Pts',(-0.114982038412656,-0.0784718756714057,
0.0873288860103631));
#15844=CARTESIAN_POINT('Ctrl Pts',(0.00357853460314598,-0.139161043603659,
0.0952678756476685));
#15845=CARTESIAN_POINT('Ctrl Pts',(0.118863112008681,-0.0724583686054966,
0.103206865284975));
#15846=CARTESIAN_POINT('Ctrl Pts',(0.125336705278751,0.0605752693714656,
0.11114585492228));
#15847=CARTESIAN_POINT('Ctrl Pts',(0.0170731091066207,0.138156245709763,
0.119084844559586));
#15848=CARTESIAN_POINT('Ctrl Pts',(-0.106819734848208,0.0892647286947484,
0.127023834196891));
#15849=CARTESIAN_POINT('Ctrl Pts',(-0.132926439498961,-0.0413425724611633,
0.134962823834197));
#15850=CARTESIAN_POINT('Ctrl Pts',(-0.0373480950846616,-0.134103559412242,
0.142901813471503));
#15851=CARTESIAN_POINT('Ctrl Pts',(0.0924198687735613,-0.104101940294199,
0.150840803108809));
#15852=CARTESIAN_POINT('Ctrl Pts',(0.137583777756591,0.0211978768359354,
0.158779792746114));
#15853=CARTESIAN_POINT('Ctrl Pts',(0.0567991668878991,0.127092487218924,
0.16671878238342));
#15854=CARTESIAN_POINT('Ctrl Pts',(-0.075981188277068,0.116642637502503,
0.174657772020726));
#15855=CARTESIAN_POINT('Ctrl Pts',(-0.139205973057234,-0.000585553717998882,
0.182596761658032));
#15856=CARTESIAN_POINT('Ctrl Pts',(-0.0749972298318695,-0.11727771015962,
0.190535751295337));
#15857=CARTESIAN_POINT('Ctrl Pts',(0.0578663373665801,-0.126610160769685,
0.198474740932643));
#15858=CARTESIAN_POINT('Ctrl Pts',(0.13775723856723,-0.0200396862227523,
0.206413730569949));
#15859=CARTESIAN_POINT('Ctrl Pts',(0.091540828968026,0.104875747581476,
0.214352720207254));
#15860=CARTESIAN_POINT('Ctrl Pts',(-0.0384749358425138,0.133784622116252,
0.22229170984456));
#15861=CARTESIAN_POINT('Ctrl Pts',(-0.133269533752038,0.0402228439430644,
0.230230699481866));
#15862=CARTESIAN_POINT('Ctrl Pts',(-0.106065007067505,-0.0901601911982067,
0.238169689119172));
#15863=CARTESIAN_POINT('Ctrl Pts',(0.0182347644767634,-0.138007750384372,
0.246108678756477));
#15864=CARTESIAN_POINT('Ctrl Pts',(0.125841858853055,-0.0595186723796334,
0.254047668393783));
#15865=CARTESIAN_POINT('Ctrl Pts',(0.118249355954961,0.073455671106145,
0.261986658031089));
#15866=CARTESIAN_POINT('Ctrl Pts',(0.00240767183786234,0.139186381940956,
0.269925647668394));
#15867=CARTESIAN_POINT('Ctrl Pts',(-0.115638070838342,0.0775014991741366,
0.277864637305701));
#15868=CARTESIAN_POINT('Ctrl Pts',(-0.12782508485658,-0.0551306945617612,
0.285803626943006));
#15869=CARTESIAN_POINT('Ctrl Pts',(-0.0229969941138309,-0.137294515779738,
0.293742616580312));
#15870=CARTESIAN_POINT('Ctrl Pts',(0.102883268653204,-0.0937746172089793,
0.301681606217617));
#15871=CARTESIAN_POINT('Ctrl Pts',(0.134580950019115,0.0355895166223291,
0.309620595854923));
#15872=CARTESIAN_POINT('Ctrl Pts',(0.0430789950773988,0.13237388709478,
0.317559585492229));
#15873=CARTESIAN_POINT('Ctrl Pts',(-0.0878588274613298,0.107979036106918,
0.325498575129534));
#15874=CARTESIAN_POINT('Ctrl Pts',(-0.1383679148179,-0.0152632221501787,
0.33343756476684));
#15875=CARTESIAN_POINT('Ctrl Pts',(-0.0622106591311991,-0.12453304658572,
0.341376554404146));
#15876=CARTESIAN_POINT('Ctrl Pts',(0.0708961914151981,-0.119801401679107,
0.349315544041452));
#15877=CARTESIAN_POINT('Ctrl Pts',(0.1391024375543,-0.00539978406154301,
0.357254533678757));
#15878=CARTESIAN_POINT('Ctrl Pts',(0.0799699354250877,0.113944965792994,
0.365193523316063));
#15879=CARTESIAN_POINT('Ctrl Pts',(-0.0523695618881846,0.128980908622551,
0.373132512953369));
#15880=CARTESIAN_POINT('Ctrl Pts',(-0.136768314413298,0.0259436692471295,
0.381071502590675));
#15881=CARTESIAN_POINT('Ctrl Pts',(-0.0959650484377783,-0.100843221288265,
0.38901049222798));
#15882=CARTESIAN_POINT('Ctrl Pts',(0.0326876424682324,-0.135315053971568,
0.396949481865287));
#15883=CARTESIAN_POINT('Ctrl Pts',(0.13141703692502,-0.0459152284901983,
0.404888471502591));
#15884=CARTESIAN_POINT('Ctrl Pts',(0.109843140674695,0.0855168418978295,
0.412827461139898));
#15885=CARTESIAN_POINT('Ctrl Pts',(-0.0122846228212416,0.13866410438033,
0.420766450777203));
#15886=CARTESIAN_POINT('Ctrl Pts',(-0.123166656044517,0.0648738825743514,
0.428705440414509));
#15887=CARTESIAN_POINT('Ctrl Pts',(-0.121298056821252,-0.0683039326309071,
0.436644430051815));
#15888=CARTESIAN_POINT('Ctrl Pts',(-0.00838939967687663,-0.138954178686792,
0.44458341968912));
#15889=CARTESIAN_POINT('Ctrl Pts',(0.11219917790857,-0.0824013973067221,
0.452522409326426));
#15890=CARTESIAN_POINT('Ctrl Pts',(0.13007709763057,0.0495842159710775,
0.460461398963732));
#15891=CARTESIAN_POINT('Ctrl Pts',(0.0288783492374893,0.136178877755608,
0.468400388601037));
#15892=CARTESIAN_POINT('Ctrl Pts',(-0.0987565487199846,0.0981111099028881,
0.476339378238344));
#15893=CARTESIAN_POINT('Ctrl Pts',(-0.135986594552616,-0.0297706550724338,
0.484278367875649));
#15894=CARTESIAN_POINT('Ctrl Pts',(-0.0487302328423073,-0.130399425645183,
0.492217357512954));
#15895=CARTESIAN_POINT('Ctrl Pts',(0.0831353173341669,-0.111656458896056,
0.50015634715026));
#15896=CARTESIAN_POINT('Ctrl Pts',(0.13889618212661,0.00930034365552528,
0.508095336787567));
#15897=CARTESIAN_POINT('Ctrl Pts',(0.0675071113591811,0.12174331898465,
0.516034326424871));
#15898=CARTESIAN_POINT('Ctrl Pts',(-0.0656800932930844,0.122738629397884,
0.523973316062178));
#15899=CARTESIAN_POINT('Ctrl Pts',(-0.138741673886299,0.0113751364249866,
0.531912305699483));
#15900=CARTESIAN_POINT('Ctrl Pts',(-0.0847947606245053,-0.110401514355972,
0.539851295336789));
#15901=CARTESIAN_POINT('Ctrl Pts',(0.0467759446245483,-0.131113145053959,
0.547790284974095));
#15902=CARTESIAN_POINT('Ctrl Pts',(0.135526478334676,-0.031799677225719,
0.555729274611401));
#15903=CARTESIAN_POINT('Ctrl Pts',(0.100211809365564,0.0966242157284558,
0.563668264248707));
#15904=CARTESIAN_POINT('Ctrl Pts',(-0.0268399031138932,0.136595261273209,
0.571607253886012));
#15905=CARTESIAN_POINT('Ctrl Pts',(-0.129321523751272,0.0515227066069736,
0.579546243523318));
#15906=CARTESIAN_POINT('Ctrl Pts',(-0.113418152377209,-0.0807153548762533,
0.587485233160623));
#15907=CARTESIAN_POINT('Ctrl Pts',(0.00631176444456456,-0.139064040754811,
0.595424222797929));
#15908=CARTESIAN_POINT('Ctrl Pts',(0.120263693490807,-0.0701091280034811,
0.603363212435234));
#15909=CARTESIAN_POINT('Ctrl Pts',(0.124122453355413,0.0630258865426945,
0.611302202072541));
#15910=CARTESIAN_POINT('Ctrl Pts',(0.0143556138404206,0.138465021405133,
0.619241191709845));
#15911=CARTESIAN_POINT('Ctrl Pts',(-0.108552806291007,0.0871489187988374,
0.627180181347153));
#15912=CARTESIAN_POINT('Ctrl Pts',(-0.132088571872698,-0.043946046262323,
0.635119170984457));
#15913=CARTESIAN_POINT('Ctrl Pts',(-0.0347063025259737,-0.134811417789573,
0.643058160621763));
#15914=CARTESIAN_POINT('Ctrl Pts',(0.0944472082050275,-0.102266175560326,
0.65099715025907));
#15915=CARTESIAN_POINT('Ctrl Pts',(0.137140772714236,0.0238967416356601,
0.658936139896373));
#15916=CARTESIAN_POINT('Ctrl Pts',(0.054291358674537,0.128183829614862,
0.666875129533682));
#15917=CARTESIAN_POINT('Ctrl Pts',(-0.0782580734018908,0.115127406593233,
0.674814119170985));
#15918=CARTESIAN_POINT('Ctrl Pts',(-0.139167602654929,-0.00332026696803425,
0.682753108808293));
#15919=CARTESIAN_POINT('Ctrl Pts',(-0.0726787294560835,-0.118728463672822,
0.690692098445597));
#15920=CARTESIAN_POINT('Ctrl Pts',(0.0603425395611779,-0.125448888878168,
0.698631088082904));
#15921=CARTESIAN_POINT('Ctrl Pts',(0.138124349154501,-0.0173294538893964,
0.706570077720209));
#15922=CARTESIAN_POINT('Ctrl Pts',(0.0894627833767505,0.106653908470079,
0.714509067357515));
#15923=CARTESIAN_POINT('Ctrl Pts',(-0.0410958292974484,0.133002927094911,
0.72244805699482));
#15924=CARTESIAN_POINT('Ctrl Pts',(-0.134034026730954,0.0375968812502473,
0.730387046632127));
#15925=CARTESIAN_POINT('Ctrl Pts',(-0.104273258644039,-0.0922265326964679,
0.738326036269432));
#15926=CARTESIAN_POINT('Ctrl Pts',(0.0209425314183671,-0.137622876656644,
0.746265025906738));
#15927=CARTESIAN_POINT('Ctrl Pts',(0.126986869252672,-0.0570349089493802,
0.754204015544043));
#15928=CARTESIAN_POINT('Ctrl Pts',(0.11678343126468,0.0757646090434518,
0.762143005181349));
#15929=CARTESIAN_POINT('Ctrl Pts',(-0.000327234354877375,0.139206819944772,
0.770081994818654));
#15930=CARTESIAN_POINT('Ctrl Pts',(-0.117138339349379,0.0752147276530931,
0.778020984455961));
#15931=CARTESIAN_POINT('Ctrl Pts',(-0.126717322684213,-0.0576312930030564,
0.785959974093266));
#15932=CARTESIAN_POINT('Ctrl Pts',(-0.0202952816069424,-0.137719814645367,
0.793898963730571));
#15933=CARTESIAN_POINT('Ctrl Pts',(0.104705698854998,-0.0917352845351548,
0.801837953367879));
#15934=CARTESIAN_POINT('Ctrl Pts',(0.133855787965376,0.0382266115373486,
0.809776943005182));
#15935=CARTESIAN_POINT('Ctrl Pts',(0.0404700769297216,0.133194664588195,
0.81771593264249));
#15936=CARTESIAN_POINT('Ctrl Pts',(-0.0899632159395838,0.106232130635072,
0.825654922279794));
#15937=CARTESIAN_POINT('Ctrl Pts',(-0.13804135019805,-0.0179786383510676,
0.833593911917101));
#15938=CARTESIAN_POINT('Ctrl Pts',(-0.059752088941783,-0.125731196083361,
0.841532901554406));
#15939=CARTESIAN_POINT('Ctrl Pts',(0.0732361146625898,-0.118385460722959,
0.849471891191712));
#15940=CARTESIAN_POINT('Ctrl Pts',(0.139181674492094,-0.00266594955618734,
0.857410880829018));
#15941=CARTESIAN_POINT('Ctrl Pts',(0.077715950067195,0.115494055719818,
0.865349870466323));
#15942=CARTESIAN_POINT('Ctrl Pts',(-0.0548934004223171,0.127927168308903,
0.87328886010363));
#15943=CARTESIAN_POINT('Ctrl Pts',(-0.137251604915624,0.0232517257326144,
0.881227849740934));
#15944=CARTESIAN_POINT('Ctrl Pts',(-0.0939653715754795,-0.102709078207047,
0.889166839378241));
#15945=CARTESIAN_POINT('Ctrl Pts',(0.0353397195745277,-0.134646760160997,
0.897105829015547));
#15946=CARTESIAN_POINT('Ctrl Pts',(0.132293719443212,-0.0433245611326863,
0.905044818652852));
#15947=CARTESIAN_POINT('Ctrl Pts',(0.108141885842356,0.0876583043865096,
0.912983808290157));
#15948=CARTESIAN_POINT('Ctrl Pts',(-0.0150064327997127,0.138395999855801,
0.920922797927463));
#15949=CARTESIAN_POINT('Ctrl Pts',(-0.124417390671652,0.0624416423544169,
0.928861787564769));
#15950=CARTESIAN_POINT('Ctrl Pts',(-0.119932754264349,-0.0706737593172073,
0.936800777202075));
#15951=CARTESIAN_POINT('Ctrl Pts',(-0.00565790085648466,-0.139092177922979,
0.944739766839381));
#15952=CARTESIAN_POINT('Ctrl Pts',(0.113796373024222,-0.0801812402497705,
0.952678756476687));
#15953=CARTESIAN_POINT('Ctrl Pts',(0.129077866376032,0.0521301276928276,
0.960617746113992));
#15954=CARTESIAN_POINT('Ctrl Pts',(0.026197419344502,0.13671993644362,0.968556735751298));
#15955=CARTESIAN_POINT('Ctrl Pts',(-0.100664969670515,0.0961520134094621,
0.976495725388603));
#15956=CARTESIAN_POINT('Ctrl Pts',(-0.13537547797311,-0.0324364881732178,
0.98443471502591));
#15957=CARTESIAN_POINT('Ctrl Pts',(-0.0461590140787468,-0.131331607851033,
0.992373704663214));
#15958=CARTESIAN_POINT('Ctrl Pts',(0.0853128637208732,-0.110001641284132,
1.00031269430052));
#15959=CARTESIAN_POINT('Ctrl Pts',(0.138686661656432,0.0120272889735618,
1.00825168393783));
#15960=CARTESIAN_POINT('Ctrl Pts',(0.0651023256631918,0.123046060459907,
1.01619067357513));
#15961=CARTESIAN_POINT('Ctrl Pts',(-0.0680787277209358,0.121424596492465,
1.02412966321244));
#15962=CARTESIAN_POINT('Ctrl Pts',(-0.138938371616466,0.00864723620724691,
1.03206865284975));
#15963=CARTESIAN_POINT('Ctrl Pts',(-0.0826094583655966,-0.112046076191904,
1.04000764248705));
#15964=CARTESIAN_POINT('Ctrl Pts',(0.0493427524230464,-0.130168884856471,
1.04794663212436));
#15965=CARTESIAN_POINT('Ctrl Pts',(0.136125055048066,-0.0291310004912345,
1.05588562176166));
#15966=CARTESIAN_POINT('Ctrl Pts',(0.0982941990358779,0.0985743183458784,
1.06382461139897));
#15967=CARTESIAN_POINT('Ctrl Pts',(-0.0295182596522469,0.136041604476578,
1.07176360103627));
#15968=CARTESIAN_POINT('Ctrl Pts',(-0.130308774647192,0.0489721252490281,
1.07970259067358));
#15969=CARTESIAN_POINT('Ctrl Pts',(-0.111810537096203,-0.0829279783650712,
1.08764158031088));
#15970=CARTESIAN_POINT('Ctrl Pts',(0.00904258428980543,-0.13891320121148,
1.09558056994819));
#15971=CARTESIAN_POINT('Ctrl Pts',(0.121617839487272,-0.067732908692211,
1.1035195595855));
#15972=CARTESIAN_POINT('Ctrl Pts',(0.122860297649024,0.0654522196953821,
1.1114585492228));
#15973=CARTESIAN_POINT('Ctrl Pts',(0.0116325734791967,0.138720326685422,
1.11939753886011));
#15974=CARTESIAN_POINT('Ctrl Pts',(-0.110243974478508,0.0849994817198388,
1.12733652849741));
#15975=CARTESIAN_POINT('Ctrl Pts',(-0.131199719314147,-0.0465325633653302,
1.13527551813472));
#15976=CARTESIAN_POINT('Ctrl Pts',(-0.0320511128216771,-0.13546723577438,
1.14321450777202));
#15977=CARTESIAN_POINT('Ctrl Pts',(0.0964380908528195,-0.100390938007982,
1.15115349740933));
#15978=CARTESIAN_POINT('Ctrl Pts',(0.136644831685568,0.0265863832644056,
1.15909248704664));
#15979=CARTESIAN_POINT('Ctrl Pts',(0.0517625939920979,0.129225692742072,
1.16703147668394));
#15980=CARTESIAN_POINT('Ctrl Pts',(-0.0805047509788913,0.113567736929491,
1.17497046632125));
#15981=CARTESIAN_POINT('Ctrl Pts',(-0.139075513779617,-0.00605369873671642,
1.18290945595855));
#15982=CARTESIAN_POINT('Ctrl Pts',(-0.0703321751825429,-0.12013338809653,
1.19084844559586));
#15983=CARTESIAN_POINT('Ctrl Pts',(0.0627954496153871,-0.124239193932754,
1.19878743523316));
#15984=CARTESIAN_POINT('Ctrl Pts',(0.138438143943654,-0.0146125323915816,
1.20672642487047));
#15985=CARTESIAN_POINT('Ctrl Pts',(0.0873502052771435,0.108390901091839,
1.21466541450777));
#15986=CARTESIAN_POINT('Ctrl Pts',(-0.043700859820065,0.132169893139269,
1.22260440414508));
#15987=CARTESIAN_POINT('Ctrl Pts',(-0.134746782767514,0.0349564062120582,
1.23054339378239));
#15988=CARTESIAN_POINT('Ctrl Pts',(-0.102441260891455,-0.0942572748833364,
1.23848238341969));
#15989=CARTESIAN_POINT('Ctrl Pts',(0.0236422145726536,-0.137184880695923,
1.246421373057));
#15990=CARTESIAN_POINT('Ctrl Pts',(0.128082862902196,-0.0545291301253663,
1.2543603626943));
#15991=CARTESIAN_POINT('Ctrl Pts',(0.115272428336817,0.0780443019497631,
1.26229935233161));
#15992=CARTESIAN_POINT('Ctrl Pts',(-0.00306201423577413,0.139173524314926,
1.27023834196891));
#15993=CARTESIAN_POINT('Ctrl Pts',(-0.118593392628464,0.0728989233548558,
1.27817733160622));
#15994=CARTESIAN_POINT('Ctrl Pts',(-0.125560647806918,-0.06010964584811,
1.28611632124353));
#15995=CARTESIAN_POINT('Ctrl Pts',(-0.0175857351491984,-0.138091953858251,
1.29405531088083));
#15996=CARTESIAN_POINT('Ctrl Pts',(0.106487712804436,-0.089660542174548,
1.30199430051814));
#15997=CARTESIAN_POINT('Ctrl Pts',(0.133078957772855,0.0408489510387311,
1.30993329015544));
#15998=CARTESIAN_POINT('Ctrl Pts',(0.0378455373822902,0.133964029124136,
1.31787227979275));
#15999=CARTESIAN_POINT('Ctrl Pts',(-0.0920328787300654,0.104444219726284,
1.32581126943006));
#16000=CARTESIAN_POINT('Ctrl Pts',(-0.137661501842601,-0.0206871148492911,
1.33375025906736));
#16001=CARTESIAN_POINT('Ctrl Pts',(-0.0572704544775333,-0.126880813469472,
1.34168924870467));
#16002=CARTESIAN_POINT('Ctrl Pts',(0.0755477687720905,-0.116923823242002,
1.34962823834197));
#16003=CARTESIAN_POINT('Ctrl Pts',(0.13920718769651,6.89141801743488E-5,
1.35756722797928));
#16004=CARTESIAN_POINT('Ctrl Pts',(0.0754319660950179,0.116998564767658,
1.36550621761658));
#16005=CARTESIAN_POINT('Ctrl Pts',(-0.0573960494825499,0.126824048933643,
1.37344520725389));
#16006=CARTESIAN_POINT('Ctrl Pts',(-0.13768191782304,0.0205508058651932,
1.38138419689119));
#16007=CARTESIAN_POINT('Ctrl Pts',(-0.0919294216917856,-0.104535287252199,
1.3893231865285));
#16008=CARTESIAN_POINT('Ctrl Pts',(0.0379781508110965,-0.133926497290667,
1.39726217616581));
#16009=CARTESIAN_POINT('Ctrl Pts',(0.133119345865688,-0.0407171622080862,
1.40520116580311));
#16010=CARTESIAN_POINT('Ctrl Pts',(0.106398871137127,0.0897659150453452,
1.41314015544042));
#16011=CARTESIAN_POINT('Ctrl Pts',(-0.0177224175491345,0.138074504763813,
1.42107914507772));
#16012=CARTESIAN_POINT('Ctrl Pts',(-0.125620162573399,0.0599852426217579,
1.42901813471503));
#16013=CARTESIAN_POINT('Ctrl Pts',(-0.118521039729242,-0.0730161975746823,
1.43695712435233));
#16014=CARTESIAN_POINT('Ctrl Pts',(-0.00292444232197888,-0.139176693688359,
1.44489611398964));
#16015=CARTESIAN_POINT('Ctrl Pts',(0.115350068603298,-0.0779297424218237,
1.45283510362695));
#16016=CARTESIAN_POINT('Ctrl Pts',(0.128028003046829,0.0546551750765237,
1.46077409326425));
#16017=CARTESIAN_POINT('Ctrl Pts',(0.0235079116789307,0.137209630484779,
1.46871308290156));
#16018=CARTESIAN_POINT('Ctrl Pts',(-0.102537447198224,0.0941531272373115,
1.47665207253886));
#16019=CARTESIAN_POINT('Ctrl Pts',(-0.134706575776555,-0.0350847218495708,
1.48459106217617));
#16020=CARTESIAN_POINT('Ctrl Pts',(-0.0435804807853106,-0.132222740314769,
1.49253005181348));
#16021=CARTESIAN_POINT('Ctrl Pts',(0.0874774386997331,-0.108286040948335,
1.50046904145078));
#16022=CARTESIAN_POINT('Ctrl Pts',(0.138385550162814,0.0147146982980264,
1.50840803108809));
#16023=CARTESIAN_POINT('Ctrl Pts',(0.0627460642121078,0.124368470664037,
1.51634702072539));
#16024=CARTESIAN_POINT('Ctrl Pts',(-0.0706026869052757,0.119928391791904,
1.5242860103627));
#16025=CARTESIAN_POINT('Ctrl Pts',(-0.116004137797729,0.0441355889673283,
1.5295786701209));
#16026=CARTESIAN_POINT('Ctrl Pts',(-0.117668597464313,0.00500517689812487,
1.532225));
#16027=CARTESIAN_POINT('',(0.0684664424539461,-0.0958295198918396,0.));
#16028=CARTESIAN_POINT('Ctrl Pts',(0.0684664424539414,-0.095829519891843,
-1.38777878078145E-17));
#16029=CARTESIAN_POINT('Ctrl Pts',(0.100334321247169,-0.0730611673843044,
0.00264632987910189));
#16030=CARTESIAN_POINT('Ctrl Pts',(0.139021564822767,0.00636891437108143,
0.00793898963730573));
#16031=CARTESIAN_POINT('Ctrl Pts',(0.0699018669780613,0.120491966796142,
0.0158779792746114));
#16032=CARTESIAN_POINT('Ctrl Pts',(-0.0632645460347191,0.123954346655885,
0.0238169689119172));
#16033=CARTESIAN_POINT('Ctrl Pts',(-0.11596266760442,0.0470121293552651,
0.0293787386625077));
#16034=CARTESIAN_POINT('Ctrl Pts',(-0.117944740497024,0.00404481602818191,
0.0322941785339964));
#16035=CARTESIAN_POINT('Ctrl Pts',(-0.117917485785546,7.60014832213644E-5,
0.0325632885263832));
#16036=CARTESIAN_POINT('Ctrl Pts',(0.0635546915223951,0.132092229195826,
-2.16840434497101E-19));
#16037=CARTESIAN_POINT('Ctrl Pts',(0.0668114782730532,0.13015255741457,
-1.00603861447787E-18));
#16038=CARTESIAN_POINT('Ctrl Pts',(0.0699821360194518,0.12808121947321,
-2.9262196004085E-17));
#16039=CARTESIAN_POINT('Ctrl Pts',(0.0730575207853233,0.125877721325919,
-2.71050543121376E-17));
#16040=CARTESIAN_POINT('Ctrl Pts',(0.0789281193465506,0.121671466161783,
-2.36378102375718E-17));
#16041=CARTESIAN_POINT('Ctrl Pts',(0.0844522091809674,0.11698398814956,
1.43782932504085E-18));
#16042=CARTESIAN_POINT('Ctrl Pts',(0.0895990070394484,0.111875963994554,
9.97465998686664E-18));
#16043=CARTESIAN_POINT('Ctrl Pts',(0.0928865546640729,0.108613183302742,
1.54276111490851E-17));
#16044=CARTESIAN_POINT('Ctrl Pts',(0.0960206821069302,0.105176950779614,
-2.53636710091701E-17));
#16045=CARTESIAN_POINT('Ctrl Pts',(0.098978417360439,0.101599719103904,
-1.56125112837913E-17));
#16046=CARTESIAN_POINT('Ctrl Pts',(0.103148772110026,0.0965558852815647,
-1.86354736740503E-18));
#16047=CARTESIAN_POINT('Ctrl Pts',(0.106976174326278,0.0912251680483688,
1.1337629845105E-17));
#16048=CARTESIAN_POINT('Ctrl Pts',(0.110435561611279,0.0856523061447448,
2.03830008427275E-17));
#16049=CARTESIAN_POINT('Ctrl Pts',(0.112407683932559,0.0824753373788608,
2.55395723911076E-17));
#16050=CARTESIAN_POINT('Ctrl Pts',(0.114261188142284,0.0792174064057451,
2.29308760465575E-17));
#16051=CARTESIAN_POINT('Ctrl Pts',(0.115986535786665,0.0758936579718971,
2.08166817117217E-17));
#16052=CARTESIAN_POINT('Ctrl Pts',(0.120573220307724,0.0670577659456877,
1.51962825639422E-17));
#16053=CARTESIAN_POINT('Ctrl Pts',(0.124235263225439,0.0578042025119142,
2.52358375750583E-18));
#16054=CARTESIAN_POINT('Ctrl Pts',(0.126883306113679,0.0482911783993335,
1.30104260698261E-17));
#16055=CARTESIAN_POINT('Ctrl Pts',(0.128478610866444,0.0425600882242624,
1.93281898253259E-17));
#16056=CARTESIAN_POINT('Ctrl Pts',(0.129704960854084,0.0367345196138549,
-5.78096029915021E-19));
#16057=CARTESIAN_POINT('Ctrl Pts',(0.130533291754837,0.0308494671050701,
0.));
#16058=CARTESIAN_POINT('Ctrl Pts',(0.131003715791213,0.0275072397983871,
3.2831114661813E-19));
#16059=CARTESIAN_POINT('Ctrl Pts',(0.131345346899704,0.0241444941465381,
-1.7128612844445E-18));
#16060=CARTESIAN_POINT('Ctrl Pts',(0.131551728167405,0.0207857616715298,
2.60208521396521E-18));
#16061=CARTESIAN_POINT('Ctrl Pts',(0.131851321606701,0.0159100565018035,
8.86587880453295E-18));
#16062=CARTESIAN_POINT('Ctrl Pts',(0.131867617692795,0.0110341713389591,
-1.68111772803455E-17));
#16063=CARTESIAN_POINT('Ctrl Pts',(0.131586936334964,0.0061777758930637,
-6.93889390390723E-18));
#16064=CARTESIAN_POINT('Ctrl Pts',(0.131099036368572,-0.00226395031615145,
9.98510028643051E-18));
#16065=CARTESIAN_POINT('Ctrl Pts',(0.129715139118287,-0.0106479390144509,
1.03491660509995E-17));
#16066=CARTESIAN_POINT('Ctrl Pts',(0.127493709984164,-0.018859987399606,
1.04083408558608E-17));
#16067=CARTESIAN_POINT('Ctrl Pts',(0.126553994220251,-0.0223338732882013,
1.04333731632617E-17));
#16068=CARTESIAN_POINT('Ctrl Pts',(0.125463061762623,-0.0257782540966497,
1.75224609115742E-17));
#16069=CARTESIAN_POINT('Ctrl Pts',(0.124232565886791,-0.0291638780753137,
1.73472347597681E-17));
#16070=CARTESIAN_POINT('Ctrl Pts',(0.12170396813588,-0.0361211392462112,
1.69871551674183E-17));
#16071=CARTESIAN_POINT('Ctrl Pts',(0.118582485980247,-0.0428512226170345,
-6.45748389186585E-19));
#16072=CARTESIAN_POINT('Ctrl Pts',(0.114911168983798,-0.0492778939609075,
3.46944695195361E-18));
#16073=CARTESIAN_POINT('Ctrl Pts',(0.112347970921096,-0.0537647937721124,
6.34254691478841E-18));
#16074=CARTESIAN_POINT('Ctrl Pts',(0.109516356061708,-0.0581036184196785,
-1.05628593522785E-17));
#16075=CARTESIAN_POINT('Ctrl Pts',(0.106427098863261,-0.0622637901458048,
-1.21430643318376E-17));
#16076=CARTESIAN_POINT('Ctrl Pts',(0.104287070791936,-0.0651456752410043,
-1.32377232732828E-17));
#16077=CARTESIAN_POINT('Ctrl Pts',(0.102021590876101,-0.067943056099314,
-1.03088264066386E-17));
#16078=CARTESIAN_POINT('Ctrl Pts',(0.0996491962474235,-0.0706287444932102,
-1.04083408558608E-17));
#16079=CARTESIAN_POINT('Ctrl Pts',(0.0938611946766418,-0.0771810981592459,
-1.06511292104842E-17));
#16080=CARTESIAN_POINT('Ctrl Pts',(0.0874218747326319,-0.0830961188460978,
9.460259835177E-18));
#16081=CARTESIAN_POINT('Ctrl Pts',(0.0803902102994179,-0.0882260767030795,
2.94902990916057E-17));
#16082=CARTESIAN_POINT('Ctrl Pts',(0.0765868618375105,-0.091000813397402,
4.03243227742548E-17));
#16083=CARTESIAN_POINT('Ctrl Pts',(0.0726097989303321,-0.0935451549285004,
-2.49510848448888E-18));
#16084=CARTESIAN_POINT('Ctrl Pts',(0.0684664424539416,-0.0958295198918429,
0.));
#16085=CARTESIAN_POINT('Ctrl Pts',(-0.00156962371674571,0.146072546381438,
1.50365));
#16086=CARTESIAN_POINT('Ctrl Pts',(0.0218361081466035,0.146362061217761,
1.50238307892777));
#16087=CARTESIAN_POINT('Ctrl Pts',(0.0452966847593804,0.141345883428421,
1.50111615785553));
#16088=CARTESIAN_POINT('Ctrl Pts',(0.0660179268768178,0.130913916311315,
1.4998492367833));
#16089=CARTESIAN_POINT('Ctrl Pts',(0.109300214423576,0.109123745727819,
1.4972029069042));
#16090=CARTESIAN_POINT('Ctrl Pts',(0.140630685714559,0.0637042888941242,
1.49455657702509));
#16091=CARTESIAN_POINT('Ctrl Pts',(0.145752650840527,0.0155206226173656,
1.49191024714599));
#16092=CARTESIAN_POINT('Ctrl Pts',(0.150874615966495,-0.0326630436593903,
1.48926391726689));
#16093=CARTESIAN_POINT('Ctrl Pts',(0.129788074927449,-0.0836109193792113,
1.48661758738779));
#16094=CARTESIAN_POINT('Ctrl Pts',(0.0921021927661857,-0.114042242015571,
1.48397125750869));
#16095=CARTESIAN_POINT('Ctrl Pts',(0.0544163106049216,-0.144473564651931,
1.48132492762959));
#16096=CARTESIAN_POINT('Ctrl Pts',(0.000131087321441313,-0.154388334204831,
1.47867859775048));
#16097=CARTESIAN_POINT('Ctrl Pts',(-0.0458840977328367,-0.139228052523514,
1.47603226787138));
#16098=CARTESIAN_POINT('Ctrl Pts',(-0.0918992827871148,-0.124067770842196,
1.47338593799228));
#16099=CARTESIAN_POINT('Ctrl Pts',(-0.129644429612189,-0.0838324379266627,
1.47073960811318));
#16100=CARTESIAN_POINT('Ctrl Pts',(-0.141854649713415,-0.0369491035797489,
1.46809327823408));
#16101=CARTESIAN_POINT('Ctrl Pts',(-0.14497337938942,-0.0249741805295802,
1.46741735368415));
#16102=CARTESIAN_POINT('Ctrl Pts',(-0.146426231435716,-0.0125655473306973,
1.46674142913422));
#16103=CARTESIAN_POINT('Ctrl Pts',(-0.14631473222987,-0.000131398079681141,
1.46606550458429));
#16104=CARTESIAN_POINT('Origin',(0.,0.,-0.0924367114736175));
#16105=CARTESIAN_POINT('',(-0.0684664424539507,-0.0958295198918364,0.));
#16106=CARTESIAN_POINT('Ctrl Pts',(-0.0686146973663072,-0.0959584553529141,
8.16675286424706E-17));
#16107=CARTESIAN_POINT('Ctrl Pts',(-0.0391968190522335,-0.116741470120209,
0.00244290680874874));
#16108=CARTESIAN_POINT('Ctrl Pts',(0.0436301113039178,-0.130476273073809,
0.0075332029917574));
#16109=CARTESIAN_POINT('Ctrl Pts',(0.134092250525203,-0.0374520209666004,
0.0152708885490261));
#16110=CARTESIAN_POINT('Ctrl Pts',(0.104134301645602,0.0924305194826295,
0.023213056671806));
#16111=CARTESIAN_POINT('Ctrl Pts',(-0.0212379681243542,0.137589894578696,
0.0311552247945861));
#16112=CARTESIAN_POINT('Ctrl Pts',(-0.106685947947232,0.0723488109778776,
0.0375631097285225));
#16113=CARTESIAN_POINT('Ctrl Pts',(-0.117663533972591,0.0165813593984342,
0.041323605288199));
#16114=CARTESIAN_POINT('Ctrl Pts',(-0.117600989619072,5.04992496179954E-5,
0.0424367114736154));
#16115=CARTESIAN_POINT('Origin',(0.,0.,0.));
#16116=CARTESIAN_POINT('Ctrl Pts',(-0.0510216505388318,0.106149619882943,
-0.0164977839420939));
#16117=CARTESIAN_POINT('Ctrl Pts',(-0.0863355867949722,0.0891756983861136,
-0.0138503945678339));
#16118=CARTESIAN_POINT('Ctrl Pts',(-0.13808023131828,0.0175094743621551,
-0.00855561581931395));
#16119=CARTESIAN_POINT('Ctrl Pts',(-0.0894531427980795,-0.106808298616542,
-0.000613447696533924));
#16120=CARTESIAN_POINT('Ctrl Pts',(0.0412394829729132,-0.132934609947913,
0.00732872042624606));
#16121=CARTESIAN_POINT('Ctrl Pts',(0.134092250525203,-0.0374520209666004,
0.0152708885490261));
#16122=CARTESIAN_POINT('Ctrl Pts',(0.104134301645602,0.0924305194826295,
0.023213056671806));
#16123=CARTESIAN_POINT('Ctrl Pts',(-0.0212379681243542,0.137589894578696,
0.0311552247945861));
#16124=CARTESIAN_POINT('Ctrl Pts',(-0.127145335141994,0.0567276974868182,
0.039097392917366));
#16125=CARTESIAN_POINT('Ctrl Pts',(-0.116579117211717,-0.0761160149501382,
0.0470395610401461));
#16126=CARTESIAN_POINT('Ctrl Pts',(0.000787973702835166,-0.139222729671589,
0.054981729162926));
#16127=CARTESIAN_POINT('Ctrl Pts',(0.117431922513572,-0.0747907597173192,
0.0629238972857061));
#16128=CARTESIAN_POINT('Ctrl Pts',(0.126496838785129,0.0581591461343325,
0.070866065408486));
#16129=CARTESIAN_POINT('Ctrl Pts',(0.0196773008918215,0.137828289815661,
0.0788082335312661));
#16130=CARTESIAN_POINT('Ctrl Pts',(-0.105168479521776,0.0912330920368172,
0.0867504016540459));
#16131=CARTESIAN_POINT('Ctrl Pts',(-0.133669226619255,-0.0389412707994331,
0.0946925697768262));
#16132=CARTESIAN_POINT('Ctrl Pts',(-0.0397151780004399,-0.133441281507892,
0.102634737899606));
#16133=CARTESIAN_POINT('Ctrl Pts',(0.0906220264938673,-0.105695447092796,
0.110576906022386));
#16134=CARTESIAN_POINT('Ctrl Pts',(0.137940159127448,0.0188783162799928,
0.118519074145166));
#16135=CARTESIAN_POINT('Ctrl Pts',(0.0588909273047484,0.126157580947307,
0.126461242267946));
#16136=CARTESIAN_POINT('Ctrl Pts',(-0.074108440039672,0.117863552156501,
0.134403410390726));
#16137=CARTESIAN_POINT('Ctrl Pts',(-0.139216864956951,0.00159439502933392,
0.142345578513506));
#16138=CARTESIAN_POINT('Ctrl Pts',(-0.0767883381764272,-0.116135388594389,
0.150287746636286));
#16139=CARTESIAN_POINT('Ctrl Pts',(0.0559861945572589,-0.127473226882309,
0.158229914759066));
#16140=CARTESIAN_POINT('Ctrl Pts',(0.137471621702818,-0.0220324926503626,
0.166172082881846));
#16141=CARTESIAN_POINT('Ctrl Pts',(0.0930189202108026,0.103592267873211,
0.174114251004626));
#16142=CARTESIAN_POINT('Ctrl Pts',(-0.0366486683060043,0.134315868829211,
0.182056419127406));
#16143=CARTESIAN_POINT('Ctrl Pts',(-0.132742311638566,0.0419923350165386,
0.189998587250186));
#16144=CARTESIAN_POINT('Ctrl Pts',(-0.107230360350792,-0.0888004916405464,
0.197940755372966));
#16145=CARTESIAN_POINT('Ctrl Pts',(0.0165156171993534,-0.138242945169174,
0.205882923495746));
#16146=CARTESIAN_POINT('Ctrl Pts',(0.125131592687617,-0.061040658666823,
0.213825091618526));
#16147=CARTESIAN_POINT('Ctrl Pts',(0.119114174013628,0.0720811421096423,
0.221767259741306));
#16148=CARTESIAN_POINT('Ctrl Pts',(0.0039759348809324,0.139169211541763,
0.229709427864086));
#16149=CARTESIAN_POINT('Ctrl Pts',(-0.114804669066963,0.0787639858025777,
0.237651595986866));
#16150=CARTESIAN_POINT('Ctrl Pts',(-0.128412401817242,-0.0537971426620367,
0.245593764109646));
#16151=CARTESIAN_POINT('Ctrl Pts',(-0.024381182195918,-0.137074561658528,
0.253535932232426));
#16152=CARTESIAN_POINT('Ctrl Pts',(0.101985705091022,-0.094777599970642,
0.261478100355206));
#16153=CARTESIAN_POINT('Ctrl Pts',(0.134923209124943,0.0343453801629359,
0.269420268477986));
#16154=CARTESIAN_POINT('Ctrl Pts',(0.0442571924125319,0.132004463632409,
0.277362436600766));
#16155=CARTESIAN_POINT('Ctrl Pts',(-0.0869529592639067,0.108733897080731,
0.285304604723546));
#16156=CARTESIAN_POINT('Ctrl Pts',(-0.138505267237684,-0.0141480898545381,
0.293246772846326));
#16157=CARTESIAN_POINT('Ctrl Pts',(-0.0631725212350128,-0.124068972994571,
0.301188940969106));
#16158=CARTESIAN_POINT('Ctrl Pts',(0.0700327441786229,-0.12032993078169,
0.309131109091886));
#16159=CARTESIAN_POINT('Ctrl Pts',(0.139080821187468,-0.00635631000930847,
0.317073277214666));
#16160=CARTESIAN_POINT('Ctrl Pts',(0.0807165776729536,0.11344034374014,
0.325015445337446));
#16161=CARTESIAN_POINT('Ctrl Pts',(-0.0515923433190751,0.129313988454311,
0.332957613460226));
#16162=CARTESIAN_POINT('Ctrl Pts',(-0.136637377548019,0.026722734813544,
0.340899781583006));
#16163=CARTESIAN_POINT('Ctrl Pts',(-0.0965085366518414,-0.100349289247285,
0.348841949705786));
#16164=CARTESIAN_POINT('Ctrl Pts',(0.0320320385160992,-0.135491055083419,
0.356784117828566));
#16165=CARTESIAN_POINT('Ctrl Pts',(0.131227975626944,-0.0465090949381858,
0.364726285951346));
#16166=CARTESIAN_POINT('Ctrl Pts',(0.110205605501345,0.0850799742312894,
0.372668454074126));
#16167=CARTESIAN_POINT('Ctrl Pts',(-0.0117764211155082,0.138727046407055,
0.380610622196906));
#16168=CARTESIAN_POINT('Ctrl Pts',(-0.122970036152848,0.065285892102983,
0.388552790319686));
#16169=CARTESIAN_POINT('Ctrl Pts',(-0.121510464882371,-0.0679638464419502,
0.396494958442466));
#16170=CARTESIAN_POINT('Ctrl Pts',(-0.00873482453528946,-0.138951719454826,
0.404437126565246));
#16171=CARTESIAN_POINT('Ctrl Pts',(0.112042812448737,-0.0826455423945668,
0.412379294688026));
#16172=CARTESIAN_POINT('Ctrl Pts',(0.130177722634257,0.049372441998279,
0.420321462810806));
#16173=CARTESIAN_POINT('Ctrl Pts',(0.0290564652212241,0.136160197297018,
0.428263630933586));
#16174=CARTESIAN_POINT('Ctrl Pts',(-0.098683499418539,0.098211223603141,
0.436205799056366));
#16175=CARTESIAN_POINT('Ctrl Pts',(-0.136019240449831,-0.0297093205335648,
0.444147967179146));
#16176=CARTESIAN_POINT('Ctrl Pts',(-0.0487473834415776,-0.130413074907061,
0.452090135301926));
#16177=CARTESIAN_POINT('Ctrl Pts',(0.0831820848081396,-0.111645054821459,
0.460032303424706));
#16178=CARTESIAN_POINT('Ctrl Pts',(0.138908217753341,0.00940130521287039,
0.467974471547486));
#16179=CARTESIAN_POINT('Ctrl Pts',(0.0673801526530663,0.121835103839429,
0.475916639670265));
#16180=CARTESIAN_POINT('Ctrl Pts',(-0.0658750545035054,0.12265543075329,
0.483858807793047));
#16181=CARTESIAN_POINT('Ctrl Pts',(-0.138781944133385,0.0111107822259715,
0.491800975915825));
#16182=CARTESIAN_POINT('Ctrl Pts',(-0.084550315326251,-0.110612484274364,
0.499743144038607));
#16183=CARTESIAN_POINT('Ctrl Pts',(0.0471380885036503,-0.131003351527116,
0.507685312161385));
#16184=CARTESIAN_POINT('Ctrl Pts',(0.135643160584381,-0.031381690295376,
0.515627480284167));
#16185=CARTESIAN_POINT('Ctrl Pts',(0.0998851624184703,0.0969888232104648,
0.523569648406945));
#16186=CARTESIAN_POINT('Ctrl Pts',(-0.0273779061153799,0.136507610615132,
0.531511816529727));
#16187=CARTESIAN_POINT('Ctrl Pts',(-0.129560000008381,0.0509714027366644,
0.539453984652505));
#16188=CARTESIAN_POINT('Ctrl Pts',(-0.113051823689188,-0.0812598465397498,
0.547396152775286));
#16189=CARTESIAN_POINT('Ctrl Pts',(0.00702343738442799,-0.139048728244533,
0.555338320898066));
#16190=CARTESIAN_POINT('Ctrl Pts',(0.12066450826877,-0.0694546898587181,
0.563280489020846));
#16191=CARTESIAN_POINT('Ctrl Pts',(0.123764493242992,0.063766979789076,
0.571222657143626));
#16192=CARTESIAN_POINT('Ctrl Pts',(0.0134834875971477,0.13857154491934,
0.579164825266405));
#16193=CARTESIAN_POINT('Ctrl Pts',(-0.109149777898995,0.0864303389077871,
0.587106993389186));
#16194=CARTESIAN_POINT('Ctrl Pts',(-0.131790633456927,-0.0448899368693808,
0.595049161511966));
#16195=CARTESIAN_POINT('Ctrl Pts',(-0.0336977294021144,-0.135086418755761,
0.602991329634746));
#16196=CARTESIAN_POINT('Ctrl Pts',(0.0952657566843092,-0.101529863106778,
0.610933497757526));
#16197=CARTESIAN_POINT('Ctrl Pts',(0.136956022624868,0.025038477707157,
0.618875665880307));
#16198=CARTESIAN_POINT('Ctrl Pts',(0.0531805018142573,0.128669000640787,
0.626817834003085));
#16199=CARTESIAN_POINT('Ctrl Pts',(-0.0793138220987445,0.114425500318782,
0.634760002125867));
#16200=CARTESIAN_POINT('Ctrl Pts',(-0.139148536750765,-0.00464351367351466,
0.642702170248646));
#16201=CARTESIAN_POINT('Ctrl Pts',(-0.0715088964667609,-0.119458592094588,
0.650644338371427));
#16202=CARTESIAN_POINT('Ctrl Pts',(0.0616402393688536,-0.124837327709565,
0.658586506494205));
#16203=CARTESIAN_POINT('Ctrl Pts',(0.138320583400205,-0.0158522461166236,
0.666528674616987));
#16204=CARTESIAN_POINT('Ctrl Pts',(0.0882850628235238,0.107655121482266,
0.674470842739765));
#16205=CARTESIAN_POINT('Ctrl Pts',(-0.0426286451686149,0.132539337972556,
0.682413010862546));
#16206=CARTESIAN_POINT('Ctrl Pts',(-0.13449013477919,0.0360039045964495,
0.690355178985326));
#16207=CARTESIAN_POINT('Ctrl Pts',(-0.103144844235522,-0.0935148042116587,
0.698297347108106));
#16208=CARTESIAN_POINT('Ctrl Pts',(0.022691720100341,-0.137364345221032,
0.706239515230886));
#16209=CARTESIAN_POINT('Ctrl Pts',(0.127740337615313,-0.0553740340325759,
0.714181683353665));
#16210=CARTESIAN_POINT('Ctrl Pts',(0.115765682611161,0.077344581120379,
0.722123851476446));
#16211=CARTESIAN_POINT('Ctrl Pts',(-0.00226223072526165,0.139207614056346,
0.730066019599226));
#16212=CARTESIAN_POINT('Ctrl Pts',(-0.118217708309552,0.0735421711751344,
0.738008187722006));
#16213=CARTESIAN_POINT('Ctrl Pts',(-0.125873620115675,-0.059495455776806,
0.745950355844786));
#16214=CARTESIAN_POINT('Ctrl Pts',(-0.0182163644075178,-0.138029133036789,
0.753892523967566));
#16215=CARTESIAN_POINT('Ctrl Pts',(0.106128952536144,-0.0901139441634624,
0.761834692090347));
#16216=CARTESIAN_POINT('Ctrl Pts',(0.133249245915149,0.0403548753208232,
0.769776860213125));
#16217=CARTESIAN_POINT('Ctrl Pts',(0.0382995408207276,0.133854483197375,
0.777719028335907));
#16218=CARTESIAN_POINT('Ctrl Pts',(-0.0917364783268051,0.104729633071593,
0.785661196458685));
#16219=CARTESIAN_POINT('Ctrl Pts',(-0.137732458880487,-0.0203383202317681,
0.793603364581467));
#16220=CARTESIAN_POINT('Ctrl Pts',(-0.0575513573065257,-0.126774282767806,
0.801545532704245));
#16221=CARTESIAN_POINT('Ctrl Pts',(0.0753527000357912,-0.117071978271622,
0.809487700827026));
#16222=CARTESIAN_POINT('Ctrl Pts',(0.139225942868322,-0.000119714417332432,
0.817429868949805));
#16223=CARTESIAN_POINT('Ctrl Pts',(0.0755539188089132,0.116942220141962,
0.825372037072586));
#16224=CARTESIAN_POINT('Ctrl Pts',(-0.0573332568284509,0.12687306712048,
0.833314205195366));
#16225=CARTESIAN_POINT('Ctrl Pts',(-0.13769727914169,0.0205751504512258,
0.841256373318145));
#16226=CARTESIAN_POINT('Ctrl Pts',(-0.0919164475821765,-0.104571717796869,
0.849198541440926));
#16227=CARTESIAN_POINT('Ctrl Pts',(0.0380692928980519,-0.133920149482284,
0.857140709563706));
#16228=CARTESIAN_POINT('Ctrl Pts',(0.133179650076608,-0.0405839661022353,
0.865082877686486));
#16229=CARTESIAN_POINT('Ctrl Pts',(0.106283765719693,0.0899312995767124,
0.873025045809266));
#16230=CARTESIAN_POINT('Ctrl Pts',(-0.0179789669825735,0.138060255849953,
0.880967213932046));
#16231=CARTESIAN_POINT('Ctrl Pts',(-0.125771118879347,0.0597118342956578,
0.888909382054826));
#16232=CARTESIAN_POINT('Ctrl Pts',(-0.118344004924669,-0.0733387619032726,
0.896851550177606));
#16233=CARTESIAN_POINT('Ctrl Pts',(-0.00250162451743248,-0.139203517821528,
0.904793718300386));
#16234=CARTESIAN_POINT('Ctrl Pts',(0.115632500949424,-0.0775435504945224,
0.912735886423165));
#16235=CARTESIAN_POINT('Ctrl Pts',(0.127835376168433,0.0551542754370876,
0.920678054545947));
#16236=CARTESIAN_POINT('Ctrl Pts',(0.0229279137899797,0.137325118854324,
0.928620222668725));
#16237=CARTESIAN_POINT('Ctrl Pts',(-0.102983873094174,0.0936920454555137,
0.936562390791507));
#16238=CARTESIAN_POINT('Ctrl Pts',(-0.134551852288801,-0.0357725669300891,
0.944504558914285));
#16239=CARTESIAN_POINT('Ctrl Pts',(-0.0428565117498991,-0.132465832952297,
0.952446727037066));
#16240=CARTESIAN_POINT('Ctrl Pts',(0.0880997963686447,-0.107806787258123,
0.960388895159846));
#16241=CARTESIAN_POINT('Ctrl Pts',(0.138347640177547,0.0156143509765511,
0.968331063282625));
#16242=CARTESIAN_POINT('Ctrl Pts',(0.061854832590724,0.124731139593481,
0.976273231405407));
#16243=CARTESIAN_POINT('Ctrl Pts',(-0.0713033562375951,0.119581390225944,
0.984215399528185));
#16244=CARTESIAN_POINT('Ctrl Pts',(-0.139140345480169,0.00488280234845834,
0.992157567650966));
#16245=CARTESIAN_POINT('Ctrl Pts',(-0.0795104838321055,-0.114288934109561,
1.00009973577375));
#16246=CARTESIAN_POINT('Ctrl Pts',(0.0529591494285269,-0.128760265574912,
1.00804190389653));
#16247=CARTESIAN_POINT('Ctrl Pts',(0.136912761112491,-0.0252739657289669,
1.0159840720193));
#16248=CARTESIAN_POINT('Ctrl Pts',(0.0954402180350474,0.101365883217864,
1.02392624014209));
#16249=CARTESIAN_POINT('Ctrl Pts',(-0.0334653697086341,0.135144169424284,
1.03186840826486));
#16250=CARTESIAN_POINT('Ctrl Pts',(-0.131713240771149,0.0451165125500212,
1.03981057638765));
#16251=CARTESIAN_POINT('Ctrl Pts',(-0.109298251871946,-0.0862425048155002,
1.04775274451043));
#16252=CARTESIAN_POINT('Ctrl Pts',(0.0132451643780021,-0.13859452774087,
1.05569491263321));
#16253=CARTESIAN_POINT('Ctrl Pts',(0.123654649330263,-0.0639797248987874,
1.06363708075599));
#16254=CARTESIAN_POINT('Ctrl Pts',(0.120783771971213,0.0692470788374567,
1.07157924887876));
#16255=CARTESIAN_POINT('Ctrl Pts',(0.00726255089817806,0.139036444335888,
1.07952141700155));
#16256=CARTESIAN_POINT('Ctrl Pts',(-0.112911912907791,0.0814541430660127,
1.08746358512433));
#16257=CARTESIAN_POINT('Ctrl Pts',(-0.129647464608677,-0.0507485213543897,
1.09540575324711));
#16258=CARTESIAN_POINT('Ctrl Pts',(-0.0276126195379174,-0.136460326620484,
1.10334792136989));
#16259=CARTESIAN_POINT('Ctrl Pts',(0.0997182217817603,-0.0971604536002107,
1.11129008949267));
#16260=CARTESIAN_POINT('Ctrl Pts',(0.135696927507188,0.0311483765905046,
1.11923225761545));
#16261=CARTESIAN_POINT('Ctrl Pts',(0.0473633069609982,0.130922093830007,
1.12717442573822));
#16262=CARTESIAN_POINT('Ctrl Pts',(-0.0843599685788644,0.110757722983492,
1.13511659386101));
#16263=CARTESIAN_POINT('Ctrl Pts',(-0.138800846271631,-0.0108721006891078,
1.14305876198379));
#16264=CARTESIAN_POINT('Ctrl Pts',(-0.0660858892268601,-0.122541963197144,
1.15100093010657));
#16265=CARTESIAN_POINT('Ctrl Pts',(0.0671705316110708,-0.121950798202395,
1.15894309822935));
#16266=CARTESIAN_POINT('Ctrl Pts',(0.138891844802359,-0.00964017357273747,
1.16688526635212));
#16267=CARTESIAN_POINT('Ctrl Pts',(0.0833739592533277,0.111501840422208,
1.17482743447491));
#16268=CARTESIAN_POINT('Ctrl Pts',(-0.0485230383040216,0.130496713571114,
1.18276960259768));
#16269=CARTESIAN_POINT('Ctrl Pts',(-0.135967947813762,0.0299431906521225,
1.19071177072047));
#16270=CARTESIAN_POINT('Ctrl Pts',(-0.0988522486080867,-0.0980413710850678,
1.19865393884324));
#16271=CARTESIAN_POINT('Ctrl Pts',(0.0288222657999454,-0.136209964735594,
1.20659610696603));
#16272=CARTESIAN_POINT('Ctrl Pts',(0.130092623711363,-0.0495962373069701,
1.21453827508881));
#16273=CARTESIAN_POINT('Ctrl Pts',(0.112184773380136,0.082452738709893,
1.22248044321158));
#16274=CARTESIAN_POINT('Ctrl Pts',(-0.00849585454694533,0.138966535376798,
1.23042261133437));
#16275=CARTESIAN_POINT('Ctrl Pts',(-0.121393406896754,0.0681727090639588,
1.23836477945715));
#16276=CARTESIAN_POINT('Ctrl Pts',(-0.123082127310551,-0.0650743223999996,
1.24630694757992));
#16277=CARTESIAN_POINT('Ctrl Pts',(-0.0120149744006178,-0.138706589206355,
1.25424911570271));
#16278=CARTESIAN_POINT('Ctrl Pts',(0.110059129405696,-0.0852693704304675,
1.26219128382548));
#16279=CARTESIAN_POINT('Ctrl Pts',(0.13130776387206,0.0462833517151888,
1.27013345194827));
#16280=CARTESIAN_POINT('Ctrl Pts',(0.0322649968732001,0.135435768819968,
1.27807562007105));
#16281=CARTESIAN_POINT('Ctrl Pts',(-0.0963358219719167,0.100515107841202,
1.28601778819382));
#16282=CARTESIAN_POINT('Ctrl Pts',(-0.136683130933199,-0.0264877182308561,
1.29395995631661));
#16283=CARTESIAN_POINT('Ctrl Pts',(-0.0518146499729274,-0.129225073214149,
1.30190212443939));
#16284=CARTESIAN_POINT('Ctrl Pts',(0.0805213734929343,-0.11357898534207,
1.30984429256217));
#16285=CARTESIAN_POINT('Ctrl Pts',(0.1390915465469,0.0061171215252809,1.31778646068495));
#16286=CARTESIAN_POINT('Ctrl Pts',(0.0702395735793815,0.120209316621791,
1.32572862880773));
#16287=CARTESIAN_POINT('Ctrl Pts',(-0.0629590648350173,0.124177428154433,
1.33367079693051));
#16288=CARTESIAN_POINT('Ctrl Pts',(-0.138480731711197,0.0143862582011507,
1.34161296505328));
#16289=CARTESIAN_POINT('Ctrl Pts',(-0.0871398218994898,-0.108584202098263,
1.34955513317607));
#16290=CARTESIAN_POINT('Ctrl Pts',(0.0440301174146577,-0.132080378229483,
1.35749730129884));
#16291=CARTESIAN_POINT('Ctrl Pts',(0.13486394497766,-0.0345773583278084,
1.36543946942163));
#16292=CARTESIAN_POINT('Ctrl Pts',(0.102148545386143,0.0946020732301706,
1.3733816375444));
#16293=CARTESIAN_POINT('Ctrl Pts',(-0.0241454188302812,0.137116288461919,
1.38132380566719));
#16294=CARTESIAN_POINT('Ctrl Pts',(-0.128319693277533,0.0540178939468163,
1.38926597378996));
#16295=CARTESIAN_POINT('Ctrl Pts',(-0.114939956470138,-0.0785664351508689,
1.39720814191275));
#16296=CARTESIAN_POINT('Ctrl Pts',(0.00373660876362508,-0.139175849115243,
1.40515031003553));
#16297=CARTESIAN_POINT('Ctrl Pts',(0.118990018389619,-0.0722858665142316,
1.41309247815831));
#16298=CARTESIAN_POINT('Ctrl Pts',(0.125236419206141,0.0608253567263532,
1.42103464628109));
#16299=CARTESIAN_POINT('Ctrl Pts',(0.0167532566496359,0.13821437898841,
1.42897681440387));
#16300=CARTESIAN_POINT('Ctrl Pts',(-0.107077349343502,0.0889846891406984,
1.43691898252665));
#16301=CARTESIAN_POINT('Ctrl Pts',(-0.132814597987359,-0.0417638487589672,
1.44486115064943));
#16302=CARTESIAN_POINT('Ctrl Pts',(-0.0368790902657646,-0.134252921254984,
1.45280331877221));
#16303=CARTESIAN_POINT('Ctrl Pts',(0.0928396680879532,-0.103751556080299,
1.46074548689499));
#16304=CARTESIAN_POINT('Ctrl Pts',(0.137511141307062,0.0217950526079239,
1.46868765501776));
#16305=CARTESIAN_POINT('Ctrl Pts',(0.0562018483347667,0.127378648737854,
1.47662982314055));
#16306=CARTESIAN_POINT('Ctrl Pts',(-0.0765818961642769,0.116263681173923,
1.48457199126332));
#16307=CARTESIAN_POINT('Ctrl Pts',(-0.13923195096087,-0.00134816270381636,
1.49251415938611));
#16308=CARTESIAN_POINT('Ctrl Pts',(-0.0742871760264013,-0.117748889605885,
1.50045632750888));
#16309=CARTESIAN_POINT('Ctrl Pts',(0.0586284551779338,-0.126233948370975,
1.50839849563167));
#16310=CARTESIAN_POINT('Ctrl Pts',(0.137995068118234,-0.019163470063063,
1.51634066375444));
#16311=CARTESIAN_POINT('Ctrl Pts',(0.0906261803825392,0.105639137646141,
1.52428283187723));
#16312=CARTESIAN_POINT('Ctrl Pts',(0.00417072711528833,0.124051375507138,
1.52957761062575));
#16313=CARTESIAN_POINT('Ctrl Pts',(-0.0334019664627544,0.1129391839063,
1.53222500000001));
#16314=CARTESIAN_POINT('Ctrl Pts',(-0.0551480035117261,0.114734422509858,
-0.0109985226280628));
#16315=CARTESIAN_POINT('Ctrl Pts',(-0.093317938433455,0.0963877427684319,
-0.00835113325380276));
#16316=CARTESIAN_POINT('Ctrl Pts',(-0.149247407742026,0.0189255452031589,
-0.00305635450528277));
#16317=CARTESIAN_POINT('Ctrl Pts',(-0.0966876253720675,-0.115446371588928,
0.00488581361749726));
#16318=CARTESIAN_POINT('Ctrl Pts',(0.0445747075563756,-0.143685636564375,
0.0128279817402772));
#16319=CARTESIAN_POINT('Ctrl Pts',(0.144936900801175,-0.0404809362687151,
0.0207701498630572));
#16320=CARTESIAN_POINT('Ctrl Pts',(0.112556116319125,0.0999057960529736,
0.0287123179858373));
#16321=CARTESIAN_POINT('Ctrl Pts',(-0.0229555792165621,0.148717415239805,
0.0366544861086172));
#16322=CARTESIAN_POINT('Ctrl Pts',(-0.137428156769908,0.0613155244327884,
0.0445966542313972));
#16323=CARTESIAN_POINT('Ctrl Pts',(-0.126007400730642,-0.0822718633254329,
0.0525388223541772));
#16324=CARTESIAN_POINT('Ctrl Pts',(0.000851700720621877,-0.150482305134309,
0.0604809904769572));
#16325=CARTESIAN_POINT('Ctrl Pts',(0.126929176276611,-0.0808394286734405,
0.0684231585997372));
#16326=CARTESIAN_POINT('Ctrl Pts',(0.136727213562698,0.0628627408439891,
0.0763653267225173));
#16327=CARTESIAN_POINT('Ctrl Pts',(0.0212686937255662,0.148975090584026,
0.0843074948452972));
#16328=CARTESIAN_POINT('Ctrl Pts',(-0.113673932864549,0.0986115272026031,
0.0922496629680772));
#16329=CARTESIAN_POINT('Ctrl Pts',(-0.144479665027646,-0.0420906285100245,
0.100191831090857));
#16330=CARTESIAN_POINT('Ctrl Pts',(-0.0429271251068198,-0.144233284958223,
0.108133999213637));
#16331=CARTESIAN_POINT('Ctrl Pts',(0.0979510420095061,-0.114243518700172,
0.116076167336417));
#16332=CARTESIAN_POINT('Ctrl Pts',(0.149096007275942,0.0204050915936607,
0.124018335459197));
#16333=CARTESIAN_POINT('Ctrl Pts',(0.0636537044864716,0.136360518400275,
0.131960503581977));
#16334=CARTESIAN_POINT('Ctrl Pts',(-0.0801019266996435,0.127395713772213,
0.139902671704757));
#16335=CARTESIAN_POINT('Ctrl Pts',(-0.15047596611352,0.00172334100814176,
0.147844839827537));
#16336=CARTESIAN_POINT('Ctrl Pts',(-0.0829985603893774,-0.125527785761544,
0.155787007950317));
#16337=CARTESIAN_POINT('Ctrl Pts',(0.0605140527882773,-0.137782566606816,
0.163729176073097));
#16338=CARTESIAN_POINT('Ctrl Pts',(0.148589577098441,-0.0238143605552183,
0.171671344195877));
#16339=CARTESIAN_POINT('Ctrl Pts',(0.100541783424623,0.111970245809892,
0.179613512318657));
#16340=CARTESIAN_POINT('Ctrl Pts',(-0.0396126128240685,0.145178604134651,
0.187555680441437));
#16341=CARTESIAN_POINT('Ctrl Pts',(-0.143477786216001,0.0453884461694337,
0.195497848564217));
#16342=CARTESIAN_POINT('Ctrl Pts',(-0.115902567375552,-0.095982191346566,
0.203440016686997));
#16343=CARTESIAN_POINT('Ctrl Pts',(0.0178513102906219,-0.149423281002214,
0.211382184809777));
#16344=CARTESIAN_POINT('Ctrl Pts',(0.135251553802876,-0.0659772944027704,
0.219324352932557));
#16345=CARTESIAN_POINT('Ctrl Pts',(0.128747479107914,0.07791067196398,0.227266521055337));
#16346=CARTESIAN_POINT('Ctrl Pts',(0.00429748682099232,0.150424458749874,
0.235208689178117));
#16347=CARTESIAN_POINT('Ctrl Pts',(-0.124089444892588,0.0851339876261335,
0.243150857300897));
#16348=CARTESIAN_POINT('Ctrl Pts',(-0.138797696890977,-0.0581479623084488,
0.251093025423677));
#16349=CARTESIAN_POINT('Ctrl Pts',(-0.0263529993083425,-0.148160405002171,
0.259035193546457));
#16350=CARTESIAN_POINT('Ctrl Pts',(0.110233752987369,-0.102442695616748,
0.266977361669237));
#16351=CARTESIAN_POINT('Ctrl Pts',(0.145835062802846,0.0371230472913779,
0.274919529792017));
#16352=CARTESIAN_POINT('Ctrl Pts',(0.0478364728857143,0.142680265085169,
0.282861697914797));
#16353=CARTESIAN_POINT('Ctrl Pts',(-0.0939852406223356,0.117527701960322,
0.290803866037577));
#16354=CARTESIAN_POINT('Ctrl Pts',(-0.14970681824969,-0.01529231023972,
0.298746034160357));
#16355=CARTESIAN_POINT('Ctrl Pts',(-0.0682815703945392,-0.134102995221473,
0.306688202283137));
#16356=CARTESIAN_POINT('Ctrl Pts',(0.0756966107742644,-0.1300615596562,
0.314630370405917));
#16357=CARTESIAN_POINT('Ctrl Pts',(0.150328919865546,-0.00687037371415525,
0.322572538528697));
#16358=CARTESIAN_POINT('Ctrl Pts',(0.0872444944832666,0.122614780370367,
0.330514706651477));
#16359=CARTESIAN_POINT('Ctrl Pts',(-0.0557648508131485,0.139772198940638,
0.338456874774257));
#16360=CARTESIAN_POINT('Ctrl Pts',(-0.147687863823926,0.0288839239377102,
0.346399042897038));
#16361=CARTESIAN_POINT('Ctrl Pts',(-0.104313621021262,-0.10846499275041,
0.354341211019817));
#16362=CARTESIAN_POINT('Ctrl Pts',(0.0346226151823369,-0.146448833047075,
0.362283379142597));
#16363=CARTESIAN_POINT('Ctrl Pts',(0.141840978962514,-0.0502704970123603,
0.370225547265377));
#16364=CARTESIAN_POINT('Ctrl Pts',(0.119118434135606,0.0919607787700563,
0.378167715388157));
#16365=CARTESIAN_POINT('Ctrl Pts',(-0.0127288338612142,0.149946533709345,
0.386109883510937));
#16366=CARTESIAN_POINT('Ctrl Pts',(-0.132915182358376,0.070565859178174,
0.394052051633717));
#16367=CARTESIAN_POINT('Ctrl Pts',(-0.131337568919768,-0.0734603918663599,
0.401994219756497));
#16368=CARTESIAN_POINT('Ctrl Pts',(-0.00944124952954395,-0.150189377088511,
0.409936387879277));
#16369=CARTESIAN_POINT('Ctrl Pts',(0.121104224366159,-0.0893294633566384,
0.417878556002057));
#16370=CARTESIAN_POINT('Ctrl Pts',(0.140705787232781,0.0533654159743681,
0.425820724124838));
#16371=CARTESIAN_POINT('Ctrl Pts',(0.0314063937394313,0.147172091835368,
0.433762892247617));
#16372=CARTESIAN_POINT('Ctrl Pts',(-0.106664482920656,0.106154012011714,
0.441705060370398));
#16373=CARTESIAN_POINT('Ctrl Pts',(-0.147019735166745,-0.032112048430678,
0.449647228493177));
#16374=CARTESIAN_POINT('Ctrl Pts',(-0.052689806088835,-0.14096017351449,
0.457589396615958));
#16375=CARTESIAN_POINT('Ctrl Pts',(0.0899093983958942,-0.120674298270189,
0.465531564738737));
#16376=CARTESIAN_POINT('Ctrl Pts',(0.15014235720654,0.0101616315312987,
0.473473732861518));
#16377=CARTESIAN_POINT('Ctrl Pts',(0.0728294921055832,0.131688462906045,
0.481415900984297));
#16378=CARTESIAN_POINT('Ctrl Pts',(-0.071202669822089,0.132575133389036,
0.489358069107078));
#16379=CARTESIAN_POINT('Ctrl Pts',(-0.150005871264529,0.012009361726732,
0.497300237229857));
#16380=CARTESIAN_POINT('Ctrl Pts',(-0.0913882839399832,-0.119558219045865,
0.505242405352637));
#16381=CARTESIAN_POINT('Ctrl Pts',(0.0509503601487159,-0.141598188489932,
0.513184573475417));
#16382=CARTESIAN_POINT('Ctrl Pts',(0.146613240011817,-0.0339196703426114,
0.521126741598197));
#16383=CARTESIAN_POINT('Ctrl Pts',(0.107963329873666,0.104832750538675,
0.529068909720978));
#16384=CARTESIAN_POINT('Ctrl Pts',(-0.0295920819230583,0.147547602048875,
0.537011077843756));
#16385=CARTESIAN_POINT('Ctrl Pts',(-0.140038106568177,0.055093691941219,
0.544953245966537));
#16386=CARTESIAN_POINT('Ctrl Pts',(-0.122194838935542,-0.0878316999746162,
0.552895414089317));
#16387=CARTESIAN_POINT('Ctrl Pts',(0.00759145471482065,-0.150294231420327,
0.560837582212097));
#16388=CARTESIAN_POINT('Ctrl Pts',(0.130423195946632,-0.0750718065719766,
0.568779750334878));
#16389=CARTESIAN_POINT('Ctrl Pts',(0.133773890807325,0.0689241055160235,
0.576721918457657));
#16390=CARTESIAN_POINT('Ctrl Pts',(0.0145739585745413,0.149778456108953,
0.584664086580438));
#16391=CARTESIAN_POINT('Ctrl Pts',(-0.117977216952174,0.0934203535806499,
0.592606254703216));
#16392=CARTESIAN_POINT('Ctrl Pts',(-0.142449141490696,-0.0485203902651028,
0.600548422825998));
#16393=CARTESIAN_POINT('Ctrl Pts',(-0.036423018067407,-0.146011471938939,
0.608490590948776));
#16394=CARTESIAN_POINT('Ctrl Pts',(0.102970331784443,-0.109741044988262,
0.616432759071558));
#16395=CARTESIAN_POINT('Ctrl Pts',(0.148032279177632,0.0270634532975707,
0.624374927194337));
#16396=CARTESIAN_POINT('Ctrl Pts',(0.0574814509102497,0.139075048028633,
0.632317095317117));
#16397=CARTESIAN_POINT('Ctrl Pts',(-0.0857282916847416,0.123679611042927,
0.640259263439898));
#16398=CARTESIAN_POINT('Ctrl Pts',(-0.150402111894479,-0.00501905574730406,
0.648201431562677));
#16399=CARTESIAN_POINT('Ctrl Pts',(-0.0772921462128499,-0.129119751845818,
0.656143599685457));
#16400=CARTESIAN_POINT('Ctrl Pts',(0.0666253659236285,-0.134933490277457,
0.664085767808237));
#16401=CARTESIAN_POINT('Ctrl Pts',(0.14950719819016,-0.0171342893707992,
0.672027935931017));
#16402=CARTESIAN_POINT('Ctrl Pts',(0.0954250774564579,0.11636168087194,
0.679970104053797));
#16403=CARTESIAN_POINT('Ctrl Pts',(-0.0460762176180427,0.143258397146306,
0.687912272176577));
#16404=CARTESIAN_POINT('Ctrl Pts',(-0.145366963764729,0.0389157041403328,
0.695854440299358));
#16405=CARTESIAN_POINT('Ctrl Pts',(-0.111486636987321,-0.101077771820372,
0.703796608422136));
#16406=CARTESIAN_POINT('Ctrl Pts',(0.02452690272786,-0.148473624679578,
0.711738776544918));
#16407=CARTESIAN_POINT('Ctrl Pts',(0.138071279799868,-0.0598523840572839,
0.719680944667696));
#16408=CARTESIAN_POINT('Ctrl Pts',(0.125128179973684,0.0835997892305201,
0.727623112790477));
#16409=CARTESIAN_POINT('Ctrl Pts',(-0.00244518761474098,0.150465967050502,
0.735565280913257));
#16410=CARTESIAN_POINT('Ctrl Pts',(-0.127778512144395,0.0794898610961098,
0.743507449036036));
#16411=CARTESIAN_POINT('Ctrl Pts',(-0.136053592364468,-0.0643071239260258,
0.751449617158818));
#16412=CARTESIAN_POINT('Ctrl Pts',(-0.019689604662082,-0.149192176910068,
0.759391785281597));
#16413=CARTESIAN_POINT('Ctrl Pts',(0.114712083700712,-0.0974018687498071,
0.767333953404378));
#16414=CARTESIAN_POINT('Ctrl Pts',(0.144025718573537,0.0436185576594447,
0.775276121527157));
#16415=CARTESIAN_POINT('Ctrl Pts',(0.0413969989087525,0.14467990414796,
0.783218289649938));
#16416=CARTESIAN_POINT('Ctrl Pts',(-0.0991556246317344,0.113199594905656,
0.791160457772717));
#16417=CARTESIAN_POINT('Ctrl Pts',(-0.148871509365196,-0.021983172706469,
0.799102625895497));
#16418=CARTESIAN_POINT('Ctrl Pts',(-0.062205797368885,-0.137027095702329,
0.807044794018277));
#16419=CARTESIAN_POINT('Ctrl Pts',(0.081446815661698,-0.126540121706451,
0.814986962141057));
#16420=CARTESIAN_POINT('Ctrl Pts',(0.150485778196879,-0.000129396266831759,
0.822929130263837));
#16421=CARTESIAN_POINT('Ctrl Pts',(0.0816643079123276,0.126399869446589,
0.830871298386618));
#16422=CARTESIAN_POINT('Ctrl Pts',(-0.0619700581130299,0.137133869194964,
0.838813466509397));
#16423=CARTESIAN_POINT('Ctrl Pts',(-0.148833484480893,0.0222391564630926,
0.846755634632177));
#16424=CARTESIAN_POINT('Ctrl Pts',(-0.0993501488194509,-0.113028908304323,
0.854697802754957));
#16425=CARTESIAN_POINT('Ctrl Pts',(0.041148129789194,-0.144750881164039,
0.862639970877736));
#16426=CARTESIAN_POINT('Ctrl Pts',(0.143950494202948,-0.0438661760544617,
0.870582139000517));
#16427=CARTESIAN_POINT('Ctrl Pts',(0.114879417330645,0.0972044528644933,
0.878524307123298));
#16428=CARTESIAN_POINT('Ctrl Pts',(-0.0194330078274841,0.149225816766708,
0.886466475246077));
#16429=CARTESIAN_POINT('Ctrl Pts',(-0.135942801386891,0.0645410019599824,
0.894408643368857));
#16430=CARTESIAN_POINT('Ctrl Pts',(-0.127915022941288,-0.0792700011911429,
0.902350811491637));
#16431=CARTESIAN_POINT('Ctrl Pts',(-0.00270394227186439,-0.150461539534541,
0.910292979614417));
#16432=CARTESIAN_POINT('Ctrl Pts',(0.124984227305131,-0.0838148501630433,
0.918235147737197));
#16433=CARTESIAN_POINT('Ctrl Pts',(0.138174004553101,0.0596148525845174,
0.926177315859977));
#16434=CARTESIAN_POINT('Ctrl Pts',(0.0247821984756025,0.148431225898158,
0.934119483982757));
#16435=CARTESIAN_POINT('Ctrl Pts',(-0.11131264737753,0.101269347369872,
0.942061652105537));
#16436=CARTESIAN_POINT('Ctrl Pts',(-0.145433672650089,-0.0386656571445607,
0.950003820228317));
#16437=CARTESIAN_POINT('Ctrl Pts',(-0.0463225128062989,-0.143178947440692,
0.957945988351097));
#16438=CARTESIAN_POINT('Ctrl Pts',(0.0952248276606132,-0.116525612549003,
0.965888156473877));
#16439=CARTESIAN_POINT('Ctrl Pts',(0.149536443172165,0.0168771545685866,
0.973830324596656));
#16440=CARTESIAN_POINT('Ctrl Pts',(0.0668573142755158,0.134818714245386,
0.981772492719438));
#16441=CARTESIAN_POINT('Ctrl Pts',(-0.0770699830103684,0.129252481220654,
0.989714660842216));
#16442=CARTESIAN_POINT('Ctrl Pts',(-0.15039325815857,0.00527769678589187,
0.997656828964997));
#16443=CARTESIAN_POINT('Ctrl Pts',(-0.0859408583470751,-0.123532000103139,
1.00559899708778));
#16444=CARTESIAN_POINT('Ctrl Pts',(0.0572421967501742,-0.139173693973137,
1.01354116521056));
#16445=CARTESIAN_POINT('Ctrl Pts',(0.147985518909957,-0.0273179863069172,
1.02148333333334));
#16446=CARTESIAN_POINT('Ctrl Pts',(0.103158902618224,0.109563803299803,
1.02942550145612));
#16447=CARTESIAN_POINT('Ctrl Pts',(-0.0361718663885326,0.146073893166727,
1.0373676695789));
#16448=CARTESIAN_POINT('Ctrl Pts',(-0.142365489706367,0.0487652901517079,
1.04530983770168));
#16449=CARTESIAN_POINT('Ctrl Pts',(-0.118137698690712,-0.0932173284908804,
1.05325200582446));
#16450=CARTESIAN_POINT('Ctrl Pts',(0.0143163610725534,-0.149803297655807,
1.06119417394724));
#16451=CARTESIAN_POINT('Ctrl Pts',(0.133655163317704,-0.0691540562905145,
1.06913634207002));
#16452=CARTESIAN_POINT('Ctrl Pts',(0.130552105047211,0.0748474051030229,
1.0770785101928));
#16453=CARTESIAN_POINT('Ctrl Pts',(0.0078499064261323,0.150280954056111,
1.08502067831558));
#16454=CARTESIAN_POINT('Ctrl Pts',(-0.122043612932812,0.0880417101447944,
1.09296284643836));
#16455=CARTESIAN_POINT('Ctrl Pts',(-0.140132644828567,-0.0548527851276936,
1.10090501456114));
#16456=CARTESIAN_POINT('Ctrl Pts',(-0.0298457776877653,-0.147496493982489,
1.10884718268392));
#16457=CARTESIAN_POINT('Ctrl Pts',(0.107782887988268,-0.10501826145877,
1.1167893508067));
#16458=CARTESIAN_POINT('Ctrl Pts',(0.146671355310253,0.033667487497105,
1.12473151892948));
#16459=CARTESIAN_POINT('Ctrl Pts',(0.0511937930472066,0.141510359113225,
1.13267368705226));
#16460=CARTESIAN_POINT('Ctrl Pts',(-0.0911825429852659,0.119715203870077,
1.14061585517504));
#16461=CARTESIAN_POINT('Ctrl Pts',(-0.150026302104679,-0.0117513769282424,
1.14855802329782));
#16462=CARTESIAN_POINT('Ctrl Pts',(-0.0714305557085884,-0.132452489195471,
1.1565001914206));
#16463=CARTESIAN_POINT('Ctrl Pts',(0.0726029180563751,-0.131813513998426,
1.16444235954338));
#16464=CARTESIAN_POINT('Ctrl Pts',(0.150124660100533,-0.010419818262018,
1.17238452766616));
#16465=CARTESIAN_POINT('Ctrl Pts',(0.0901167906002831,0.120519501471002,
1.18032669578894));
#16466=CARTESIAN_POINT('Ctrl Pts',(-0.0524473171394798,0.141050576417769,
1.18826886391172));
#16467=CARTESIAN_POINT('Ctrl Pts',(-0.146964294261872,0.0323648326895764,
1.1962110320345));
#16468=CARTESIAN_POINT('Ctrl Pts',(-0.106846879624786,-0.105970422747861,
1.20415320015727));
#16469=CARTESIAN_POINT('Ctrl Pts',(0.0311532535456026,-0.14722588419309,
1.21209536828006));
#16470=CARTESIAN_POINT('Ctrl Pts',(0.140613805972886,-0.0536073106276968,
1.22003753640283));
#16471=CARTESIAN_POINT('Ctrl Pts',(0.121257666323848,0.0891210667609394,
1.22797970452562));
#16472=CARTESIAN_POINT('Ctrl Pts',(-0.00918295295119051,0.150205391241489,
1.2359218726484));
#16473=CARTESIAN_POINT('Ctrl Pts',(-0.131211043922368,0.0736861461587066,
1.24386404077118));
#16474=CARTESIAN_POINT('Ctrl Pts',(-0.133036338837895,-0.0703371788708997,
1.25180620889396));
#16475=CARTESIAN_POINT('Ctrl Pts',(-0.0129866800356469,-0.149924422041766,
1.25974837701674));
#16476=CARTESIAN_POINT('Ctrl Pts',(0.118960111851797,-0.0921654923014072,
1.26769054513952));
#16477=CARTESIAN_POINT('Ctrl Pts',(0.141927220045961,0.050026496908035,
1.2756327132623));
#16478=CARTESIAN_POINT('Ctrl Pts',(0.0348744139414821,0.146389075532006,
1.28357488138508));
#16479=CARTESIAN_POINT('Ctrl Pts',(-0.104126938119509,0.108644221848311,
1.29151704950786));
#16480=CARTESIAN_POINT('Ctrl Pts',(-0.147737317493493,-0.0286299004949125,
1.29945921763064));
#16481=CARTESIAN_POINT('Ctrl Pts',(-0.0560051364173496,-0.139676092720537,
1.30740138575342));
#16482=CARTESIAN_POINT('Ctrl Pts',(0.0870335032532438,-0.122764634549313,
1.3153435538762));
#16483=CARTESIAN_POINT('Ctrl Pts',(0.150340512633584,0.00661184096937889,
1.32328572199898));
#16484=CARTESIAN_POINT('Ctrl Pts',(0.0759201674095095,0.129931190880528,
1.33122789012176));
#16485=CARTESIAN_POINT('Ctrl Pts',(-0.0680508508044829,0.134220221643466,
1.33917005824454));
#16486=CARTESIAN_POINT('Ctrl Pts',(-0.149680298423566,0.0155497403439283,
1.34711222636732));
#16487=CARTESIAN_POINT('Ctrl Pts',(-0.0941872156892785,-0.117365900463673,
1.3550543944901));
#16488=CARTESIAN_POINT('Ctrl Pts',(0.0475910332998192,-0.142762319241037,
1.36299656261288));
#16489=CARTESIAN_POINT('Ctrl Pts',(0.145771005694385,-0.0373737865856905,
1.37093873073566));
#16490=CARTESIAN_POINT('Ctrl Pts',(0.110409762917901,0.10225297323032,1.37888089885844));
#16491=CARTESIAN_POINT('Ctrl Pts',(-0.0260981686868614,0.148205506441964,
1.38682306698121));
#16492=CARTESIAN_POINT('Ctrl Pts',(-0.138697490589939,0.0583865667538053,
1.394765235104));
#16493=CARTESIAN_POINT('Ctrl Pts',(-0.124235673603468,-0.0849204601545819,
1.40270740322677));
#16494=CARTESIAN_POINT('Ctrl Pts',(0.0040388053119065,-0.150431633134115,
1.41064957134956));
#16495=CARTESIAN_POINT('Ctrl Pts',(0.12861328245382,-0.0781319533624403,
1.41859173947234));
#16496=CARTESIAN_POINT('Ctrl Pts',(0.1353648581188,0.0657445800149866,1.42653390759512));
#16497=CARTESIAN_POINT('Ctrl Pts',(0.0181081687242482,0.149392404544468,
1.43447607571789));
#16498=CARTESIAN_POINT('Ctrl Pts',(-0.115737181672069,0.0961812857364522,
1.44241824384068));
#16499=CARTESIAN_POINT('Ctrl Pts',(-0.143555918690644,-0.0451414811888502,
1.45036041196346));
#16500=CARTESIAN_POINT('Ctrl Pts',(-0.0398616700558823,-0.145110565703753,
1.45830258008624));
#16501=CARTESIAN_POINT('Ctrl Pts',(0.100348034367198,-0.112142416378873,
1.46624474820902));
#16502=CARTESIAN_POINT('Ctrl Pts',(0.14863229283285,0.0235577176564554,
1.4741869163318));
#16503=CARTESIAN_POINT('Ctrl Pts',(0.0607471474677608,0.137680339497592,
1.48212908445458));
#16504=CARTESIAN_POINT('Ctrl Pts',(-0.0827754224726193,0.125666453945577,
1.49007125257736));
#16505=CARTESIAN_POINT('Ctrl Pts',(-0.150492272191201,-0.00145719475437189,
1.49801342070014));
#16506=CARTESIAN_POINT('Ctrl Pts',(-0.0802951178786721,-0.12727177793954,
1.50595558882292));
#16507=CARTESIAN_POINT('Ctrl Pts',(0.0633700050447994,-0.136443062004882,
1.5138977569457));
#16508=CARTESIAN_POINT('Ctrl Pts',(0.149155357006591,-0.0207133070603065,
1.52183992506848));
#16509=CARTESIAN_POINT('Ctrl Pts',(0.0979555318420461,0.114182655252422,
1.52978209319126));
#16510=CARTESIAN_POINT('Ctrl Pts',(0.00450803278943675,0.134083974545181,
1.53507687193978));
#16511=CARTESIAN_POINT('Ctrl Pts',(-0.0361033354337414,0.122073089461022,
1.53772426131404));
#16512=CARTESIAN_POINT('Ctrl Pts',(-0.0592743564846203,0.123319225136773,
-0.00549926131403157));
#16513=CARTESIAN_POINT('Ctrl Pts',(-0.100300290071938,0.10359978715075,
-0.00285187193977157));
#16514=CARTESIAN_POINT('Ctrl Pts',(-0.160414584165772,0.0203416160441626,
0.00244290680874841));
#16515=CARTESIAN_POINT('Ctrl Pts',(-0.103922107946056,-0.124084444561314,
0.0103850749315284));
#16516=CARTESIAN_POINT('Ctrl Pts',(0.0479099321398382,-0.154436663180837,
0.0183272430543084));
#16517=CARTESIAN_POINT('Ctrl Pts',(0.155781551077148,-0.0435098515708298,
0.0262694111770884));
#16518=CARTESIAN_POINT('Ctrl Pts',(0.120977930992648,0.107381072623318,
0.0342115792998684));
#16519=CARTESIAN_POINT('Ctrl Pts',(-0.0246731903087699,0.159844935900913,
0.0421537474226484));
#16520=CARTESIAN_POINT('Ctrl Pts',(-0.147710978397823,0.0659033513787588,
0.0500959155454284));
#16521=CARTESIAN_POINT('Ctrl Pts',(-0.135435684249567,-0.0884277117007276,
0.0580380836682085));
#16522=CARTESIAN_POINT('Ctrl Pts',(0.000915427738408385,-0.16174188059703,
0.0659802517909884));
#16523=CARTESIAN_POINT('Ctrl Pts',(0.13642643003965,-0.0868880976295618,
0.0739224199137684));
#16524=CARTESIAN_POINT('Ctrl Pts',(0.146957588340267,0.0675663355536457,
0.0818645880365484));
#16525=CARTESIAN_POINT('Ctrl Pts',(0.0228600865593111,0.160121891352391,
0.0898067561593285));
#16526=CARTESIAN_POINT('Ctrl Pts',(-0.122179386207322,0.105989962368389,
0.0977489242821083));
#16527=CARTESIAN_POINT('Ctrl Pts',(-0.155290103436038,-0.0452399862206161,
0.105691092404888));
#16528=CARTESIAN_POINT('Ctrl Pts',(-0.0461390722131997,-0.155025288408554,
0.113633260527668));
#16529=CARTESIAN_POINT('Ctrl Pts',(0.105280057525145,-0.122791590307548,
0.121575428650448));
#16530=CARTESIAN_POINT('Ctrl Pts',(0.160251855424436,0.0219318669073289,
0.129517596773229));
#16531=CARTESIAN_POINT('Ctrl Pts',(0.0684164816681947,0.146563455853242,
0.137459764896008));
#16532=CARTESIAN_POINT('Ctrl Pts',(-0.086095413359615,0.136927875387926,
0.145401933018789));
#16533=CARTESIAN_POINT('Ctrl Pts',(-0.16173506727009,0.00185228698694943,
0.153344101141568));
#16534=CARTESIAN_POINT('Ctrl Pts',(-0.0892087826023274,-0.134920182928699,
0.161286269264348));
#16535=CARTESIAN_POINT('Ctrl Pts',(0.0650419110192955,-0.148091906331324,
0.169228437387128));
#16536=CARTESIAN_POINT('Ctrl Pts',(0.159707532494063,-0.025596228460074,
0.177170605509908));
#16537=CARTESIAN_POINT('Ctrl Pts',(0.108064646638443,0.120348223746572,
0.185112773632688));
#16538=CARTESIAN_POINT('Ctrl Pts',(-0.0425765573421325,0.156041339440091,
0.193054941755468));
#16539=CARTESIAN_POINT('Ctrl Pts',(-0.154213260793436,0.0487845573223287,
0.200997109878248));
#16540=CARTESIAN_POINT('Ctrl Pts',(-0.124574774400312,-0.103163891052585,
0.208939278001028));
#16541=CARTESIAN_POINT('Ctrl Pts',(0.0191870033818907,-0.160603616835255,
0.216881446123808));
#16542=CARTESIAN_POINT('Ctrl Pts',(0.145371514918136,-0.0709139301387177,
0.224823614246588));
#16543=CARTESIAN_POINT('Ctrl Pts',(0.138380784202201,0.0837402018183176,
0.232765782369368));
#16544=CARTESIAN_POINT('Ctrl Pts',(0.00461903876105218,0.161679705957985,
0.240707950492149));
#16545=CARTESIAN_POINT('Ctrl Pts',(-0.133374220718213,0.0915039894496894,
0.248650118614928));
#16546=CARTESIAN_POINT('Ctrl Pts',(-0.149182991964712,-0.0624987819548612,
0.256592286737709));
#16547=CARTESIAN_POINT('Ctrl Pts',(-0.0283248164207669,-0.159246248345813,
0.264534454860488));
#16548=CARTESIAN_POINT('Ctrl Pts',(0.118481800883715,-0.110107791262854,
0.272476622983269));
#16549=CARTESIAN_POINT('Ctrl Pts',(0.156746916480749,0.0399007144198201,
0.280418791106048));
#16550=CARTESIAN_POINT('Ctrl Pts',(0.0514157533588968,0.153356066537929,
0.288360959228829));
#16551=CARTESIAN_POINT('Ctrl Pts',(-0.101017521980764,0.126321506839912,
0.296303127351608));
#16552=CARTESIAN_POINT('Ctrl Pts',(-0.160908369261695,-0.0164365306249019,
0.304245295474388));
#16553=CARTESIAN_POINT('Ctrl Pts',(-0.0733906195540655,-0.144137017448375,
0.312187463597168));
#16554=CARTESIAN_POINT('Ctrl Pts',(0.0813604773699057,-0.13979318853071,
0.320129631719948));
#16555=CARTESIAN_POINT('Ctrl Pts',(0.161577018543625,-0.00738443741900211,
0.328071799842729));
#16556=CARTESIAN_POINT('Ctrl Pts',(0.0937724112935796,0.131789217000595,
0.336013967965508));
#16557=CARTESIAN_POINT('Ctrl Pts',(-0.0599373583072218,0.150230409426965,
0.343956136088289));
#16558=CARTESIAN_POINT('Ctrl Pts',(-0.158738350099833,0.0310451130618767,
0.351898304211068));
#16559=CARTESIAN_POINT('Ctrl Pts',(-0.112118705390683,-0.116580696253536,
0.359840472333849));
#16560=CARTESIAN_POINT('Ctrl Pts',(0.0372131918485748,-0.15740661101073,
0.367782640456628));
#16561=CARTESIAN_POINT('Ctrl Pts',(0.152453982298084,-0.0540318990865351,
0.375724808579408));
#16562=CARTESIAN_POINT('Ctrl Pts',(0.128031262769868,0.0988415833088236,
0.383666976702188));
#16563=CARTESIAN_POINT('Ctrl Pts',(-0.0136812466069205,0.161166021011634,
0.391609144824968));
#16564=CARTESIAN_POINT('Ctrl Pts',(-0.142860328563903,0.0758458262533652,
0.399551312947749));
#16565=CARTESIAN_POINT('Ctrl Pts',(-0.141164672957165,-0.0789569372907697,
0.407493481070528));
#16566=CARTESIAN_POINT('Ctrl Pts',(-0.0101476745237983,-0.161427034722196,
0.415435649193308));
#16567=CARTESIAN_POINT('Ctrl Pts',(0.130165636283581,-0.0960133843187101,
0.423377817316089));
#16568=CARTESIAN_POINT('Ctrl Pts',(0.151233851831306,0.0573583899504574,
0.431319985438868));
#16569=CARTESIAN_POINT('Ctrl Pts',(0.0337563222576384,0.158183986373718,
0.439262153561649));
#16570=CARTESIAN_POINT('Ctrl Pts',(-0.114645466422773,0.114096800420287,
0.447204321684428));
#16571=CARTESIAN_POINT('Ctrl Pts',(-0.158020229883659,-0.0345147763277912,
0.455146489807208));
#16572=CARTESIAN_POINT('Ctrl Pts',(-0.0566322287360923,-0.151507272121918,
0.463088657929988));
#16573=CARTESIAN_POINT('Ctrl Pts',(0.0966367119836487,-0.129703541718919,
0.471030826052768));
#16574=CARTESIAN_POINT('Ctrl Pts',(0.161376496659739,0.0109219578497271,
0.478972994175549));
#16575=CARTESIAN_POINT('Ctrl Pts',(0.0782788315581001,0.141541821972661,
0.486915162298328));
#16576=CARTESIAN_POINT('Ctrl Pts',(-0.0765302851406724,0.142494836024782,
0.494857330421108));
#16577=CARTESIAN_POINT('Ctrl Pts',(-0.161229798395673,0.0129079412274925,
0.502799498543889));
#16578=CARTESIAN_POINT('Ctrl Pts',(-0.0982262525537151,-0.128503953817366,
0.510741666666668));
#16579=CARTESIAN_POINT('Ctrl Pts',(0.0547626317937811,-0.152193025452748,
0.518683834789449));
#16580=CARTESIAN_POINT('Ctrl Pts',(0.157583319439253,-0.0364576503898468,
0.526626002912228));
#16581=CARTESIAN_POINT('Ctrl Pts',(0.116041497328862,0.112676677866884,
0.534568171035008));
#16582=CARTESIAN_POINT('Ctrl Pts',(-0.0318062577307366,0.158587593482618,
0.542510339157789));
#16583=CARTESIAN_POINT('Ctrl Pts',(-0.150516213127973,0.0592159811457737,
0.550452507280567));
#16584=CARTESIAN_POINT('Ctrl Pts',(-0.131337854181896,-0.0944035534094825,
0.558394675403349));
#16585=CARTESIAN_POINT('Ctrl Pts',(0.00815947204521347,-0.161539734596121,
0.566336843526128));
#16586=CARTESIAN_POINT('Ctrl Pts',(0.140181883624494,-0.080688923285235,
0.574279011648909));
#16587=CARTESIAN_POINT('Ctrl Pts',(0.143783288371658,0.0740812312429708,
0.582221179771688));
#16588=CARTESIAN_POINT('Ctrl Pts',(0.0156644295519346,0.160985367298567,
0.590163347894469));
#16589=CARTESIAN_POINT('Ctrl Pts',(-0.126804656005353,0.100410368253513,
0.598105516017247));
#16590=CARTESIAN_POINT('Ctrl Pts',(-0.153107649524464,-0.0521508436608248,
0.606047684140029));
#16591=CARTESIAN_POINT('Ctrl Pts',(-0.0391483067326994,-0.156936525122116,
0.613989852262808));
#16592=CARTESIAN_POINT('Ctrl Pts',(0.110674906884577,-0.117952226869747,
0.621932020385589));
#16593=CARTESIAN_POINT('Ctrl Pts',(0.159108535730396,0.0290884288879846,
0.629874188508368));
#16594=CARTESIAN_POINT('Ctrl Pts',(0.061782400006242,0.14948109541648,0.637816356631148));
#16595=CARTESIAN_POINT('Ctrl Pts',(-0.0921427612707386,0.132933721767072,
0.645758524753929));
#16596=CARTESIAN_POINT('Ctrl Pts',(-0.161655687038194,-0.0053945978210935,
0.653700692876707));
#16597=CARTESIAN_POINT('Ctrl Pts',(-0.0830753959589387,-0.138780911597048,
0.661642860999489));
#16598=CARTESIAN_POINT('Ctrl Pts',(0.0716104924784035,-0.145029652845349,
0.669585029122267));
#16599=CARTESIAN_POINT('Ctrl Pts',(0.160693812980115,-0.0184163326249747,
0.677527197245049));
#16600=CARTESIAN_POINT('Ctrl Pts',(0.102565092089392,0.125068240261613,
0.685469365367828));
#16601=CARTESIAN_POINT('Ctrl Pts',(-0.0495237900674707,0.153977456320057,
0.693411533490608));
#16602=CARTESIAN_POINT('Ctrl Pts',(-0.156243792750268,0.0418275036842162,
0.701353701613389));
#16603=CARTESIAN_POINT('Ctrl Pts',(-0.119828429739121,-0.108640739429086,
0.709295869736167));
#16604=CARTESIAN_POINT('Ctrl Pts',(0.0263620853553792,-0.159582904138124,
0.717238037858949));
#16605=CARTESIAN_POINT('Ctrl Pts',(0.148402221984423,-0.0643307340819919,
0.725180205981728));
#16606=CARTESIAN_POINT('Ctrl Pts',(0.134490677336207,0.0898549973406614,
0.733122374104509));
#16607=CARTESIAN_POINT('Ctrl Pts',(-0.00262814450422035,0.161724320044658,
0.741064542227287));
#16608=CARTESIAN_POINT('Ctrl Pts',(-0.137339315979238,0.0854375510170853,
0.749006710350069));
#16609=CARTESIAN_POINT('Ctrl Pts',(-0.146233564613262,-0.0691187920752458,
0.756948878472847));
#16610=CARTESIAN_POINT('Ctrl Pts',(-0.0211628449166461,-0.160355220783347,
0.764891046595629));
#16611=CARTESIAN_POINT('Ctrl Pts',(0.12329521486528,-0.104689793336152,
0.772833214718408));
#16612=CARTESIAN_POINT('Ctrl Pts',(0.154802191231926,0.0468822399980663,
0.780775382841188));
#16613=CARTESIAN_POINT('Ctrl Pts',(0.0444944569967772,0.155505325098544,
0.788717550963968));
#16614=CARTESIAN_POINT('Ctrl Pts',(-0.106574770936664,0.121669556739719,
0.796659719086747));
#16615=CARTESIAN_POINT('Ctrl Pts',(-0.160010559849905,-0.0236280251811701,
0.804601887209529));
#16616=CARTESIAN_POINT('Ctrl Pts',(-0.0668602374312443,-0.147279908636853,
0.812544055332307));
#16617=CARTESIAN_POINT('Ctrl Pts',(0.0875409312876049,-0.13600826514128,
0.820486223455089));
#16618=CARTESIAN_POINT('Ctrl Pts',(0.161745613525436,-0.000139078116330951,
0.828428391577867));
#16619=CARTESIAN_POINT('Ctrl Pts',(0.0877746970157421,0.135857518751215,
0.836370559700649));
#16620=CARTESIAN_POINT('Ctrl Pts',(-0.0666068593976089,0.147394671269449,
0.844312727823428));
#16621=CARTESIAN_POINT('Ctrl Pts',(-0.159969689820096,0.0239031624749592,
0.852254895946208));
#16622=CARTESIAN_POINT('Ctrl Pts',(-0.106783850056725,-0.121486098811777,
0.860197064068988));
#16623=CARTESIAN_POINT('Ctrl Pts',(0.0442269666803361,-0.155581612845794,
0.868139232191768));
#16624=CARTESIAN_POINT('Ctrl Pts',(0.154721338329289,-0.0471483860066884,
0.876081400314548));
#16625=CARTESIAN_POINT('Ctrl Pts',(0.123475068941597,0.104477606152275,
0.884023568437328));
#16626=CARTESIAN_POINT('Ctrl Pts',(-0.0208870486723946,0.160391377683462,
0.891965736560109));
#16627=CARTESIAN_POINT('Ctrl Pts',(-0.146114483894434,0.0693701696243073,
0.899907904682887));
#16628=CARTESIAN_POINT('Ctrl Pts',(-0.137486040957907,-0.0852012404790134,
0.907850072805669));
#16629=CARTESIAN_POINT('Ctrl Pts',(-0.00290626002629624,-0.161719561247554,
0.915792240928448));
#16630=CARTESIAN_POINT('Ctrl Pts',(0.134335953660838,-0.0900861498315643,
0.923734409051229));
#16631=CARTESIAN_POINT('Ctrl Pts',(0.148512632937768,0.0640754297319473,
0.931676577174007));
#16632=CARTESIAN_POINT('Ctrl Pts',(0.0266364831612253,0.159537332941991,
0.939618745296788));
#16633=CARTESIAN_POINT('Ctrl Pts',(-0.119641421660886,0.10884664928423,
0.947560913419568));
#16634=CARTESIAN_POINT('Ctrl Pts',(-0.156315493011378,-0.0415587473590326,
0.955503081542348));
#16635=CARTESIAN_POINT('Ctrl Pts',(-0.0497885138626987,-0.153892061929087,
0.963445249665127));
#16636=CARTESIAN_POINT('Ctrl Pts',(0.102349858952582,-0.125244437839883,
0.971387417787908));
#16637=CARTESIAN_POINT('Ctrl Pts',(0.160725246166783,0.018139958160622,
0.979329585910688));
#16638=CARTESIAN_POINT('Ctrl Pts',(0.0718597959603077,0.14490628889729,
0.987271754033468));
#16639=CARTESIAN_POINT('Ctrl Pts',(-0.0828366097831417,0.138923572215364,
0.995213922156248));
#16640=CARTESIAN_POINT('Ctrl Pts',(-0.161646170836971,0.00567259122332548,
1.00315609027903));
#16641=CARTESIAN_POINT('Ctrl Pts',(-0.0923712328620446,-0.132775066096718,
1.01109825840181));
#16642=CARTESIAN_POINT('Ctrl Pts',(0.0615252440718216,-0.149587122371362,
1.01904042652459));
#16643=CARTESIAN_POINT('Ctrl Pts',(0.159058276707423,-0.0293620068848675,
1.02698259464737));
#16644=CARTESIAN_POINT('Ctrl Pts',(0.1108775872014,0.117761723381742,1.03492476277015));
#16645=CARTESIAN_POINT('Ctrl Pts',(-0.0388783630684312,0.157003616909169,
1.04286693089293));
#16646=CARTESIAN_POINT('Ctrl Pts',(-0.153017738641585,0.0524140677533946,
1.05080909901571));
#16647=CARTESIAN_POINT('Ctrl Pts',(-0.126977145509477,-0.10019215216626,
1.05875126713849));
#16648=CARTESIAN_POINT('Ctrl Pts',(0.0153875577671049,-0.161012067570745,
1.06669343526127));
#16649=CARTESIAN_POINT('Ctrl Pts',(0.143655677305146,-0.0743283876822416,
1.07463560338405));
#16650=CARTESIAN_POINT('Ctrl Pts',(0.140320438123209,0.080447731368589,
1.08257777150683));
#16651=CARTESIAN_POINT('Ctrl Pts',(0.00843726195408678,0.161525463776335,
1.09051993962961));
#16652=CARTESIAN_POINT('Ctrl Pts',(-0.131175312957834,0.094629277223576,
1.09846210775239));
#16653=CARTESIAN_POINT('Ctrl Pts',(-0.150617825048456,-0.0589570489009974,
1.10640427587517));
#16654=CARTESIAN_POINT('Ctrl Pts',(-0.0320789358376135,-0.158532661344495,
1.11434644399795));
#16655=CARTESIAN_POINT('Ctrl Pts',(0.115847554194776,-0.112876069317329,
1.12228861212073));
#16656=CARTESIAN_POINT('Ctrl Pts',(0.157645783113317,0.0361865984037055,
1.13023078024351));
#16657=CARTESIAN_POINT('Ctrl Pts',(0.0550242791334153,0.152098624396442,
1.13817294836629));
#16658=CARTESIAN_POINT('Ctrl Pts',(-0.0980051173916675,0.128672684756662,
1.14611511648907));
#16659=CARTESIAN_POINT('Ctrl Pts',(-0.161251757937727,-0.0126306531673768,
1.15405728461185));
#16660=CARTESIAN_POINT('Ctrl Pts',(-0.0767752221903169,-0.142363015193798,
1.16199945273463));
#16661=CARTESIAN_POINT('Ctrl Pts',(0.0780353045016797,-0.141676229794458,
1.16994162085741));
#16662=CARTESIAN_POINT('Ctrl Pts',(0.161357475398708,-0.0111994629512984,
1.17788378898019));
#16663=CARTESIAN_POINT('Ctrl Pts',(0.0968596219472387,0.129537162519796,
1.18582595710297));
#16664=CARTESIAN_POINT('Ctrl Pts',(-0.0563715959749383,0.151604439264423,
1.19376812522575));
#16665=CARTESIAN_POINT('Ctrl Pts',(-0.157960640709981,0.0347864747270306,
1.20171029334853));
#16666=CARTESIAN_POINT('Ctrl Pts',(-0.114841510641486,-0.113899474410655,
1.20965246147131));
#16667=CARTESIAN_POINT('Ctrl Pts',(0.03348424129126,-0.158241803650584,
1.21759462959409));
#16668=CARTESIAN_POINT('Ctrl Pts',(0.151134988234409,-0.0576183839484237,
1.22553679771687));
#16669=CARTESIAN_POINT('Ctrl Pts',(0.130330559267559,0.0957893948119858,
1.23347896583965));
#16670=CARTESIAN_POINT('Ctrl Pts',(-0.0098700513554357,0.16144424710618,
1.24142113396243));
#16671=CARTESIAN_POINT('Ctrl Pts',(-0.141028680947982,0.0791995832534545,
1.24936330208521));
#16672=CARTESIAN_POINT('Ctrl Pts',(-0.142990550365238,-0.0756000353418,
1.25730547020799));
#16673=CARTESIAN_POINT('Ctrl Pts',(-0.013958385670676,-0.161142254877177,
1.26524763833077));
#16674=CARTESIAN_POINT('Ctrl Pts',(0.127861094297897,-0.0990616141723472,
1.27318980645355));
#16675=CARTESIAN_POINT('Ctrl Pts',(0.152546676219863,0.0537696421008814,
1.28113197457633));
#16676=CARTESIAN_POINT('Ctrl Pts',(0.0374838310097642,0.157342382244044,
1.28907414269911));
#16677=CARTESIAN_POINT('Ctrl Pts',(-0.111918054267102,0.116773335855419,
1.29701631082189));
#16678=CARTESIAN_POINT('Ctrl Pts',(-0.158791504053787,-0.0307720827589687,
1.30495847894467));
#16679=CARTESIAN_POINT('Ctrl Pts',(-0.060195622861772,-0.150127112226926,
1.31290064706745));
#16680=CARTESIAN_POINT('Ctrl Pts',(0.0935456330135535,-0.131950283756556,
1.32084281519023));
#16681=CARTESIAN_POINT('Ctrl Pts',(0.161589478720268,0.00710656041347678,
1.32878498331301));
#16682=CARTESIAN_POINT('Ctrl Pts',(0.0816007612396376,0.139653065139265,
1.33672715143579));
#16683=CARTESIAN_POINT('Ctrl Pts',(-0.0731426367739486,0.144263015132499,
1.34466931955857));
#16684=CARTESIAN_POINT('Ctrl Pts',(-0.160879865135934,0.0167132224867059,
1.35261148768135));
#16685=CARTESIAN_POINT('Ctrl Pts',(-0.101234609479067,-0.126147598829082,
1.36055365580413));
#16686=CARTESIAN_POINT('Ctrl Pts',(0.051151949184981,-0.153444260252591,
1.36849582392691));
#16687=CARTESIAN_POINT('Ctrl Pts',(0.15667806641111,-0.0401702148435725,
1.37643799204969));
#16688=CARTESIAN_POINT('Ctrl Pts',(0.118670980449659,0.10990387323047,1.38438016017247));
#16689=CARTESIAN_POINT('Ctrl Pts',(-0.0280509185434417,0.159294724422008,
1.39232232829525));
#16690=CARTESIAN_POINT('Ctrl Pts',(-0.149075287902345,0.0627552395607943,
1.40026449641803));
#16691=CARTESIAN_POINT('Ctrl Pts',(-0.133531390736797,-0.0912744851582948,
1.40820666454081));
#16692=CARTESIAN_POINT('Ctrl Pts',(0.00434100186018791,-0.161687417152987,
1.41614883266359));
#16693=CARTESIAN_POINT('Ctrl Pts',(0.138236546518021,-0.0839780402106489,
1.42409100078637));
#16694=CARTESIAN_POINT('Ctrl Pts',(0.145493297031458,0.07066380330362,1.43203316890915));
#16695=CARTESIAN_POINT('Ctrl Pts',(0.0194630807988606,0.160570430100525,
1.43997533703193));
#16696=CARTESIAN_POINT('Ctrl Pts',(-0.124397014000637,0.103377882332206,
1.44791750515471));
#16697=CARTESIAN_POINT('Ctrl Pts',(-0.15429723939393,-0.0485191136187331,
1.45585967327749));
#16698=CARTESIAN_POINT('Ctrl Pts',(-0.042844249846,-0.155968210152522,1.46380184140027));
#16699=CARTESIAN_POINT('Ctrl Pts',(0.107856400646442,-0.120533276677448,
1.47174400952305));
#16700=CARTESIAN_POINT('Ctrl Pts',(0.159753444358638,0.0253203827049868,
1.47968617764583));
#16701=CARTESIAN_POINT('Ctrl Pts',(0.0652924466007548,0.147982030257331,
1.48762834576861));
#16702=CARTESIAN_POINT('Ctrl Pts',(-0.0889689487809616,0.13506922671723,
1.49557051389139));
#16703=CARTESIAN_POINT('Ctrl Pts',(-0.161752593421533,-0.00156622680492735,
1.50351268201417));
#16704=CARTESIAN_POINT('Ctrl Pts',(-0.086303059730943,-0.136794666273195,
1.51145485013695));
#16705=CARTESIAN_POINT('Ctrl Pts',(0.0681115549116652,-0.14665217563879,
1.51939701825973));
#16706=CARTESIAN_POINT('Ctrl Pts',(0.160315645894948,-0.02226314405755,
1.52733918638251));
#16707=CARTESIAN_POINT('Ctrl Pts',(0.105284883301553,0.122726172858702,
1.53528135450529));
#16708=CARTESIAN_POINT('Ctrl Pts',(0.00484533846358528,0.144116573583224,
1.54057613325381));
#16709=CARTESIAN_POINT('Ctrl Pts',(-0.0388047044047284,0.131206995015745,
1.54322352262807));
#16710=CARTESIAN_POINT('Ctrl Pts',(-0.0634007094575145,0.131904027763688,
-3.88578058618805E-16));
#16711=CARTESIAN_POINT('Ctrl Pts',(-0.107282641710421,0.110811831533068,
0.00264738937425961));
#16712=CARTESIAN_POINT('Ctrl Pts',(-0.171581760589518,0.0217576868851663,
0.0079421681227796));
#16713=CARTESIAN_POINT('Ctrl Pts',(-0.111156590520044,-0.1327225175337,
0.0158843362455596));
#16714=CARTESIAN_POINT('Ctrl Pts',(0.0512451567233008,-0.165187689797298,
0.0238265043683396));
#16715=CARTESIAN_POINT('Ctrl Pts',(0.16662620135312,-0.0465387668729445,
0.0317686724911196));
#16716=CARTESIAN_POINT('Ctrl Pts',(0.129399745666171,0.114856349193662,
0.0397108406138996));
#16717=CARTESIAN_POINT('Ctrl Pts',(-0.026390801400978,0.170972456562021,
0.0476530087366796));
#16718=CARTESIAN_POINT('Ctrl Pts',(-0.157993800025737,0.070491178324729,
0.0555951768594596));
#16719=CARTESIAN_POINT('Ctrl Pts',(-0.144863967768493,-0.0945835600760224,
0.0635373449822396));
#16720=CARTESIAN_POINT('Ctrl Pts',(0.000979154756195248,-0.17300145605975,
0.0714795131050195));
#16721=CARTESIAN_POINT('Ctrl Pts',(0.145923683802689,-0.0929367665856833,
0.0794216812277997));
#16722=CARTESIAN_POINT('Ctrl Pts',(0.157187963117837,0.0722699302633024,
0.0873638493505794));
#16723=CARTESIAN_POINT('Ctrl Pts',(0.0244514793930555,0.171268692120756,
0.0953060174733598));
#16724=CARTESIAN_POINT('Ctrl Pts',(-0.130684839550095,0.113368397534175,
0.103248185596139));
#16725=CARTESIAN_POINT('Ctrl Pts',(-0.166100541844429,-0.0483893439312075,
0.11119035371892));
#16726=CARTESIAN_POINT('Ctrl Pts',(-0.0493510193195793,-0.165817291858885,
0.119132521841699));
#16727=CARTESIAN_POINT('Ctrl Pts',(0.112609073040783,-0.131339661914923,
0.12707468996448));
#16728=CARTESIAN_POINT('Ctrl Pts',(0.17140770357293,0.0234586422209967,
0.135016858087259));
#16729=CARTESIAN_POINT('Ctrl Pts',(0.0731792588499177,0.156766393306209,
0.14295902621004));
#16730=CARTESIAN_POINT('Ctrl Pts',(-0.0920889000195865,0.146460037003638,
0.150901194332819));
#16731=CARTESIAN_POINT('Ctrl Pts',(-0.172994168426659,0.00198123296575728,
0.1588433624556));
#16732=CARTESIAN_POINT('Ctrl Pts',(-0.0954190048152776,-0.144312580095855,
0.16678553057838));
#16733=CARTESIAN_POINT('Ctrl Pts',(0.0695697692503139,-0.158401246055831,
0.17472769870116));
#16734=CARTESIAN_POINT('Ctrl Pts',(0.170825487889685,-0.0273780963649298,
0.18266986682394));
#16735=CARTESIAN_POINT('Ctrl Pts',(0.115587509852263,0.128726201683253,
0.19061203494672));
#16736=CARTESIAN_POINT('Ctrl Pts',(-0.0455405018601966,0.16690407474553,
0.198554203069499));
#16737=CARTESIAN_POINT('Ctrl Pts',(-0.164948735370872,0.0521806684752238,
0.20649637119228));
#16738=CARTESIAN_POINT('Ctrl Pts',(-0.133246981425072,-0.110345590758605,
0.214438539315059));
#16739=CARTESIAN_POINT('Ctrl Pts',(0.0205226964731592,-0.171783952668295,
0.22238070743784));
#16740=CARTESIAN_POINT('Ctrl Pts',(0.155491476033395,-0.0758505658746651,
0.230322875560619));
#16741=CARTESIAN_POINT('Ctrl Pts',(0.148014089296488,0.0895697316726553,
0.2382650436834));
#16742=CARTESIAN_POINT('Ctrl Pts',(0.00494059070111224,0.172934953166096,
0.24620721180618));
#16743=CARTESIAN_POINT('Ctrl Pts',(-0.142658996543838,0.0978739912732451,
0.25414937992896));
#16744=CARTESIAN_POINT('Ctrl Pts',(-0.159568287038446,-0.0668496016012732,
0.262091548051739));
#16745=CARTESIAN_POINT('Ctrl Pts',(-0.0302966335331915,-0.170332091689456,
0.27003371617452));
#16746=CARTESIAN_POINT('Ctrl Pts',(0.126729848780061,-0.11777288690896,
0.2779758842973));
#16747=CARTESIAN_POINT('Ctrl Pts',(0.167658770158652,0.0426783815482623,
0.28591805242008));
#16748=CARTESIAN_POINT('Ctrl Pts',(0.0549950338320791,0.164031867990689,
0.293860220542859));
#16749=CARTESIAN_POINT('Ctrl Pts',(-0.108049803339193,0.135115311719503,
0.30180238866564));
#16750=CARTESIAN_POINT('Ctrl Pts',(-0.1721099202737,-0.0175807510100837,
0.309744556788419));
#16751=CARTESIAN_POINT('Ctrl Pts',(-0.0784996687135917,-0.154171039675278,
0.3176867249112));
#16752=CARTESIAN_POINT('Ctrl Pts',(0.087024343965547,-0.14952481740522,
0.325628893033979));
#16753=CARTESIAN_POINT('Ctrl Pts',(0.172825117221703,-0.00789850112384905,
0.33357106115676));
#16754=CARTESIAN_POINT('Ctrl Pts',(0.100300328103893,0.140963653630822,
0.341513229279539));
#16755=CARTESIAN_POINT('Ctrl Pts',(-0.0641098658012952,0.160688619913292,
0.349455397402319));
#16756=CARTESIAN_POINT('Ctrl Pts',(-0.16978883637574,0.033206302186043,
0.357397565525099));
#16757=CARTESIAN_POINT('Ctrl Pts',(-0.119923789760104,-0.124696399756661,
0.36533973364788));
#16758=CARTESIAN_POINT('Ctrl Pts',(0.0398037685148125,-0.168364388974385,
0.373281901770659));
#16759=CARTESIAN_POINT('Ctrl Pts',(0.163066985633654,-0.0577933011607096,
0.38122406989344));
#16760=CARTESIAN_POINT('Ctrl Pts',(0.136944091404129,0.10572238784759,0.38916623801622));
#16761=CARTESIAN_POINT('Ctrl Pts',(-0.0146336593526265,0.172385508313924,
0.397108406138999));
#16762=CARTESIAN_POINT('Ctrl Pts',(-0.152805474769431,0.0811257933285562,
0.40505057426178));
#16763=CARTESIAN_POINT('Ctrl Pts',(-0.150991776994562,-0.0844534827151793,
0.412992742384559));
#16764=CARTESIAN_POINT('Ctrl Pts',(-0.0108540995180527,-0.172664692355881,
0.42093491050734));
#16765=CARTESIAN_POINT('Ctrl Pts',(0.139227048201004,-0.102697305280782,
0.428877078630119));
#16766=CARTESIAN_POINT('Ctrl Pts',(0.16176191642983,0.0613513639265466,
0.4368192467529));
#16767=CARTESIAN_POINT('Ctrl Pts',(0.0361062507758455,0.169195880912067,
0.444761414875679));
#16768=CARTESIAN_POINT('Ctrl Pts',(-0.12262644992489,0.12203958882886,0.45270358299846));
#16769=CARTESIAN_POINT('Ctrl Pts',(-0.169020724600573,-0.0369175042249048,
0.460645751121239));
#16770=CARTESIAN_POINT('Ctrl Pts',(-0.0605746513833496,-0.162054370729346,
0.468587919244019));
#16771=CARTESIAN_POINT('Ctrl Pts',(0.103364025571403,-0.138732785167649,
0.4765300873668));
#16772=CARTESIAN_POINT('Ctrl Pts',(0.172610636112938,0.0116822841681558,
0.484472255489579));
#16773=CARTESIAN_POINT('Ctrl Pts',(0.083728171010617,0.151395181039277,
0.49241442361236));
#16774=CARTESIAN_POINT('Ctrl Pts',(-0.081857900459256,0.152414538660527,
0.500356591735139));
#16775=CARTESIAN_POINT('Ctrl Pts',(-0.172453725526818,0.0138065207282529,
0.50829875985792));
#16776=CARTESIAN_POINT('Ctrl Pts',(-0.105064221167447,-0.137449688588867,
0.516240927980699));
#16777=CARTESIAN_POINT('Ctrl Pts',(0.0585749034388466,-0.162787862415564,
0.52418309610348));
#16778=CARTESIAN_POINT('Ctrl Pts',(0.168553398866689,-0.0389956304370821,
0.532125264226259));
#16779=CARTESIAN_POINT('Ctrl Pts',(0.124119664784058,0.120520605195094,
0.54006743234904));
#16780=CARTESIAN_POINT('Ctrl Pts',(-0.0340204335384149,0.16962758491636,
0.548009600471819));
#16781=CARTESIAN_POINT('Ctrl Pts',(-0.160994319687769,0.0633382703503284,
0.5559517685946));
#16782=CARTESIAN_POINT('Ctrl Pts',(-0.14048086942825,-0.100975406844349,
0.563893936717379));
#16783=CARTESIAN_POINT('Ctrl Pts',(0.00872748937560605,-0.172785237771916,
0.57183610484016));
#16784=CARTESIAN_POINT('Ctrl Pts',(0.149940571302356,-0.0863060399984934,
0.579778272962939));
#16785=CARTESIAN_POINT('Ctrl Pts',(0.153792685935992,0.0792383569699183,
0.58772044108572));
#16786=CARTESIAN_POINT('Ctrl Pts',(0.0167549005293281,0.17219227848818,
0.595662609208499));
#16787=CARTESIAN_POINT('Ctrl Pts',(-0.135632095058532,0.107400382926376,
0.60360477733128));
#16788=CARTESIAN_POINT('Ctrl Pts',(-0.163766157558233,-0.0557812970565469,
0.611546945454059));
#16789=CARTESIAN_POINT('Ctrl Pts',(-0.0418735953979919,-0.167861578305293,
0.61948911357684));
#16790=CARTESIAN_POINT('Ctrl Pts',(0.118379481984711,-0.126163408751231,
0.627431281699619));
#16791=CARTESIAN_POINT('Ctrl Pts',(0.17018479228316,0.0311134044783985,
0.6353734498224));
#16792=CARTESIAN_POINT('Ctrl Pts',(0.0660833491022344,0.159887142804326,
0.643315617945179));
#16793=CARTESIAN_POINT('Ctrl Pts',(-0.0985572308567358,0.142187832491218,
0.651257786067961));
#16794=CARTESIAN_POINT('Ctrl Pts',(-0.172909262181909,-0.00577013989488307,
0.659199954190738));
#16795=CARTESIAN_POINT('Ctrl Pts',(-0.0888586457050277,-0.148442071348278,
0.667142122313521));
#16796=CARTESIAN_POINT('Ctrl Pts',(0.0765956190331784,-0.155125815413241,
0.675084290436298));
#16797=CARTESIAN_POINT('Ctrl Pts',(0.171880427770071,-0.0196983758791502,
0.683026458559081));
#16798=CARTESIAN_POINT('Ctrl Pts',(0.109705106722326,0.133774799651286,
0.690968626681858));
#16799=CARTESIAN_POINT('Ctrl Pts',(-0.0529713625168984,0.164696515493808,
0.698910794804641));
#16800=CARTESIAN_POINT('Ctrl Pts',(-0.167120621735807,0.0447393032280997,
0.706852962927418));
#16801=CARTESIAN_POINT('Ctrl Pts',(-0.12817022249092,-0.116203707037801,
0.7147951310502));
#16802=CARTESIAN_POINT('Ctrl Pts',(0.0281972679828983,-0.17069218359667,
0.722737299172979));
#16803=CARTESIAN_POINT('Ctrl Pts',(0.158733164168978,-0.0688090841067,0.73067946729576));
#16804=CARTESIAN_POINT('Ctrl Pts',(0.14385317469873,0.0961102054508026,
0.738621635418538));
#16805=CARTESIAN_POINT('Ctrl Pts',(-0.00281110139369983,0.172982673038814,
0.746563803541321));
#16806=CARTESIAN_POINT('Ctrl Pts',(-0.146900119814081,0.0913852409380608,
0.754505971664098));
#16807=CARTESIAN_POINT('Ctrl Pts',(-0.156413536862055,-0.0739304602244656,
0.762448139786881));
#16808=CARTESIAN_POINT('Ctrl Pts',(-0.0226360851712103,-0.171518264656626,
0.770390307909658));
#16809=CARTESIAN_POINT('Ctrl Pts',(0.131878346029848,-0.111977717922496,
0.778332476032441));
#16810=CARTESIAN_POINT('Ctrl Pts',(0.165578663890314,0.0501459223366878,
0.786274644155218));
#16811=CARTESIAN_POINT('Ctrl Pts',(0.047591915084802,0.166330746049129,
0.794216812278001));
#16812=CARTESIAN_POINT('Ctrl Pts',(-0.113993917241593,0.130139518573781,
0.802158980400778));
#16813=CARTESIAN_POINT('Ctrl Pts',(-0.171149610334614,-0.0252728776558711,
0.81010114852356));
#16814=CARTESIAN_POINT('Ctrl Pts',(-0.0715146774936035,-0.157532721571376,
0.818043316646339));
#16815=CARTESIAN_POINT('Ctrl Pts',(0.0936350469135118,-0.14547640857611,
0.825985484769119));
#16816=CARTESIAN_POINT('Ctrl Pts',(0.173005448853992,-0.000148759965830227,
0.8339276528919));
#16817=CARTESIAN_POINT('Ctrl Pts',(0.0938850861191564,0.145315168055841,
0.841869821014678));
#16818=CARTESIAN_POINT('Ctrl Pts',(-0.0712436606821878,0.157655473343934,
0.849811989137461));
#16819=CARTESIAN_POINT('Ctrl Pts',(-0.171105895159299,0.0255671684868261,
0.857754157260238));
#16820=CARTESIAN_POINT('Ctrl Pts',(-0.114217551294,-0.129943289319231,0.86569632538302));
#16821=CARTESIAN_POINT('Ctrl Pts',(0.0473058035714782,-0.166412344527548,
0.873638493505798));
#16822=CARTESIAN_POINT('Ctrl Pts',(0.16549218245563,-0.0504305959589149,
0.88158066162858));
#16823=CARTESIAN_POINT('Ctrl Pts',(0.132070720552549,0.111750759440056,
0.889522829751358));
#16824=CARTESIAN_POINT('Ctrl Pts',(-0.022341089517305,0.171556938600217,
0.89746499787414));
#16825=CARTESIAN_POINT('Ctrl Pts',(-0.156286166401977,0.074199337288632,
0.905407165996919));
#16826=CARTESIAN_POINT('Ctrl Pts',(-0.147057058974526,-0.0911324797668838,
0.913349334119699));
#16827=CARTESIAN_POINT('Ctrl Pts',(-0.00310857778072832,-0.172977582960567,
0.92129150224248));
#16828=CARTESIAN_POINT('Ctrl Pts',(0.143687680016546,-0.0963574495000853,
0.929233670365259));
#16829=CARTESIAN_POINT('Ctrl Pts',(0.158851261322436,0.0685360068793772,
0.93717583848804));
#16830=CARTESIAN_POINT('Ctrl Pts',(0.0284907678468484,0.170643439985825,
0.945118006610819));
#16831=CARTESIAN_POINT('Ctrl Pts',(-0.127970195944242,0.116423951198588,
0.9530601747336));
#16832=CARTESIAN_POINT('Ctrl Pts',(-0.167197313372666,-0.0444518375735043,
0.961002342856378));
#16833=CARTESIAN_POINT('Ctrl Pts',(-0.0532545149190986,-0.164605176417482,
0.96894451097916));
#16834=CARTESIAN_POINT('Ctrl Pts',(0.10947489024455,-0.133963263130763,
0.976886679101939));
#16835=CARTESIAN_POINT('Ctrl Pts',(0.1719140491614,0.0194027617526574,0.984828847224719));
#16836=CARTESIAN_POINT('Ctrl Pts',(0.0768622776450996,0.154993863549195,
0.992771015347499));
#16837=CARTESIAN_POINT('Ctrl Pts',(-0.088603236555915,0.148594663210074,
1.00071318347028));
#16838=CARTESIAN_POINT('Ctrl Pts',(-0.172899083515371,0.00606748566075909,
1.00865535159306));
#16839=CARTESIAN_POINT('Ctrl Pts',(-0.0988016073770141,-0.142018132090297,
1.01659751971584));
#16840=CARTESIAN_POINT('Ctrl Pts',(0.0658082913934689,-0.160000550769587,
1.02453968783862));
#16841=CARTESIAN_POINT('Ctrl Pts',(0.170131034504888,-0.0314060274628177,
1.0324818559614));
#16842=CARTESIAN_POINT('Ctrl Pts',(0.118596271784576,0.125959643463681,
1.04042402408418));
#16843=CARTESIAN_POINT('Ctrl Pts',(-0.0415848597483297,0.167933340651612,
1.04836619220696));
#16844=CARTESIAN_POINT('Ctrl Pts',(-0.163669987576804,0.0560628453550813,
1.05630836032974));
#16845=CARTESIAN_POINT('Ctrl Pts',(-0.135816592328243,-0.107166975841641,
1.06425052845252));
#16846=CARTESIAN_POINT('Ctrl Pts',(0.0164587544616562,-0.172220837485682,
1.0721926965753));
#16847=CARTESIAN_POINT('Ctrl Pts',(0.153656191292587,-0.0795027190739688,
1.08013486469808));
#16848=CARTESIAN_POINT('Ctrl Pts',(0.150088771199207,0.0860480576341552,
1.08807703282086));
#16849=CARTESIAN_POINT('Ctrl Pts',(0.00902461748204118,0.172769973496559,
1.09601920094364));
#16850=CARTESIAN_POINT('Ctrl Pts',(-0.140307012982855,0.101216844302358,
1.10396136906642));
#16851=CARTESIAN_POINT('Ctrl Pts',(-0.161103005268346,-0.0630613126743013,
1.1119035371892));
#16852=CARTESIAN_POINT('Ctrl Pts',(-0.0343120939874615,-0.1695688287065,
1.11984570531198));
#16853=CARTESIAN_POINT('Ctrl Pts',(0.123912220401285,-0.120733877175888,
1.12778787343476));
#16854=CARTESIAN_POINT('Ctrl Pts',(0.168620210916381,0.0387057093103061,
1.13573004155754));
#16855=CARTESIAN_POINT('Ctrl Pts',(0.0588547652196237,0.162686889679659,
1.14367220968032));
#16856=CARTESIAN_POINT('Ctrl Pts',(-0.104827691798069,0.137630165643247,
1.1516143778031));
#16857=CARTESIAN_POINT('Ctrl Pts',(-0.172477213770776,-0.0135099294065116,
1.15955654592588));
#16858=CARTESIAN_POINT('Ctrl Pts',(-0.0821198886720452,-0.152273541192125,
1.16749871404866));
#16859=CARTESIAN_POINT('Ctrl Pts',(0.083467690946984,-0.15153894559049,
1.17544088217144));
#16860=CARTESIAN_POINT('Ctrl Pts',(0.172590290696882,-0.0119791076405788,
1.18338305029422));
#16861=CARTESIAN_POINT('Ctrl Pts',(0.103602453294194,0.13855482356859,1.191325218417));
#16862=CARTESIAN_POINT('Ctrl Pts',(-0.0602958748103966,0.162158302111078,
1.19926738653978));
#16863=CARTESIAN_POINT('Ctrl Pts',(-0.168956987158091,0.0372081167644847,
1.20720955466256));
#16864=CARTESIAN_POINT('Ctrl Pts',(-0.122836141658186,-0.121828526073448,
1.21515172278534));
#16865=CARTESIAN_POINT('Ctrl Pts',(0.0358152290369173,-0.169257723108079,
1.22309389090812));
#16866=CARTESIAN_POINT('Ctrl Pts',(0.161656170495932,-0.0616294572691503,
1.2310360590309));
#16867=CARTESIAN_POINT('Ctrl Pts',(0.13940345221127,0.102457722863032,1.23897822715368));
#16868=CARTESIAN_POINT('Ctrl Pts',(-0.0105571497596809,0.172683102970871,
1.24692039527646));
#16869=CARTESIAN_POINT('Ctrl Pts',(-0.150846317973597,0.0847130203482025,
1.25486256339924));
#16870=CARTESIAN_POINT('Ctrl Pts',(-0.152944761892581,-0.0808628918127005,
1.26280473152202));
#16871=CARTESIAN_POINT('Ctrl Pts',(-0.0149300913057054,-0.172360087712588,
1.2707468996448));
#16872=CARTESIAN_POINT('Ctrl Pts',(0.136762076743997,-0.105957736043287,
1.27868906776758));
#16873=CARTESIAN_POINT('Ctrl Pts',(0.163166132393764,0.0575127872937276,
1.28663123589036));
#16874=CARTESIAN_POINT('Ctrl Pts',(0.0400932480780463,0.168295688956082,
1.29457340401314));
#16875=CARTESIAN_POINT('Ctrl Pts',(-0.119709170414695,0.124902449862528,
1.30251557213592));
#16876=CARTESIAN_POINT('Ctrl Pts',(-0.169845690614082,-0.0329142650230248,
1.3104577402587));
#16877=CARTESIAN_POINT('Ctrl Pts',(-0.0643861093061943,-0.160578131733314,
1.31839990838148));
#16878=CARTESIAN_POINT('Ctrl Pts',(0.100057762773863,-0.141135932963798,
1.32634207650426));
#16879=CARTESIAN_POINT('Ctrl Pts',(0.172838444806952,0.00760127985757451,
1.33428424462704));
#16880=CARTESIAN_POINT('Ctrl Pts',(0.0872813550697656,0.149374939398002,
1.34222641274982));
#16881=CARTESIAN_POINT('Ctrl Pts',(-0.0782344227434143,0.154305808621531,
1.3501685808726));
#16882=CARTESIAN_POINT('Ctrl Pts',(-0.172079431848303,0.0178767046294837,
1.35811074899538));
#16883=CARTESIAN_POINT('Ctrl Pts',(-0.108282003268856,-0.134929297194493,
1.36605291711816));
#16884=CARTESIAN_POINT('Ctrl Pts',(0.0547128650701426,-0.164126201264144,
1.37399508524094));
#16885=CARTESIAN_POINT('Ctrl Pts',(0.167585127127835,-0.0429666431014547,
1.38193725336372));
#16886=CARTESIAN_POINT('Ctrl Pts',(0.126932197981417,0.117554773230619,
1.3898794214865));
#16887=CARTESIAN_POINT('Ctrl Pts',(-0.0300036684000219,0.170383942402052,
1.39782158960928));
#16888=CARTESIAN_POINT('Ctrl Pts',(-0.159453085214751,0.0671239123677834,
1.40576375773206));
#16889=CARTESIAN_POINT('Ctrl Pts',(-0.142827107870127,-0.0976285101620078,
1.41370592585484));
#16890=CARTESIAN_POINT('Ctrl Pts',(0.00464319840846943,-0.172943201171859,
1.42164809397762));
#16891=CARTESIAN_POINT('Ctrl Pts',(0.147859810582222,-0.0898241270588577,
1.4295902621004));
#16892=CARTESIAN_POINT('Ctrl Pts',(0.155621735944117,0.0755830265922534,
1.43753243022318));
#16893=CARTESIAN_POINT('Ctrl Pts',(0.0208179928734729,0.171748455656582,
1.44547459834596));
#16894=CARTESIAN_POINT('Ctrl Pts',(-0.133056846329205,0.11057447892796,
1.45341676646874));
#16895=CARTESIAN_POINT('Ctrl Pts',(-0.165038560097216,-0.0518967460486161,
1.46135893459152));
#16896=CARTESIAN_POINT('Ctrl Pts',(-0.0458268296361176,-0.166825854601292,
1.4693011027143));
#16897=CARTESIAN_POINT('Ctrl Pts',(0.115364766925686,-0.128924136976022,
1.47724327083708));
#16898=CARTESIAN_POINT('Ctrl Pts',(0.170874595884426,0.0270830477535184,
1.48518543895986));
#16899=CARTESIAN_POINT('Ctrl Pts',(0.0698377457337486,0.158283721017069,
1.49312760708264));
#16900=CARTESIAN_POINT('Ctrl Pts',(-0.0951624750893037,0.144471999488883,
1.50106977520542));
#16901=CARTESIAN_POINT('Ctrl Pts',(-0.173012914651864,-0.00167525885548286,
1.5090119433282));
#16902=CARTESIAN_POINT('Ctrl Pts',(-0.092311001583214,-0.14631755460685,
1.51695411145098));
#16903=CARTESIAN_POINT('Ctrl Pts',(0.072853104778531,-0.156861289272697,
1.52489627957376));
#16904=CARTESIAN_POINT('Ctrl Pts',(0.171475934783304,-0.0238129810547936,
1.53283844769654));
#16905=CARTESIAN_POINT('Ctrl Pts',(0.11261423476106,0.131269690464983,1.54078061581932));
#16906=CARTESIAN_POINT('Ctrl Pts',(0.00518264413773371,0.154149172621267,
1.54607539456784));
#16907=CARTESIAN_POINT('Ctrl Pts',(-0.0415060733757155,0.140340900570467,
1.5487227839421));
#16908=CARTESIAN_POINT('Ctrl Pts',(-0.146248097568756,-0.000123763188177425,
1.45893449541571));
#16909=CARTESIAN_POINT('Ctrl Pts',(-0.146367493381718,-0.0150081347743067,
1.45974264180765));
#16910=CARTESIAN_POINT('Ctrl Pts',(-0.144277648885518,-0.0298597803798721,
1.46055078819958));
#16911=CARTESIAN_POINT('Ctrl Pts',(-0.139839652725699,-0.043973059977961,
1.46135893459152));
#16912=CARTESIAN_POINT('Ctrl Pts',(-0.125301316610186,-0.0902064488995044,
1.46400632396578));
#16913=CARTESIAN_POINT('Ctrl Pts',(-0.08556407312315,-0.1285161517504,1.46665371334004));
#16914=CARTESIAN_POINT('Ctrl Pts',(-0.0388301852859989,-0.141354050238301,
1.4693011027143));
#16915=CARTESIAN_POINT('Ctrl Pts',(0.00790370255115092,-0.154191948726202,
1.47194849208856));
#16916=CARTESIAN_POINT('Ctrl Pts',(0.0616342347384179,-0.141558042851112,
1.47459588146282));
#16917=CARTESIAN_POINT('Ctrl Pts',(0.0977511389918415,-0.109239892458645,
1.47724327083708));
#16918=CARTESIAN_POINT('Ctrl Pts',(0.133868043245265,-0.0769217420661769,
1.47989066021134));
#16919=CARTESIAN_POINT('Ctrl Pts',(0.152371319564846,-0.024919347156331,
1.4825380495856));
#16920=CARTESIAN_POINT('Ctrl Pts',(0.144783482699524,0.0229486291758506,
1.48518543895986));
#16921=CARTESIAN_POINT('Ctrl Pts',(0.137195645834202,0.0708166055080336,
1.48783282833412));
#16922=CARTESIAN_POINT('Ctrl Pts',(0.103516695783975,0.114550163262552,
1.49048021770838));
#16923=CARTESIAN_POINT('Ctrl Pts',(0.0591771839550196,0.13411498855178,
1.49312760708264));
#16924=CARTESIAN_POINT('Ctrl Pts',(0.014837672126065,0.153679813841007,
1.4957749964569));
#16925=CARTESIAN_POINT('Ctrl Pts',(-0.0401624014816186,0.149075906664945,
1.49842238583116));
#16926=CARTESIAN_POINT('Ctrl Pts',(-0.0806375115458872,0.122416076686187,
1.50106977520542));
#16927=CARTESIAN_POINT('Ctrl Pts',(-0.0937869288003098,0.113754921033589,
1.50192985013695));
#16928=CARTESIAN_POINT('Ctrl Pts',(-0.105403311347291,0.102765876910903,
1.50278992506847));
#16929=CARTESIAN_POINT('Ctrl Pts',(-0.115078604842433,0.0902138214954038,
1.50365));
#16930=CARTESIAN_POINT('Ctrl Pts',(-0.0686146973663081,-0.0959584553529135,
1.07336015076065E-17));
#16931=CARTESIAN_POINT('Ctrl Pts',(-0.0712979561985307,-0.0944995001033786,
9.02613639135873E-18));
#16932=CARTESIAN_POINT('Ctrl Pts',(-0.0739152333025289,-0.0929325179580126,
1.64107321374712E-17));
#16933=CARTESIAN_POINT('Ctrl Pts',(-0.0764591723283171,-0.0912589988675934,
1.6154612370034E-17));
#16934=CARTESIAN_POINT('Ctrl Pts',(-0.0824897891353913,-0.0872917841461184,
1.52077426268717E-17));
#16935=CARTESIAN_POINT('Ctrl Pts',(-0.0881090519769445,-0.0827275518978924,
1.30971627060498E-17));
#16936=CARTESIAN_POINT('Ctrl Pts',(-0.0932912133381108,-0.0776621329443405,
1.43114686768087E-17));
#16937=CARTESIAN_POINT('Ctrl Pts',(-0.0960634919631888,-0.074952307504085,
1.49610807310118E-17));
#16938=CARTESIAN_POINT('Ctrl Pts',(-0.0987043519497191,-0.0721043812799658,
1.74993329480528E-17));
#16939=CARTESIAN_POINT('Ctrl Pts',(-0.101206237074718,-0.0691378820326018,
9.97465998686664E-18));
#16940=CARTESIAN_POINT('Ctrl Pts',(-0.105823426721714,-0.0636632543305198,
-3.91200561030858E-18));
#16941=CARTESIAN_POINT('Ctrl Pts',(-0.109972666997065,-0.0577811896139199,
2.24798207762934E-18));
#16942=CARTESIAN_POINT('Ctrl Pts',(-0.113625452403263,-0.0515741981665521,
9.54097911787244E-18));
#16943=CARTESIAN_POINT('Ctrl Pts',(-0.115386295340069,-0.0485820878086944,
1.30566037435822E-17));
#16944=CARTESIAN_POINT('Ctrl Pts',(-0.117027309103105,-0.0455212415157476,
-2.79521757168051E-18));
#16945=CARTESIAN_POINT('Ctrl Pts',(-0.118543833519887,-0.0424058589801268,
-3.46944695195361E-18));
#16946=CARTESIAN_POINT('Ctrl Pts',(-0.122700941917732,-0.0338659484069709,
-5.31764971597768E-18));
#16947=CARTESIAN_POINT('Ctrl Pts',(-0.125931492798984,-0.0249085743588085,
-1.15219401683824E-18));
#16948=CARTESIAN_POINT('Ctrl Pts',(-0.128167520083254,-0.0157105262534848,
9.54097911787244E-18));
#16949=CARTESIAN_POINT('Ctrl Pts',(-0.128992166906242,-0.0123182862745252,
1.3484621181291E-17));
#16950=CARTESIAN_POINT('Ctrl Pts',(-0.129681150280034,-0.00889298553317688,
1.10989611676181E-17));
#16951=CARTESIAN_POINT('Ctrl Pts',(-0.130229483957028,-0.00544263935519351,
9.54097911787244E-18));
#16952=CARTESIAN_POINT('Ctrl Pts',(-0.130761899349706,-0.00209245771889707,
8.02822573502553E-18));
#16953=CARTESIAN_POINT('Ctrl Pts',(-0.131160261982709,0.00127366115726457,
1.11791151702242E-17));
#16954=CARTESIAN_POINT('Ctrl Pts',(-0.131420990891747,0.00464012593483382,
8.67361737988404E-18));
#16955=CARTESIAN_POINT('Ctrl Pts',(-0.131728666658755,0.00861275649723166,
5.71697955546795E-18));
#16956=CARTESIAN_POINT('Ctrl Pts',(-0.131845259942619,0.0125891451047215,
-9.26473565962443E-18));
#16957=CARTESIAN_POINT('Ctrl Pts',(-0.131765781147177,0.0165567997877194,
-1.04083408558608E-17));
#16958=CARTESIAN_POINT('Ctrl Pts',(-0.131635692412819,0.0230509492424239,
-1.21888544026837E-17));
#16959=CARTESIAN_POINT('Ctrl Pts',(-0.13098103789945,0.0295216962360144,
-2.67049856555875E-17));
#16960=CARTESIAN_POINT('Ctrl Pts',(-0.129839098367345,0.0359278479980343,
-3.46944695195361E-17));
#16961=CARTESIAN_POINT('Ctrl Pts',(-0.129254890951344,0.0392051855997028,
-3.87818275556788E-17));
#16962=CARTESIAN_POINT('Ctrl Pts',(-0.128542951403208,0.0424656461998481,
-3.10678831811161E-17));
#16963=CARTESIAN_POINT('Ctrl Pts',(-0.1277070993652,0.0457037274559979,
-3.29597460435593E-17));
#16964=CARTESIAN_POINT('Ctrl Pts',(-0.126886363095037,0.0488832504000222,
-3.48173959609792E-17));
#16965=CARTESIAN_POINT('Ctrl Pts',(-0.125948031872817,0.0520333657183593,
-3.53366201082739E-17));
#16966=CARTESIAN_POINT('Ctrl Pts',(-0.124899042599898,0.0551436241923499,
-3.46944695195361E-17));
#16967=CARTESIAN_POINT('Ctrl Pts',(-0.122234979928128,0.0630425834229368,
-3.30636335736642E-17));
#16968=CARTESIAN_POINT('Ctrl Pts',(-0.118856305871375,0.070695441500891,
-2.1366080483524E-17));
#16969=CARTESIAN_POINT('Ctrl Pts',(-0.114834854776346,0.078019637496205,
-1.73472347597681E-17));
#16970=CARTESIAN_POINT('Ctrl Pts',(-0.11215901866562,0.0828930893082948,
-1.46731322388254E-17));
#16971=CARTESIAN_POINT('Ctrl Pts',(-0.109198005187061,0.0876211033078822,
8.28606628989234E-18));
#16972=CARTESIAN_POINT('Ctrl Pts',(-0.105966883726074,0.0921780034666525,
8.67361737988404E-18));
#16973=CARTESIAN_POINT('Ctrl Pts',(-0.104137243112614,0.094758373688769,
8.89307035390601E-18));
#16974=CARTESIAN_POINT('Ctrl Pts',(-0.102221042121924,0.0972831505018574,
-2.31209379389524E-17));
#16975=CARTESIAN_POINT('Ctrl Pts',(-0.100229777791505,0.0997373632832089,
-2.08166817117217E-17));
#16976=CARTESIAN_POINT('Ctrl Pts',(-0.0937202782075859,0.107760254486057,
-1.32840027382311E-17));
#16977=CARTESIAN_POINT('Ctrl Pts',(-0.0863914655699752,0.115060936709644,
5.4842312373535E-18));
#16978=CARTESIAN_POINT('Ctrl Pts',(-0.0783508402622743,0.121487309774744,
1.38777878078145E-17));
#16979=CARTESIAN_POINT('Ctrl Pts',(-0.073610711791116,0.125275800441382,
1.8825977152717E-17));
#16980=CARTESIAN_POINT('Ctrl Pts',(-0.068622257850438,0.128760167547443,
-9.09579695168528E-18));
#16981=CARTESIAN_POINT('Ctrl Pts',(-0.0634007094575209,0.131904027763685,
-6.93889390390723E-18));
#16982=CARTESIAN_POINT('Origin',(0.,0.,0.));
#16983=CARTESIAN_POINT('Origin',(-0.0721687836487033,-0.125,-0.3));
#16984=CARTESIAN_POINT('',(-0.0721687836487033,-0.125,-0.3));
#16985=CARTESIAN_POINT('',(0.0721687836487032,-0.125,-0.3));
#16986=CARTESIAN_POINT('',(-0.0360843918243517,-0.125,-0.3));
#16987=CARTESIAN_POINT('',(-0.0721687836487033,-0.125,-0.15));
#16988=CARTESIAN_POINT('',(-0.0721687836487033,-0.125,-0.3));
#16989=CARTESIAN_POINT('',(0.0721687836487032,-0.125,-0.15));
#16990=CARTESIAN_POINT('',(-0.0721687836487033,-0.125,-0.15));
#16991=CARTESIAN_POINT('',(0.0721687836487032,-0.125,-0.3));
#16992=CARTESIAN_POINT('Origin',(-0.144337567297406,1.76762539787485E-17,
-0.3));
#16993=CARTESIAN_POINT('',(-0.144337567297406,1.76762539787485E-17,-0.3));
#16994=CARTESIAN_POINT('',(-0.126295371385231,-0.03125,-0.3));
#16995=CARTESIAN_POINT('',(-0.144337567297406,2.77555756156289E-17,-0.15));
#16996=CARTESIAN_POINT('',(-0.144337567297406,1.76762539787485E-17,-0.3));
#16997=CARTESIAN_POINT('',(-0.144337567297406,1.76762539787485E-17,-0.15));
#16998=CARTESIAN_POINT('Origin',(-0.0721687836487032,0.125,-0.3));
#16999=CARTESIAN_POINT('',(-0.0721687836487032,0.125,-0.3));
#17000=CARTESIAN_POINT('',(-0.090210979560879,0.09375,-0.3));
#17001=CARTESIAN_POINT('',(-0.0721687836487032,0.125,-0.15));
#17002=CARTESIAN_POINT('',(-0.0721687836487032,0.125,-0.3));
#17003=CARTESIAN_POINT('',(-0.0721687836487032,0.125,-0.15));
#17004=CARTESIAN_POINT('Origin',(0.0721687836487032,0.125,-0.3));
#17005=CARTESIAN_POINT('',(0.0721687836487032,0.125,-0.3));
#17006=CARTESIAN_POINT('',(0.0360843918243516,0.125,-0.3));
#17007=CARTESIAN_POINT('',(0.0721687836487032,0.125,-0.15));
#17008=CARTESIAN_POINT('',(0.0721687836487032,0.125,-0.3));
#17009=CARTESIAN_POINT('',(0.0721687836487032,0.125,-0.15));
#17010=CARTESIAN_POINT('Origin',(0.144337567297406,0.,-0.3));
#17011=CARTESIAN_POINT('',(0.144337567297406,0.,-0.3));
#17012=CARTESIAN_POINT('',(0.126295371385231,0.03125,-0.3));
#17013=CARTESIAN_POINT('',(0.144337567297406,0.,-0.15));
#17014=CARTESIAN_POINT('',(0.144337567297406,0.,-0.3));
#17015=CARTESIAN_POINT('',(0.144337567297406,0.,-0.15));
#17016=CARTESIAN_POINT('Origin',(0.0721687836487032,-0.125,-0.3));
#17017=CARTESIAN_POINT('',(0.0902109795608791,-0.09375,-0.3));
#17018=CARTESIAN_POINT('',(0.0721687836487032,-0.125,-0.15));
#17019=CARTESIAN_POINT('Origin',(0.,0.,-0.15));
#17020=CARTESIAN_POINT('Origin',(0.,0.,0.));
#17021=CARTESIAN_POINT('',(-0.275,-3.36777869765522E-17,0.));
#17022=CARTESIAN_POINT('Origin',(0.,0.,0.));
#17023=CARTESIAN_POINT('Origin',(0.,0.,-0.3));
#17024=CARTESIAN_POINT('',(-0.275,-3.36777869765522E-17,-0.3));
#17025=CARTESIAN_POINT('',(-0.275,-3.36777869765522E-17,-0.3));
#17026=CARTESIAN_POINT('Origin',(0.,0.,-0.3));
#17027=CARTESIAN_POINT('Origin',(0.,0.,-0.3));
#17028=CARTESIAN_POINT('Origin',(0.,0.,1.6));
#18564=UNCERTAINTY_MEASURE_WITH_UNIT(LENGTH_MEASURE(0.001),#18581,
'DISTANCE_ACCURACY_VALUE',
'Maximum model space distance between geometric entities at asserted c
onnectivities');
#18568=UNCERTAINTY_MEASURE_WITH_UNIT(LENGTH_MEASURE(0.001),#18581,
'DISTANCE_ACCURACY_VALUE',
'Maximum model space distance between geometric entities at asserted c
onnectivities');
#18576=(
GEOMETRIC_REPRESENTATION_CONTEXT(3)
GLOBAL_UNCERTAINTY_ASSIGNED_CONTEXT((#18564))
GLOBAL_UNIT_ASSIGNED_CONTEXT((#18581,#18583,#18584))
REPRESENTATION_CONTEXT('','3D')
);
#18580=(
GEOMETRIC_REPRESENTATION_CONTEXT(3)
GLOBAL_UNCERTAINTY_ASSIGNED_CONTEXT((#18568))
GLOBAL_UNIT_ASSIGNED_CONTEXT((#18581,#18583,#18584))
REPRESENTATION_CONTEXT('','3D')
);
#18581=(
LENGTH_UNIT()
NAMED_UNIT(*)
SI_UNIT(.CENTI.,.METRE.)
);
#18583=(
NAMED_UNIT(*)
PLANE_ANGLE_UNIT()
SI_UNIT($,.RADIAN.)
);
#18584=(
NAMED_UNIT(*)
SI_UNIT($,.STERADIAN.)
SOLID_ANGLE_UNIT()
);
#18592=SHAPE_DEFINITION_REPRESENTATION(#18603,#18630);
#18603=PRODUCT_DEFINITION_SHAPE('',$,#18642);
#18630=SHAPE_REPRESENTATION('',(#6948),#18576);
#18634=PRODUCT_DEFINITION_CONTEXT('part definition',#18669,'design');
#18642=PRODUCT_DEFINITION('2026-11-10-05-09-36-733',
'Socket head cap screw M3x16',#18653,#18634);
#18653=PRODUCT_DEFINITION_FORMATION('',$,#18678);
#18669=APPLICATION_CONTEXT(
'Core Data for Automotive Mechanical Design Process');
#18670=PRODUCT_CONTEXT('part definition',#18669,'mechanical');
#18678=PRODUCT('2026-11-10-05-09-36-733','Socket head cap screw M3x16',
$,(#18670));
#18685=PRESENTATION_STYLE_ASSIGNMENT((#18693));
#18693=SURFACE_STYLE_USAGE(.BOTH.,#18701);
#18701=SURFACE_SIDE_STYLE('',(#18709));
#18709=SURFACE_STYLE_FILL_AREA(#18717);
#18717=FILL_AREA_STYLE('Dark gray',(#18725));
#18725=FILL_AREA_STYLE_COLOUR('Dark gray',#18733);
#18733=COLOUR_RGB('Dark gray',0.250980392156863,0.282352941176471,0.32156862745098);
ENDSEC;
END-ISO-10303-21;
